ISO-10303-21;
HEADER;
/* Generated by software containing ST-Developer
 * from STEP Tools, Inc. (www.steptools.com) 
 */

FILE_DESCRIPTION(
/* description */ (''),
/* implementation_level */ '2;1');

FILE_NAME(
/* name */ '20_Rear_Cap_Screw_ISO_4762_M6x20.step',
/* time_stamp */ '2026-10-26T03:50:32-07:00',
/* author */ (''),
/* organization */ (''),
/* preprocessor_version */ 'ST-DEVELOPER v20.2',
/* originating_system */ 'Autodesk Translation Framework v15.15.0.0',
/* authorisation */ '');

FILE_SCHEMA (('AUTOMOTIVE_DESIGN { 1 0 10303 214 3 1 1 }'));
ENDSEC;

DATA;
#10=MECHANICAL_DESIGN_GEOMETRIC_PRESENTATION_REPRESENTATION('',(#1058),#76660);
#172=B_SPLINE_SURFACE_WITH_KNOTS('',3,3,((#74631,#74632,#74633,#74634,#74635,
#74636,#74637,#74638,#74639,#74640,#74641,#74642,#74643,#74644,#74645,#74646,
#74647,#74648,#74649,#74650,#74651,#74652,#74653,#74654,#74655,#74656,#74657,
#74658,#74659,#74660,#74661,#74662,#74663,#74664,#74665,#74666,#74667,#74668,
#74669,#74670,#74671,#74672,#74673,#74674,#74675,#74676,#74677,#74678,#74679,
#74680,#74681,#74682,#74683,#74684,#74685,#74686,#74687,#74688,#74689,#74690,
#74691,#74692,#74693,#74694,#74695,#74696,#74697,#74698,#74699,#74700,#74701,
#74702,#74703,#74704,#74705,#74706,#74707,#74708,#74709,#74710,#74711,#74712,
#74713,#74714,#74715,#74716,#74717,#74718,#74719,#74720,#74721,#74722,#74723,
#74724,#74725,#74726,#74727,#74728,#74729,#74730,#74731,#74732,#74733,#74734,
#74735,#74736,#74737,#74738,#74739,#74740,#74741,#74742,#74743,#74744,#74745,
#74746,#74747,#74748,#74749,#74750,#74751,#74752,#74753,#74754,#74755,#74756,
#74757),(#74758,#74759,#74760,#74761,#74762,#74763,#74764,#74765,#74766,
#74767,#74768,#74769,#74770,#74771,#74772,#74773,#74774,#74775,#74776,#74777,
#74778,#74779,#74780,#74781,#74782,#74783,#74784,#74785,#74786,#74787,#74788,
#74789,#74790,#74791,#74792,#74793,#74794,#74795,#74796,#74797,#74798,#74799,
#74800,#74801,#74802,#74803,#74804,#74805,#74806,#74807,#74808,#74809,#74810,
#74811,#74812,#74813,#74814,#74815,#74816,#74817,#74818,#74819,#74820,#74821,
#74822,#74823,#74824,#74825,#74826,#74827,#74828,#74829,#74830,#74831,#74832,
#74833,#74834,#74835,#74836,#74837,#74838,#74839,#74840,#74841,#74842,#74843,
#74844,#74845,#74846,#74847,#74848,#74849,#74850,#74851,#74852,#74853,#74854,
#74855,#74856,#74857,#74858,#74859,#74860,#74861,#74862,#74863,#74864,#74865,
#74866,#74867,#74868,#74869,#74870,#74871,#74872,#74873,#74874,#74875,#74876,
#74877,#74878,#74879,#74880,#74881,#74882,#74883,#74884),(#74885,#74886,
#74887,#74888,#74889,#74890,#74891,#74892,#74893,#74894,#74895,#74896,#74897,
#74898,#74899,#74900,#74901,#74902,#74903,#74904,#74905,#74906,#74907,#74908,
#74909,#74910,#74911,#74912,#74913,#74914,#74915,#74916,#74917,#74918,#74919,
#74920,#74921,#74922,#74923,#74924,#74925,#74926,#74927,#74928,#74929,#74930,
#74931,#74932,#74933,#74934,#74935,#74936,#74937,#74938,#74939,#74940,#74941,
#74942,#74943,#74944,#74945,#74946,#74947,#74948,#74949,#74950,#74951,#74952,
#74953,#74954,#74955,#74956,#74957,#74958,#74959,#74960,#74961,#74962,#74963,
#74964,#74965,#74966,#74967,#74968,#74969,#74970,#74971,#74972,#74973,#74974,
#74975,#74976,#74977,#74978,#74979,#74980,#74981,#74982,#74983,#74984,#74985,
#74986,#74987,#74988,#74989,#74990,#74991,#74992,#74993,#74994,#74995,#74996,
#74997,#74998,#74999,#75000,#75001,#75002,#75003,#75004,#75005,#75006,#75007,
#75008,#75009,#75010,#75011),(#75012,#75013,#75014,#75015,#75016,#75017,
#75018,#75019,#75020,#75021,#75022,#75023,#75024,#75025,#75026,#75027,#75028,
#75029,#75030,#75031,#75032,#75033,#75034,#75035,#75036,#75037,#75038,#75039,
#75040,#75041,#75042,#75043,#75044,#75045,#75046,#75047,#75048,#75049,#75050,
#75051,#75052,#75053,#75054,#75055,#75056,#75057,#75058,#75059,#75060,#75061,
#75062,#75063,#75064,#75065,#75066,#75067,#75068,#75069,#75070,#75071,#75072,
#75073,#75074,#75075,#75076,#75077,#75078,#75079,#75080,#75081,#75082,#75083,
#75084,#75085,#75086,#75087,#75088,#75089,#75090,#75091,#75092,#75093,#75094,
#75095,#75096,#75097,#75098,#75099,#75100,#75101,#75102,#75103,#75104,#75105,
#75106,#75107,#75108,#75109,#75110,#75111,#75112,#75113,#75114,#75115,#75116,
#75117,#75118,#75119,#75120,#75121,#75122,#75123,#75124,#75125,#75126,#75127,
#75128,#75129,#75130,#75131,#75132,#75133,#75134,#75135,#75136,#75137,#75138)),
 .UNSPECIFIED.,.F.,.F.,.F.,(4,4),(4,1,1,1,1,1,1,1,1,1,1,1,1,1,1,1,1,1,1,
1,1,1,1,1,1,1,1,1,1,1,1,1,1,1,1,1,1,1,1,1,1,1,1,1,1,1,1,1,1,1,1,1,1,1,1,
1,1,1,1,1,1,1,1,1,1,1,1,1,1,1,1,1,1,1,1,1,1,1,1,1,1,1,1,1,1,1,1,1,1,1,1,
1,1,1,1,1,1,1,1,1,1,1,1,1,1,1,1,1,1,1,1,1,1,1,1,1,1,1,1,1,1,1,1,1,4),(0.,
0.0658467982010767),(8.30747755240103,9.30251287567468,10.2975481989483,
11.292583522222,12.2876188454956,13.2826541687693,14.2776894920429,15.2727248153166,
16.2677601385902,17.2627954618639,18.2578307851375,19.2528661084112,20.2479014316848,
21.2429367549585,22.2379720782321,23.2330074015058,24.2280427247794,25.2230780480531,
26.2181133713267,27.2131486946004,28.208184017874,29.2032193411477,30.1982546644213,
31.193289987695,32.1883253109686,33.1833606342423,34.1783959575159,35.1734312807896,
36.1684666040632,37.1635019273369,38.1585372506105,39.1535725738842,40.1486078971578,
41.1436432204315,42.1386785437051,43.1337138669788,44.1287491902524,45.1237845135261,
46.1188198367997,47.1138551600734,48.108890483347,49.1039258066207,50.0989611298943,
51.093996453168,52.0890317764416,53.0840670997153,54.0791024229889,55.0741377462626,
56.0691730695362,57.0642083928099,58.0592437160835,59.0542790393572,60.0493143626308,
61.0443496859045,62.0393850091781,63.0344203324518,64.0294556557254,65.0244909789991,
66.0195263022727,67.0145616255464,68.00959694882,69.0046322720937,69.9996675953673,
70.994702918641,71.9897382419146,72.9847735651883,73.9798088884619,74.9748442117356,
75.9698795350092,76.9649148582829,77.9599501815565,78.9549855048302,79.9500208281038,
80.9450561513775,81.9400914746511,82.9351267979248,83.9301621211984,84.9251974444721,
85.9202327677457,86.9152680910194,87.910303414293,88.9053387375667,89.9003740608403,
90.895409384114,91.8904447073876,92.8854800306613,93.8805153539349,94.8755506772086,
95.8705860004822,96.8656213237559,97.8606566470295,98.8556919703032,99.8507272935768,
100.84576261685,101.840797940124,102.835833263398,103.830868586671,104.825903909945,
105.820939233219,106.815974556492,107.811009879766,108.80604520304,109.801080526313,
110.796115849587,111.791151172861,112.786186496134,113.781221819408,114.776257142682,
115.771292465955,116.766327789229,117.761363112503,118.756398435776,119.75143375905,
120.746469082323,121.741504405597,122.736539728871,123.731575052144,124.726610375418,
125.721645698692,126.716681021965,127.711716345239,128.706751668513,129.701786991786,
130.69682231506,131.691857638334),.UNSPECIFIED.);
#173=B_SPLINE_SURFACE_WITH_KNOTS('',3,3,((#75281,#75282,#75283,#75284,#75285,
#75286,#75287,#75288,#75289,#75290,#75291,#75292,#75293,#75294,#75295,#75296,
#75297,#75298,#75299,#75300,#75301,#75302,#75303,#75304,#75305,#75306,#75307,
#75308,#75309,#75310,#75311,#75312,#75313,#75314,#75315,#75316,#75317,#75318,
#75319,#75320,#75321,#75322,#75323,#75324,#75325,#75326,#75327,#75328,#75329,
#75330,#75331,#75332,#75333,#75334,#75335,#75336,#75337,#75338,#75339,#75340,
#75341,#75342,#75343,#75344,#75345,#75346,#75347,#75348,#75349,#75350,#75351,
#75352,#75353,#75354,#75355,#75356,#75357,#75358,#75359,#75360,#75361,#75362,
#75363,#75364,#75365,#75366,#75367,#75368,#75369,#75370,#75371,#75372,#75373,
#75374,#75375,#75376,#75377,#75378,#75379,#75380,#75381,#75382,#75383,#75384,
#75385,#75386,#75387,#75388,#75389,#75390,#75391,#75392,#75393,#75394,#75395,
#75396,#75397,#75398,#75399,#75400,#75401,#75402,#75403,#75404,#75405,#75406,
#75407),(#75408,#75409,#75410,#75411,#75412,#75413,#75414,#75415,#75416,
#75417,#75418,#75419,#75420,#75421,#75422,#75423,#75424,#75425,#75426,#75427,
#75428,#75429,#75430,#75431,#75432,#75433,#75434,#75435,#75436,#75437,#75438,
#75439,#75440,#75441,#75442,#75443,#75444,#75445,#75446,#75447,#75448,#75449,
#75450,#75451,#75452,#75453,#75454,#75455,#75456,#75457,#75458,#75459,#75460,
#75461,#75462,#75463,#75464,#75465,#75466,#75467,#75468,#75469,#75470,#75471,
#75472,#75473,#75474,#75475,#75476,#75477,#75478,#75479,#75480,#75481,#75482,
#75483,#75484,#75485,#75486,#75487,#75488,#75489,#75490,#75491,#75492,#75493,
#75494,#75495,#75496,#75497,#75498,#75499,#75500,#75501,#75502,#75503,#75504,
#75505,#75506,#75507,#75508,#75509,#75510,#75511,#75512,#75513,#75514,#75515,
#75516,#75517,#75518,#75519,#75520,#75521,#75522,#75523,#75524,#75525,#75526,
#75527,#75528,#75529,#75530,#75531,#75532,#75533,#75534),(#75535,#75536,
#75537,#75538,#75539,#75540,#75541,#75542,#75543,#75544,#75545,#75546,#75547,
#75548,#75549,#75550,#75551,#75552,#75553,#75554,#75555,#75556,#75557,#75558,
#75559,#75560,#75561,#75562,#75563,#75564,#75565,#75566,#75567,#75568,#75569,
#75570,#75571,#75572,#75573,#75574,#75575,#75576,#75577,#75578,#75579,#75580,
#75581,#75582,#75583,#75584,#75585,#75586,#75587,#75588,#75589,#75590,#75591,
#75592,#75593,#75594,#75595,#75596,#75597,#75598,#75599,#75600,#75601,#75602,
#75603,#75604,#75605,#75606,#75607,#75608,#75609,#75610,#75611,#75612,#75613,
#75614,#75615,#75616,#75617,#75618,#75619,#75620,#75621,#75622,#75623,#75624,
#75625,#75626,#75627,#75628,#75629,#75630,#75631,#75632,#75633,#75634,#75635,
#75636,#75637,#75638,#75639,#75640,#75641,#75642,#75643,#75644,#75645,#75646,
#75647,#75648,#75649,#75650,#75651,#75652,#75653,#75654,#75655,#75656,#75657,
#75658,#75659,#75660,#75661),(#75662,#75663,#75664,#75665,#75666,#75667,
#75668,#75669,#75670,#75671,#75672,#75673,#75674,#75675,#75676,#75677,#75678,
#75679,#75680,#75681,#75682,#75683,#75684,#75685,#75686,#75687,#75688,#75689,
#75690,#75691,#75692,#75693,#75694,#75695,#75696,#75697,#75698,#75699,#75700,
#75701,#75702,#75703,#75704,#75705,#75706,#75707,#75708,#75709,#75710,#75711,
#75712,#75713,#75714,#75715,#75716,#75717,#75718,#75719,#75720,#75721,#75722,
#75723,#75724,#75725,#75726,#75727,#75728,#75729,#75730,#75731,#75732,#75733,
#75734,#75735,#75736,#75737,#75738,#75739,#75740,#75741,#75742,#75743,#75744,
#75745,#75746,#75747,#75748,#75749,#75750,#75751,#75752,#75753,#75754,#75755,
#75756,#75757,#75758,#75759,#75760,#75761,#75762,#75763,#75764,#75765,#75766,
#75767,#75768,#75769,#75770,#75771,#75772,#75773,#75774,#75775,#75776,#75777,
#75778,#75779,#75780,#75781,#75782,#75783,#75784,#75785,#75786,#75787,#75788)),
 .UNSPECIFIED.,.F.,.F.,.F.,(4,4),(4,1,1,1,1,1,1,1,1,1,1,1,1,1,1,1,1,1,1,
1,1,1,1,1,1,1,1,1,1,1,1,1,1,1,1,1,1,1,1,1,1,1,1,1,1,1,1,1,1,1,1,1,1,1,1,
1,1,1,1,1,1,1,1,1,1,1,1,1,1,1,1,1,1,1,1,1,1,1,1,1,1,1,1,1,1,1,1,1,1,1,1,
1,1,1,1,1,1,1,1,1,1,1,1,1,1,1,1,1,1,1,1,1,1,1,1,1,1,1,1,1,1,1,1,1,4),(0.,
0.0658467982010767),(11.6150328478182,12.6100681710919,13.6051034943655,
14.6001388176392,15.5951741409128,16.5902094641865,17.5852447874601,18.5802801107338,
19.5753154340074,20.5703507572811,21.5653860805547,22.5604214038284,23.555456727102,
24.5504920503757,25.5455273736493,26.540562696923,27.5355980201966,28.5306333434703,
29.5256686667439,30.5207039900176,31.5157393132912,32.5107746365649,33.5058099598385,
34.5008452831122,35.4958806063858,36.4909159296595,37.4859512529331,38.4809865762068,
39.4760218994804,40.4710572227541,41.4660925460277,42.4611278693014,43.456163192575,
44.4511985158487,45.4462338391223,46.441269162396,47.4363044856696,48.4313398089433,
49.4263751322169,50.4214104554906,51.4164457787642,52.4114811020379,53.4065164253115,
54.4015517485852,55.3965870718588,56.3916223951325,57.3866577184061,58.3816930416798,
59.3767283649534,60.3717636882271,61.3667990115007,62.3618343347744,63.356869658048,
64.3519049813217,65.3469403045953,66.341975627869,67.3370109511426,68.3320462744163,
69.3270815976899,70.3221169209636,71.3171522442372,72.3121875675109,73.3072228907845,
74.3022582140582,75.2972935373318,76.2923288606055,77.2873641838791,78.2823995071528,
79.2774348304264,80.2724701537001,81.2675054769737,82.2625408002474,83.257576123521,
84.2526114467947,85.2476467700683,86.242682093342,87.2377174166156,88.2327527398893,
89.2277880631629,90.2228233864366,91.2178587097102,92.2128940329839,93.2079293562575,
94.2029646795312,95.1980000028048,96.1930353260785,97.1880706493521,98.1831059726258,
99.1781412958994,100.173176619173,101.168211942447,102.16324726572,103.158282588994,
104.153317912268,105.148353235541,106.143388558815,107.138423882089,108.133459205362,
109.128494528636,110.12352985191,111.118565175183,112.113600498457,113.108635821731,
114.103671145004,115.098706468278,116.093741791551,117.088777114825,118.083812438099,
119.078847761372,120.073883084646,121.06891840792,122.063953731193,123.058989054467,
124.054024377741,125.049059701014,126.044095024288,127.039130347562,128.034165670835,
129.029200994109,130.024236317383,131.019271640656,132.01430696393,133.009342287204,
134.004377610477,134.999412933751),.UNSPECIFIED.);
#914=B_SPLINE_CURVE_WITH_KNOTS('',3,(#73088,#73089,#73090,#73091,#73092,
#73093,#73094,#73095,#73096,#73097),.UNSPECIFIED.,.F.,.F.,(4,3,3,4),(-4.09293042013066,
-3.9801412930946,-2.98510596982095,-2.06863817490914),.UNSPECIFIED.);
#915=B_SPLINE_CURVE_WITH_KNOTS('',3,(#73100,#73101,#73102,#73103,#73104,
#73105,#73106),.UNSPECIFIED.,.F.,.F.,(4,3,4),(0.,0.995035323273648,1.11730040836815),
 .UNSPECIFIED.);
#916=B_SPLINE_CURVE_WITH_KNOTS('',3,(#73111,#73112,#73113,#73114,#73115,
#73116,#73117,#73118,#73119,#73120,#73121,#73122,#73123,#73124,#73125,#73126,
#73127,#73128,#73129,#73130,#73131,#73132),.UNSPECIFIED.,.F.,.F.,(4,3,3,
3,3,3,3,4),(-10.3761157273103,-9.9503532327365,-8.95531790946285,-7.9602825861892,
-6.96524726291555,-5.9702119396419,-4.97517661636825,-4.09293042013066),
 .UNSPECIFIED.);
#917=B_SPLINE_CURVE_WITH_KNOTS('',3,(#73133,#73134,#73135,#73136,#73137,
#73138,#73139,#73140,#73141,#73142,#73143,#73144,#73145,#73146,#73147,#73148,
#73149,#73150,#73151,#73152,#73153,#73154),.UNSPECIFIED.,.F.,.F.,(4,3,3,
3,3,3,3,4),(1.11730040836815,1.9900706465473,2.98510596982095,3.9801412930946,
4.97517661636825,5.9702119396419,6.96524726291555,7.40048571554773),
 .UNSPECIFIED.);
#918=B_SPLINE_CURVE_WITH_KNOTS('',3,(#73159,#73160,#73161,#73162,#73163,
#73164,#73165,#73166,#73167,#73168,#73169,#73170,#73171,#73172,#73173,#73174,
#73175,#73176,#73177,#73178,#73179,#73180),.UNSPECIFIED.,.F.,.F.,(4,3,3,
3,3,3,3,4),(-16.6593010344898,-15.9205651723784,-14.9255298491048,-13.9304945258311,
-12.9354592025574,-11.9404238792838,-10.9453885560101,-10.3761157273103),
 .UNSPECIFIED.);
#919=B_SPLINE_CURVE_WITH_KNOTS('',3,(#73181,#73182,#73183,#73184,#73185,
#73186,#73187,#73188,#73189,#73190,#73191,#73192,#73193,#73194,#73195,#73196,
#73197,#73198,#73199,#73200,#73201,#73202),.UNSPECIFIED.,.F.,.F.,(4,3,3,
3,3,3,3,4),(7.40048571554773,7.9602825861892,8.95531790946285,9.95035323273651,
10.9453885560102,11.9404238792838,12.9354592025575,13.6836710227273),
 .UNSPECIFIED.);
#920=B_SPLINE_CURVE_WITH_KNOTS('',3,(#73207,#73208,#73209,#73210,#73211,
#73212,#73213,#73214,#73215,#73216,#73217,#73218,#73219,#73220,#73221,#73222,
#73223,#73224,#73225,#73226,#73227,#73228,#73229,#73230,#73231),
 .UNSPECIFIED.,.F.,.F.,(4,3,3,3,3,3,3,3,4),(-22.9424863416694,-22.885812435294,
-21.8907771120203,-20.8957417887467,-19.900706465473,-18.9056711421993,
-17.9106358189257,-16.9156004956521,-16.6593010344898),.UNSPECIFIED.);
#921=B_SPLINE_CURVE_WITH_KNOTS('',3,(#73232,#73233,#73234,#73235,#73236,
#73237,#73238,#73239,#73240,#73241,#73242,#73243,#73244,#73245,#73246,#73247,
#73248,#73249,#73250,#73251,#73252,#73253,#73254,#73255,#73256),
 .UNSPECIFIED.,.F.,.F.,(4,3,3,3,3,3,3,3,4),(13.6836710227273,13.9304945258311,
14.9255298491048,15.9205651723784,16.9156004956521,17.9106358189257,18.9056711421993,
19.900706465473,19.9668563299069),.UNSPECIFIED.);
#922=B_SPLINE_CURVE_WITH_KNOTS('',3,(#73261,#73262,#73263,#73264,#73265,
#73266,#73267,#73268,#73269,#73270,#73271,#73272,#73273,#73274,#73275,#73276,
#73277,#73278,#73279,#73280,#73281,#73282),.UNSPECIFIED.,.F.,.F.,(4,3,3,
3,3,3,3,4),(-29.225671648849,-28.8560243749359,-27.8609890516622,-26.8659537283885,
-25.8709184051149,-24.8758830818412,-23.8808477585676,-22.9424863416694),
 .UNSPECIFIED.);
#923=B_SPLINE_CURVE_WITH_KNOTS('',3,(#73283,#73284,#73285,#73286,#73287,
#73288,#73289,#73290,#73291,#73292,#73293,#73294,#73295,#73296,#73297,#73298,
#73299,#73300,#73301,#73302,#73303,#73304),.UNSPECIFIED.,.F.,.F.,(4,3,3,
3,3,3,3,4),(19.9668563299069,20.8957417887466,21.8907771120203,22.8858124352939,
23.8808477585676,24.8758830818412,25.8709184051149,26.2500416370865),
 .UNSPECIFIED.);
#924=B_SPLINE_CURVE_WITH_KNOTS('',3,(#73309,#73310,#73311,#73312,#73313,
#73314,#73315,#73316,#73317,#73318,#73319,#73320,#73321,#73322,#73323,#73324,
#73325,#73326,#73327,#73328,#73329,#73330),.UNSPECIFIED.,.F.,.F.,(4,3,3,
3,3,3,3,4),(-35.5088569560286,-34.8262363145777,-33.8312009913041,-32.8361656680304,
-31.8411303447568,-30.8460950214831,-29.8510596982095,-29.225671648849),
 .UNSPECIFIED.);
#925=B_SPLINE_CURVE_WITH_KNOTS('',3,(#73331,#73332,#73333,#73334,#73335,
#73336,#73337,#73338,#73339,#73340,#73341,#73342,#73343,#73344,#73345,#73346,
#73347,#73348,#73349,#73350,#73351,#73352),.UNSPECIFIED.,.F.,.F.,(4,3,3,
3,3,3,3,4),(26.2500416370865,26.8659537283885,27.8609890516622,28.8560243749358,
29.8510596982095,30.8460950214831,31.8411303447568,32.5332269442661),
 .UNSPECIFIED.);
#926=B_SPLINE_CURVE_WITH_KNOTS('',3,(#73357,#73358,#73359,#73360,#73361,
#73362,#73363,#73364,#73365,#73366,#73367,#73368,#73369,#73370,#73371,#73372,
#73373,#73374,#73375,#73376,#73377,#73378),.UNSPECIFIED.,.F.,.F.,(4,3,3,
3,3,3,3,4),(-41.7920422632082,-40.7964482542196,-39.801412930946,-38.8063776076723,
-37.8113422843987,-36.8163069611251,-35.8212716378514,-35.5088569560286),
 .UNSPECIFIED.);
#927=B_SPLINE_CURVE_WITH_KNOTS('',3,(#73379,#73380,#73381,#73382,#73383,
#73384,#73385,#73386,#73387,#73388,#73389,#73390,#73391,#73392,#73393,#73394,
#73395,#73396,#73397,#73398,#73399,#73400,#73401,#73402,#73403),
 .UNSPECIFIED.,.F.,.F.,(4,3,3,3,3,3,3,3,4),(32.5332269442661,32.8361656680304,
33.8312009913041,34.8262363145777,35.8212716378514,36.816306961125,37.8113422843987,
38.8063776076723,38.8164122514457),.UNSPECIFIED.);
#928=B_SPLINE_CURVE_WITH_KNOTS('',3,(#73408,#73409,#73410,#73411,#73412,
#73413,#73414,#73415,#73416,#73417,#73418,#73419,#73420,#73421,#73422,#73423,
#73424,#73425,#73426,#73427,#73428,#73429),.UNSPECIFIED.,.F.,.F.,(4,3,3,
3,3,3,3,4),(-48.0752275703878,-47.7616955171352,-46.7666601938616,-45.7716248705879,
-44.7765895473142,-43.7815542240406,-42.7865189007669,-41.7920422632082),
 .UNSPECIFIED.);
#929=B_SPLINE_CURVE_WITH_KNOTS('',3,(#73430,#73431,#73432,#73433,#73434,
#73435,#73436,#73437,#73438,#73439,#73440,#73441,#73442,#73443,#73444,#73445,
#73446,#73447,#73448,#73449,#73450,#73451),.UNSPECIFIED.,.F.,.F.,(4,3,3,
3,3,3,3,4),(38.8164122514457,39.801412930946,40.7964482542196,41.7914835774933,
42.7865189007669,43.7815542240406,44.7765895473143,45.0995975586253),
 .UNSPECIFIED.);
#930=B_SPLINE_CURVE_WITH_KNOTS('',3,(#73456,#73457,#73458,#73459,#73460,
#73461,#73462,#73463,#73464,#73465,#73466,#73467,#73468,#73469,#73470,#73471,
#73472,#73473,#73474,#73475,#73476,#73477),.UNSPECIFIED.,.F.,.F.,(4,3,3,
3,3,3,3,4),(-54.3584128775674,-53.7319074567771,-52.7368721335034,-51.7418368102298,
-50.7468014869562,-49.7517661636825,-48.7567308404089,-48.0752275703878),
 .UNSPECIFIED.);
#931=B_SPLINE_CURVE_WITH_KNOTS('',3,(#73478,#73479,#73480,#73481,#73482,
#73483,#73484,#73485,#73486,#73487,#73488,#73489,#73490,#73491,#73492,#73493,
#73494,#73495,#73496,#73497,#73498,#73499),.UNSPECIFIED.,.F.,.F.,(4,3,3,
3,3,3,3,4),(45.0995975586253,45.7716248705879,46.7666601938615,47.7616955171352,
48.7567308404088,49.7517661636825,50.7468014869561,51.3827828658048),
 .UNSPECIFIED.);
#932=B_SPLINE_CURVE_WITH_KNOTS('',3,(#73504,#73505,#73506,#73507,#73508,
#73509,#73510,#73511,#73512,#73513,#73514,#73515,#73516,#73517,#73518,#73519,
#73520,#73521,#73522,#73523,#73524,#73525),.UNSPECIFIED.,.F.,.F.,(4,3,3,
3,3,3,3,4),(-60.641598184747,-59.702119396419,-58.7070840731453,-57.7120487498717,
-56.7170134265981,-55.7219781033244,-54.7269427800508,-54.3584128775674),
 .UNSPECIFIED.);
#933=B_SPLINE_CURVE_WITH_KNOTS('',3,(#73526,#73527,#73528,#73529,#73530,
#73531,#73532,#73533,#73534,#73535,#73536,#73537,#73538,#73539,#73540,#73541,
#73542,#73543,#73544,#73545,#73546,#73547),.UNSPECIFIED.,.F.,.F.,(4,3,3,
3,3,3,3,4),(51.3827828658048,51.7418368102298,52.7368721335034,53.7319074567771,
54.7269427800507,55.7219781033244,56.717013426598,57.6659681729844),
 .UNSPECIFIED.);
#934=B_SPLINE_CURVE_WITH_KNOTS('',3,(#73552,#73553,#73554,#73555,#73556,
#73557,#73558,#73559,#73560,#73561,#73562,#73563,#73564,#73565,#73566,#73567,
#73568,#73569,#73570,#73571,#73572,#73573,#73574,#73575,#73576),
 .UNSPECIFIED.,.F.,.F.,(4,3,3,3,3,3,3,3,4),(-66.9247834919266,-66.6673666593345,
-65.6723313360609,-64.6772960127873,-63.6822606895136,-62.6872253662399,
-61.6921900429663,-60.6971547196927,-60.641598184747),.UNSPECIFIED.);
#935=B_SPLINE_CURVE_WITH_KNOTS('',3,(#73577,#73578,#73579,#73580,#73581,
#73582,#73583,#73584,#73585,#73586,#73587,#73588,#73589,#73590,#73591,#73592,
#73593,#73594,#73595,#73596,#73597,#73598,#73599,#73600,#73601),
 .UNSPECIFIED.,.F.,.F.,(4,3,3,3,3,3,3,3,4),(57.6659681729844,57.7120487498717,
58.7070840731453,59.702119396419,60.6971547196927,61.6921900429663,62.68722536624,
63.6822606895136,63.949153480164),.UNSPECIFIED.);
#936=B_SPLINE_CURVE_WITH_KNOTS('',3,(#73606,#73607,#73608,#73609,#73610,
#73611,#73612,#73613,#73614,#73615,#73616,#73617,#73618,#73619,#73620,#73621,
#73622,#73623,#73624,#73625,#73626,#73627),.UNSPECIFIED.,.F.,.F.,(4,3,3,
3,3,3,3,4),(-73.2079687991062,-72.6375785989764,-71.6425432757028,-70.6475079524291,
-69.6524726291555,-68.6574373058818,-67.6624019826082,-66.9247834919266),
 .UNSPECIFIED.);
#937=B_SPLINE_CURVE_WITH_KNOTS('',3,(#73628,#73629,#73630,#73631,#73632,
#73633,#73634,#73635,#73636,#73637,#73638,#73639,#73640,#73641,#73642,#73643,
#73644,#73645,#73646,#73647,#73648,#73649),.UNSPECIFIED.,.F.,.F.,(4,3,3,
3,3,3,3,4),(63.949153480164,64.6772960127873,65.6723313360609,66.6673666593345,
67.6624019826082,68.6574373058818,69.6524726291555,70.2323387873436),
 .UNSPECIFIED.);
#938=B_SPLINE_CURVE_WITH_KNOTS('',3,(#73654,#73655,#73656,#73657,#73658,
#73659,#73660,#73661,#73662,#73663,#73664,#73665,#73666,#73667,#73668,#73669,
#73670,#73671,#73672,#73673,#73674,#73675),.UNSPECIFIED.,.F.,.F.,(4,3,3,
3,3,3,3,4),(-79.4911541062857,-78.6077905386183,-77.6127552153447,-76.6177198920711,
-75.6226845687974,-74.6276492455237,-73.6326139222501,-73.2079687991062),
 .UNSPECIFIED.);
#939=B_SPLINE_CURVE_WITH_KNOTS('',3,(#73676,#73677,#73678,#73679,#73680,
#73681,#73682,#73683,#73684,#73685,#73686,#73687,#73688,#73689,#73690,#73691,
#73692,#73693,#73694,#73695,#73696,#73697),.UNSPECIFIED.,.F.,.F.,(4,3,3,
3,3,3,3,4),(70.2323387873436,70.6475079524291,71.6425432757028,72.6375785989764,
73.6326139222501,74.6276492455237,75.6226845687974,76.5155240945232),
 .UNSPECIFIED.);
#940=B_SPLINE_CURVE_WITH_KNOTS('',3,(#73702,#73703,#73704,#73705,#73706,
#73707,#73708,#73709,#73710,#73711,#73712,#73713,#73714,#73715,#73716,#73717,
#73718,#73719,#73720,#73721,#73722,#73723,#73724,#73725,#73726),
 .UNSPECIFIED.,.F.,.F.,(4,3,3,3,3,3,3,3,4),(-85.7743394134653,-85.5730378015339,
-84.5780024782602,-83.5829671549866,-82.587931831713,-81.5928965084393,
-80.5978611851656,-79.602825861892,-79.4911541062857),.UNSPECIFIED.);
#941=B_SPLINE_CURVE_WITH_KNOTS('',3,(#73727,#73728,#73729,#73730,#73731,
#73732,#73733,#73734,#73735,#73736,#73737,#73738,#73739,#73740,#73741,#73742,
#73743,#73744,#73745,#73746,#73747,#73748,#73749,#73750,#73751),
 .UNSPECIFIED.,.F.,.F.,(4,3,3,3,3,3,3,3,4),(76.5155240945232,76.617719892071,
77.6127552153447,78.6077905386183,79.602825861892,80.5978611851656,81.5928965084393,
82.5879318317129,82.7987094017028),.UNSPECIFIED.);
#942=B_SPLINE_CURVE_WITH_KNOTS('',3,(#73756,#73757,#73758,#73759,#73760,
#73761,#73762,#73763,#73764,#73765,#73766,#73767,#73768,#73769,#73770,#73771,
#73772,#73773,#73774,#73775,#73776,#73777),.UNSPECIFIED.,.F.,.F.,(4,3,3,
3,3,3,3,4),(-92.0575247206449,-91.5432497411758,-90.5482144179021,-89.5531790946285,
-88.5581437713548,-87.5631084480812,-86.5680731248076,-85.7743394134653),
 .UNSPECIFIED.);
#943=B_SPLINE_CURVE_WITH_KNOTS('',3,(#73778,#73779,#73780,#73781,#73782,
#73783,#73784,#73785,#73786,#73787,#73788,#73789,#73790,#73791,#73792,#73793,
#73794,#73795,#73796,#73797,#73798,#73799),.UNSPECIFIED.,.F.,.F.,(4,3,3,
3,3,3,3,4),(82.7987094017028,83.5829671549866,84.5780024782602,85.5730378015339,
86.5680731248075,87.5631084480812,88.5581437713548,89.0818947088824),
 .UNSPECIFIED.);
#944=B_SPLINE_CURVE_WITH_KNOTS('',3,(#73804,#73805,#73806,#73807,#73808,
#73809,#73810,#73811,#73812,#73813,#73814,#73815,#73816,#73817,#73818,#73819,
#73820,#73821,#73822,#73823,#73824,#73825),.UNSPECIFIED.,.F.,.F.,(4,3,3,
3,3,3,3,4),(-98.3407100278245,-97.5134616808177,-96.518426357544,-95.5233910342704,
-94.5283557109967,-93.5333203877231,-92.5382850644494,-92.0575247206449),
 .UNSPECIFIED.);
#945=B_SPLINE_CURVE_WITH_KNOTS('',3,(#73826,#73827,#73828,#73829,#73830,
#73831,#73832,#73833,#73834,#73835,#73836,#73837,#73838,#73839,#73840,#73841,
#73842,#73843,#73844,#73845,#73846,#73847),.UNSPECIFIED.,.F.,.F.,(4,3,3,
3,3,3,3,4),(89.0818947088824,89.5531790946285,90.5482144179021,91.5432497411758,
92.5382850644494,93.5333203877231,94.5283557109967,95.365080016062),
 .UNSPECIFIED.);
#946=B_SPLINE_CURVE_WITH_KNOTS('',3,(#73852,#73853,#73854,#73855,#73856,
#73857,#73858,#73859,#73860,#73861,#73862,#73863,#73864,#73865,#73866,#73867,
#73868,#73869,#73870,#73871,#73872,#73873,#73874,#73875,#73876),
 .UNSPECIFIED.,.F.,.F.,(4,3,3,3,3,3,3,3,4),(-104.623895335004,-104.478708943733,
-103.48367362046,-102.488638297186,-101.493602973912,-100.498567650639,
-99.503532327365,-98.5084970040914,-98.3407100278245),.UNSPECIFIED.);
#947=B_SPLINE_CURVE_WITH_KNOTS('',3,(#73877,#73878,#73879,#73880,#73881,
#73882,#73883,#73884,#73885,#73886,#73887,#73888,#73889,#73890,#73891,#73892,
#73893,#73894,#73895,#73896,#73897,#73898,#73899,#73900,#73901),
 .UNSPECIFIED.,.F.,.F.,(4,3,3,3,3,3,3,3,4),(95.365080016062,95.5233910342704,
96.518426357544,97.5134616808177,98.5084970040913,99.503532327365,100.498567650639,
101.493602973912,101.648265323242),.UNSPECIFIED.);
#948=B_SPLINE_CURVE_WITH_KNOTS('',3,(#73906,#73907,#73908,#73909,#73910,
#73911,#73912,#73913,#73914,#73915,#73916,#73917,#73918,#73919,#73920,#73921,
#73922,#73923,#73924,#73925,#73926,#73927),.UNSPECIFIED.,.F.,.F.,(4,3,3,
3,3,3,3,4),(-110.907080642184,-110.448920883375,-109.453885560102,-108.458850236828,
-107.463814913554,-106.468779590281,-105.473744267007,-104.623895335004),
 .UNSPECIFIED.);
#949=B_SPLINE_CURVE_WITH_KNOTS('',3,(#73928,#73929,#73930,#73931,#73932,
#73933,#73934,#73935,#73936,#73937,#73938,#73939,#73940,#73941,#73942,#73943,
#73944,#73945,#73946,#73947,#73948,#73949),.UNSPECIFIED.,.F.,.F.,(4,3,3,
3,3,3,3,4),(101.648265323242,102.488638297186,103.48367362046,104.478708943733,
105.473744267007,106.468779590281,107.463814913554,107.931450630421),
 .UNSPECIFIED.);
#950=B_SPLINE_CURVE_WITH_KNOTS('',3,(#73954,#73955,#73956,#73957,#73958,
#73959,#73960,#73961,#73962,#73963,#73964,#73965,#73966,#73967,#73968,#73969,
#73970,#73971,#73972,#73973,#73974,#73975),.UNSPECIFIED.,.F.,.F.,(4,3,3,
3,3,3,3,4),(-117.190265949363,-116.419132823017,-115.424097499743,-114.42906217647,
-113.434026853196,-112.438991529922,-111.443956206649,-110.907080642184),
 .UNSPECIFIED.);
#951=B_SPLINE_CURVE_WITH_KNOTS('',3,(#73976,#73977,#73978,#73979,#73980,
#73981,#73982,#73983,#73984,#73985,#73986,#73987,#73988,#73989,#73990,#73991,
#73992,#73993,#73994,#73995,#73996,#73997),.UNSPECIFIED.,.F.,.F.,(4,3,3,
3,3,3,3,4),(107.931450630421,108.458850236828,109.453885560101,110.448920883375,
111.443956206649,112.438991529922,113.434026853196,114.214635937601),
 .UNSPECIFIED.);
#952=B_SPLINE_CURVE_WITH_KNOTS('',3,(#74004,#74005,#74006,#74007,#74008,
#74009,#74010,#74011,#74012,#74013,#74014,#74015,#74016,#74017,#74018,#74019,
#74020,#74021,#74022,#74023,#74024,#74025),.UNSPECIFIED.,.F.,.F.,(4,3,3,
3,3,3,3,4),(-123.384380085933,-122.389344762659,-121.394309439385,-120.399274116112,
-119.404238792838,-118.409203469564,-117.414168146291,-117.190265949363),
 .UNSPECIFIED.);
#953=B_SPLINE_CURVE_WITH_KNOTS('',3,(#74026,#74027,#74028,#74029,#74030,
#74031,#74032,#74033,#74034,#74035,#74036,#74037,#74038,#74039,#74040,#74041,
#74042,#74043,#74044,#74045,#74046,#74047,#74048,#74049,#74050),
 .UNSPECIFIED.,.F.,.F.,(4,3,3,3,3,3,3,3,4),(114.214635937601,114.42906217647,
115.424097499743,116.419132823017,117.414168146291,118.409203469564,119.404238792838,
120.399274116112,120.49782124478),.UNSPECIFIED.);
#954=B_SPLINE_CURVE_WITH_KNOTS('',3,(#74056,#74057,#74058,#74059,#74060,
#74061,#74062,#74063),.UNSPECIFIED.,.F.,.F.,(4,1,1,1,1,4),(128.805298797182,
129.029200994109,130.024236317383,131.019271640656,132.01430696393,132.930774758842),
 .UNSPECIFIED.);
#955=B_SPLINE_CURVE_WITH_KNOTS('',3,(#74066,#74067,#74068,#74069,#74070,
#74071),.UNSPECIFIED.,.F.,.F.,(4,1,1,4),(128.805298797182,129.701786991786,
130.69682231506,131.691857638334),.UNSPECIFIED.);
#956=B_SPLINE_CURVE_WITH_KNOTS('',3,(#74076,#74077,#74078,#74079,#74080,
#74081,#74082,#74083,#74084,#74085),.UNSPECIFIED.,.F.,.F.,(4,1,1,1,1,1,
1,4),(122.522113490002,123.058989054467,124.054024377741,125.049059701014,
126.044095024288,127.039130347562,128.034165670835,128.805298797182),
 .UNSPECIFIED.);
#957=B_SPLINE_CURVE_WITH_KNOTS('',3,(#74086,#74087,#74088,#74089,#74090,
#74091,#74092,#74093,#74094,#74095,#74096),.UNSPECIFIED.,.F.,.F.,(4,1,1,
1,1,1,1,1,4),(122.522113490002,122.736539728871,123.731575052144,124.726610375418,
125.721645698692,126.716681021965,127.711716345239,128.706751668513,128.805298797182),
 .UNSPECIFIED.);
#958=B_SPLINE_CURVE_WITH_KNOTS('',3,(#74101,#74102,#74103,#74104,#74105,
#74106,#74107,#74108,#74109,#74110),.UNSPECIFIED.,.F.,.F.,(4,1,1,1,1,1,
1,4),(116.238928182822,117.088777114825,118.083812438099,119.078847761372,
120.073883084646,121.06891840792,122.063953731193,122.522113490002),
 .UNSPECIFIED.);
#959=B_SPLINE_CURVE_WITH_KNOTS('',3,(#74111,#74112,#74113,#74114,#74115,
#74116,#74117,#74118,#74119,#74120),.UNSPECIFIED.,.F.,.F.,(4,1,1,1,1,1,
1,4),(116.238928182822,116.766327789229,117.761363112503,118.756398435776,
119.75143375905,120.746469082323,121.741504405597,122.522113490002),
 .UNSPECIFIED.);
#960=B_SPLINE_CURVE_WITH_KNOTS('',3,(#74125,#74126,#74127,#74128,#74129,
#74130,#74131,#74132,#74133,#74134,#74135),.UNSPECIFIED.,.F.,.F.,(4,1,1,
1,1,1,1,1,4),(109.955742875643,110.12352985191,111.118565175183,112.113600498457,
113.108635821731,114.103671145004,115.098706468278,116.093741791551,116.238928182822),
 .UNSPECIFIED.);
#961=B_SPLINE_CURVE_WITH_KNOTS('',3,(#74136,#74137,#74138,#74139,#74140,
#74141,#74142,#74143,#74144,#74145),.UNSPECIFIED.,.F.,.F.,(4,1,1,1,1,1,
1,4),(109.955742875643,110.796115849587,111.791151172861,112.786186496134,
113.781221819408,114.776257142682,115.771292465955,116.238928182822),
 .UNSPECIFIED.);
#962=B_SPLINE_CURVE_WITH_KNOTS('',3,(#74150,#74151,#74152,#74153,#74154,
#74155,#74156,#74157,#74158,#74159),.UNSPECIFIED.,.F.,.F.,(4,1,1,1,1,1,
1,4),(103.672557568463,104.153317912268,105.148353235541,106.143388558815,
107.138423882089,108.133459205362,109.128494528636,109.955742875643),
 .UNSPECIFIED.);
#963=B_SPLINE_CURVE_WITH_KNOTS('',3,(#74160,#74161,#74162,#74163,#74164,
#74165,#74166,#74167,#74168,#74169,#74170),.UNSPECIFIED.,.F.,.F.,(4,1,1,
1,1,1,1,1,4),(103.672557568463,103.830868586671,104.825903909945,105.820939233219,
106.815974556492,107.811009879766,108.80604520304,109.801080526313,109.955742875643),
 .UNSPECIFIED.);
#964=B_SPLINE_CURVE_WITH_KNOTS('',3,(#74175,#74176,#74177,#74178,#74179,
#74180,#74181,#74182,#74183,#74184),.UNSPECIFIED.,.F.,.F.,(4,1,1,1,1,1,
1,4),(97.3893722612836,98.1831059726258,99.1781412958994,100.173176619173,
101.168211942447,102.16324726572,103.158282588994,103.672557568463),
 .UNSPECIFIED.);
#965=B_SPLINE_CURVE_WITH_KNOTS('',3,(#74185,#74186,#74187,#74188,#74189,
#74190,#74191,#74192,#74193,#74194),.UNSPECIFIED.,.F.,.F.,(4,1,1,1,1,1,
1,4),(97.3893722612835,97.8606566470295,98.8556919703032,99.8507272935768,
100.84576261685,101.840797940124,102.835833263398,103.672557568463),
 .UNSPECIFIED.);
#966=B_SPLINE_CURVE_WITH_KNOTS('',3,(#74199,#74200,#74201,#74202,#74203,
#74204,#74205,#74206,#74207,#74208,#74209),.UNSPECIFIED.,.F.,.F.,(4,1,1,
1,1,1,1,1,4),(91.106186954104,91.2178587097102,92.2128940329839,93.2079293562575,
94.2029646795312,95.1980000028048,96.1930353260785,97.1880706493521,97.3893722612836),
 .UNSPECIFIED.);
#967=B_SPLINE_CURVE_WITH_KNOTS('',3,(#74210,#74211,#74212,#74213,#74214,
#74215,#74216,#74217,#74218,#74219),.UNSPECIFIED.,.F.,.F.,(4,1,1,1,1,1,
1,4),(91.1061869541039,91.8904447073876,92.8854800306613,93.8805153539349,
94.8755506772086,95.8705860004822,96.8656213237559,97.3893722612835),
 .UNSPECIFIED.);
#968=B_SPLINE_CURVE_WITH_KNOTS('',3,(#74224,#74225,#74226,#74227,#74228,
#74229,#74230,#74231,#74232,#74233),.UNSPECIFIED.,.F.,.F.,(4,1,1,1,1,1,
1,4),(84.8230016469244,85.2476467700683,86.242682093342,87.2377174166156,
88.2327527398893,89.2277880631629,90.2228233864366,91.106186954104),
 .UNSPECIFIED.);
#969=B_SPLINE_CURVE_WITH_KNOTS('',3,(#74234,#74235,#74236,#74237,#74238,
#74239,#74240,#74241,#74242,#74243,#74244),.UNSPECIFIED.,.F.,.F.,(4,1,1,
1,1,1,1,1,4),(84.8230016469244,84.9251974444721,85.9202327677457,86.9152680910194,
87.910303414293,88.9053387375667,89.9003740608403,90.895409384114,91.1061869541039),
 .UNSPECIFIED.);
#970=B_SPLINE_CURVE_WITH_KNOTS('',3,(#74249,#74250,#74251,#74252,#74253,
#74254,#74255,#74256,#74257,#74258),.UNSPECIFIED.,.F.,.F.,(4,1,1,1,1,1,
1,4),(78.5398163397448,79.2774348304264,80.2724701537001,81.2675054769737,
82.2625408002474,83.257576123521,84.2526114467947,84.8230016469244),
 .UNSPECIFIED.);
#971=B_SPLINE_CURVE_WITH_KNOTS('',3,(#74259,#74260,#74261,#74262,#74263,
#74264,#74265,#74266,#74267,#74268),.UNSPECIFIED.,.F.,.F.,(4,1,1,1,1,1,
1,4),(78.5398163397448,78.9549855048302,79.9500208281038,80.9450561513775,
81.9400914746511,82.9351267979248,83.9301621211984,84.8230016469244),
 .UNSPECIFIED.);
#972=B_SPLINE_CURVE_WITH_KNOTS('',3,(#74273,#74274,#74275,#74276,#74277,
#74278,#74279,#74280,#74281,#74282,#74283),.UNSPECIFIED.,.F.,.F.,(4,1,1,
1,1,1,1,1,4),(72.2566310325652,72.3121875675109,73.3072228907845,74.3022582140582,
75.2972935373318,76.2923288606055,77.2873641838791,78.2823995071528,78.5398163397448),
 .UNSPECIFIED.);
#973=B_SPLINE_CURVE_WITH_KNOTS('',3,(#74284,#74285,#74286,#74287,#74288,
#74289,#74290,#74291,#74292,#74293),.UNSPECIFIED.,.F.,.F.,(4,1,1,1,1,1,
1,4),(72.2566310325652,72.9847735651883,73.9798088884619,74.9748442117356,
75.9698795350092,76.9649148582829,77.9599501815565,78.5398163397448),
 .UNSPECIFIED.);
#974=B_SPLINE_CURVE_WITH_KNOTS('',3,(#74298,#74299,#74300,#74301,#74302,
#74303,#74304,#74305,#74306,#74307),.UNSPECIFIED.,.F.,.F.,(4,1,1,1,1,1,
1,4),(65.9734457253856,66.341975627869,67.3370109511426,68.3320462744163,
69.3270815976899,70.3221169209636,71.3171522442372,72.2566310325652),
 .UNSPECIFIED.);
#975=B_SPLINE_CURVE_WITH_KNOTS('',3,(#74308,#74309,#74310,#74311,#74312,
#74313,#74314,#74315,#74316,#74317,#74318),.UNSPECIFIED.,.F.,.F.,(4,1,1,
1,1,1,1,1,4),(65.9734457253856,66.0195263022727,67.0145616255464,68.00959694882,
69.0046322720937,69.9996675953673,70.994702918641,71.9897382419146,72.2566310325652),
 .UNSPECIFIED.);
#976=B_SPLINE_CURVE_WITH_KNOTS('',3,(#74323,#74324,#74325,#74326,#74327,
#74328,#74329,#74330,#74331,#74332),.UNSPECIFIED.,.F.,.F.,(4,1,1,1,1,1,
1,4),(59.690260418206,60.3717636882271,61.3667990115007,62.3618343347744,
63.356869658048,64.3519049813217,65.3469403045953,65.9734457253856),
 .UNSPECIFIED.);
#977=B_SPLINE_CURVE_WITH_KNOTS('',3,(#74333,#74334,#74335,#74336,#74337,
#74338,#74339,#74340,#74341,#74342),.UNSPECIFIED.,.F.,.F.,(4,1,1,1,1,1,
1,4),(59.690260418206,60.0493143626308,61.0443496859045,62.0393850091781,
63.0344203324518,64.0294556557254,65.0244909789991,65.9734457253856),
 .UNSPECIFIED.);
#978=B_SPLINE_CURVE_WITH_KNOTS('',3,(#74347,#74348,#74349,#74350,#74351,
#74352,#74353,#74354,#74355,#74356),.UNSPECIFIED.,.F.,.F.,(4,1,1,1,1,1,
1,4),(53.4070751110264,54.4015517485852,55.3965870718588,56.3916223951325,
57.3866577184061,58.3816930416798,59.3767283649534,59.690260418206),
 .UNSPECIFIED.);
#979=B_SPLINE_CURVE_WITH_KNOTS('',3,(#74357,#74358,#74359,#74360,#74361,
#74362,#74363,#74364,#74365,#74366),.UNSPECIFIED.,.F.,.F.,(4,1,1,1,1,1,
1,4),(53.4070751110264,54.0791024229889,55.0741377462626,56.0691730695362,
57.0642083928099,58.0592437160835,59.0542790393572,59.690260418206),
 .UNSPECIFIED.);
#980=B_SPLINE_CURVE_WITH_KNOTS('',3,(#74371,#74372,#74373,#74374,#74375,
#74376,#74377,#74378,#74379,#74380,#74381),.UNSPECIFIED.,.F.,.F.,(4,1,1,
1,1,1,1,1,4),(47.1238898038468,47.4363044856696,48.4313398089433,49.4263751322169,
50.4214104554906,51.4164457787642,52.4114811020379,53.4065164253115,53.4070751110264),
 .UNSPECIFIED.);
#981=B_SPLINE_CURVE_WITH_KNOTS('',3,(#74382,#74383,#74384,#74385,#74386,
#74387,#74388,#74389,#74390,#74391),.UNSPECIFIED.,.F.,.F.,(4,1,1,1,1,1,
1,4),(47.1238898038468,48.108890483347,49.1039258066207,50.0989611298943,
51.093996453168,52.0890317764416,53.0840670997153,53.4070751110264),
 .UNSPECIFIED.);
#982=B_SPLINE_CURVE_WITH_KNOTS('',3,(#74396,#74397,#74398,#74399,#74400,
#74401,#74402,#74403,#74404,#74405),.UNSPECIFIED.,.F.,.F.,(4,1,1,1,1,1,
1,4),(40.8407044966672,41.4660925460277,42.4611278693014,43.456163192575,
44.4511985158487,45.4462338391223,46.441269162396,47.1238898038468),
 .UNSPECIFIED.);
#983=B_SPLINE_CURVE_WITH_KNOTS('',3,(#74406,#74407,#74408,#74409,#74410,
#74411,#74412,#74413,#74414,#74415,#74416),.UNSPECIFIED.,.F.,.F.,(4,1,1,
1,1,1,1,1,4),(40.8407044966672,41.1436432204315,42.1386785437051,43.1337138669788,
44.1287491902524,45.1237845135261,46.1188198367997,47.1138551600734,47.1238898038468),
 .UNSPECIFIED.);
#984=B_SPLINE_CURVE_WITH_KNOTS('',3,(#74421,#74422,#74423,#74424,#74425,
#74426,#74427,#74428,#74429,#74430),.UNSPECIFIED.,.F.,.F.,(4,1,1,1,1,1,
1,4),(34.5575191894877,35.4958806063858,36.4909159296595,37.4859512529331,
38.4809865762068,39.4760218994804,40.4710572227541,40.8407044966672),
 .UNSPECIFIED.);
#985=B_SPLINE_CURVE_WITH_KNOTS('',3,(#74431,#74432,#74433,#74434,#74435,
#74436,#74437,#74438,#74439,#74440),.UNSPECIFIED.,.F.,.F.,(4,1,1,1,1,1,
1,4),(34.5575191894876,35.1734312807896,36.1684666040632,37.1635019273369,
38.1585372506105,39.1535725738842,40.1486078971578,40.8407044966672),
 .UNSPECIFIED.);
#986=B_SPLINE_CURVE_WITH_KNOTS('',3,(#74445,#74446,#74447,#74448,#74449,
#74450,#74451,#74452,#74453,#74454,#74455),.UNSPECIFIED.,.F.,.F.,(4,1,1,
1,1,1,1,1,4),(28.2743338823081,28.5306333434703,29.5256686667439,30.5207039900176,
31.5157393132912,32.5107746365649,33.5058099598385,34.5008452831122,34.5575191894877),
 .UNSPECIFIED.);
#987=B_SPLINE_CURVE_WITH_KNOTS('',3,(#74456,#74457,#74458,#74459,#74460,
#74461,#74462,#74463,#74464,#74465),.UNSPECIFIED.,.F.,.F.,(4,1,1,1,1,1,
1,4),(28.274333882308,29.2032193411477,30.1982546644213,31.193289987695,
32.1883253109686,33.1833606342423,34.1783959575159,34.5575191894876),
 .UNSPECIFIED.);
#988=B_SPLINE_CURVE_WITH_KNOTS('',3,(#74470,#74471,#74472,#74473,#74474,
#74475,#74476,#74477,#74478,#74479),.UNSPECIFIED.,.F.,.F.,(4,1,1,1,1,1,
1,4),(21.9911485751285,22.5604214038284,23.555456727102,24.5504920503757,
25.5455273736493,26.540562696923,27.5355980201966,28.2743338823081),
 .UNSPECIFIED.);
#989=B_SPLINE_CURVE_WITH_KNOTS('',3,(#74480,#74481,#74482,#74483,#74484,
#74485,#74486,#74487,#74488,#74489,#74490),.UNSPECIFIED.,.F.,.F.,(4,1,1,
1,1,1,1,1,4),(21.9911485751284,22.2379720782321,23.2330074015058,24.2280427247794,
25.2230780480531,26.2181133713267,27.2131486946004,28.208184017874,28.274333882308),
 .UNSPECIFIED.);
#990=B_SPLINE_CURVE_WITH_KNOTS('',3,(#74495,#74496,#74497,#74498,#74499,
#74500,#74501,#74502,#74503,#74504),.UNSPECIFIED.,.F.,.F.,(4,1,1,1,1,1,
1,4),(15.7079632679489,16.5902094641865,17.5852447874601,18.5802801107338,
19.5753154340074,20.5703507572811,21.5653860805547,21.9911485751285),
 .UNSPECIFIED.);
#991=B_SPLINE_CURVE_WITH_KNOTS('',3,(#74505,#74506,#74507,#74508,#74509,
#74510,#74511,#74512,#74513,#74514),.UNSPECIFIED.,.F.,.F.,(4,1,1,1,1,1,
1,4),(15.7079632679489,16.2677601385902,17.2627954618639,18.2578307851375,
19.2528661084112,20.2479014316848,21.2429367549585,21.9911485751284),
 .UNSPECIFIED.);
#992=B_SPLINE_CURVE_WITH_KNOTS('',3,(#74516,#74517,#74518,#74519,#74520,
#74521,#74522,#74523,#74524,#74525,#74526,#74527,#74528,#74529,#74530,#74531,
#74532,#74533,#74534,#74535,#74536,#74537,#74538,#74539,#74540,#74541,#74542,
#74543,#74544,#74545,#74546,#74547,#74548,#74549,#74550,#74551,#74552,#74553,
#74554,#74555,#74556,#74557,#74558,#74559,#74560,#74561,#74562,#74563,#74564,
#74565,#74566,#74567,#74568,#74569,#74570),.UNSPECIFIED.,.F.,.F.,(4,3,3,
3,3,3,3,3,3,3,3,3,3,3,3,3,3,3,4),(-0.555272788399296,-0.536334845639292,
-0.498799075009887,-0.480079388780021,-0.444545864814167,-0.427699608514178,
-0.413313249422015,-0.365214576623026,-0.332698016808039,-0.315863285595313,
-0.281639241746625,-0.246434336528297,-0.224130346638797,-0.211045162239551,
-0.161112023899574,-0.115330355900824,-0.101980705380743,-0.0495823722640936,
0.),.UNSPECIFIED.);
#993=B_SPLINE_CURVE_WITH_KNOTS('',3,(#74573,#74574,#74575,#74576,#74577,
#74578,#74579,#74580,#74581,#74582,#74583,#74584,#74585,#74586,#74587,#74588,
#74589,#74590,#74591,#74592,#74593,#74594,#74595,#74596,#74597,#74598,#74599,
#74600,#74601,#74602,#74603,#74604,#74605,#74606,#74607,#74608,#74609,#74610,
#74611,#74612,#74613,#74614,#74615,#74616,#74617,#74618,#74619,#74620,#74621,
#74622,#74623,#74624,#74625,#74626,#74627,#74628,#74629,#74630),
 .UNSPECIFIED.,.F.,.F.,(4,3,3,3,3,3,3,3,3,3,3,3,3,3,3,3,3,3,3,4),(-0.552745378375053,
-0.529682502351927,-0.492625929038547,-0.475852674070136,-0.459554142798526,
-0.429705175104552,-0.407584520370654,-0.3903823622905,-0.340467563061915,
-0.306542400025418,-0.292717972343459,-0.251653204733385,-0.202811158742405,
-0.189814062131831,-0.142360546598873,-0.105670766634947,-0.0926673115723117,
-0.0463336557861558,-0.00283643147681147,0.),.UNSPECIFIED.);
#994=B_SPLINE_CURVE_WITH_KNOTS('',3,(#75139,#75140,#75141,#75142),
 .UNSPECIFIED.,.F.,.F.,(4,4),(120.49782124478,121.315741911023),
 .UNSPECIFIED.);
#995=B_SPLINE_CURVE_WITH_KNOTS('',3,(#75144,#75145,#75146,#75147,#75148,
#75149,#75150,#75151,#75152,#75153,#75154,#75155,#75156,#75157,#75158,#75159,
#75160,#75161,#75162,#75163,#75164,#75165,#75166,#75167,#75168,#75169,#75170,
#75171,#75172,#75173,#75174,#75175,#75176,#75177,#75178,#75179,#75180,#75181,
#75182,#75183,#75184,#75185,#75186,#75187,#75188,#75189,#75190,#75191,#75192,
#75193,#75194,#75195,#75196,#75197,#75198),.UNSPECIFIED.,.F.,.F.,(4,3,3,
3,3,3,3,3,3,3,3,3,3,3,3,3,3,3,4),(-0.55527278839938,-0.536334845639381,
-0.498799076325247,-0.480079393209122,-0.444545051261333,-0.427702481446592,
-0.413318783858085,-0.365220196215889,-0.332701424146626,-0.315863774062079,
-0.281639241746661,-0.246434336528328,-0.22413033896029,-0.211045152097239,
-0.161112024781915,-0.115330357453797,-0.101980704464306,-0.0495823608376667,
0.),.UNSPECIFIED.);
#996=B_SPLINE_CURVE_WITH_KNOTS('',3,(#75199,#75200,#75201,#75202,#75203,
#75204,#75205,#75206,#75207),.UNSPECIFIED.,.F.,.F.,(4,1,1,1,1,1,4),(10.3761157273102,
11.292583522222,12.2876188454956,13.2826541687693,14.2776894920429,15.2727248153166,
15.7079632679489),.UNSPECIFIED.);
#997=B_SPLINE_CURVE_WITH_KNOTS('',3,(#75213,#75214,#75215,#75216,#75217,
#75218,#75219,#75220,#75221,#75222,#75223,#75224,#75225,#75226,#75227,#75228,
#75229,#75230,#75231,#75232,#75233,#75234,#75235,#75236,#75237,#75238,#75239,
#75240,#75241,#75242,#75243,#75244,#75245,#75246,#75247,#75248,#75249,#75250,
#75251,#75252,#75253,#75254,#75255,#75256,#75257,#75258,#75259,#75260,#75261,
#75262,#75263,#75264,#75265,#75266,#75267,#75268,#75269,#75270),
 .UNSPECIFIED.,.F.,.F.,(4,3,3,3,3,3,3,3,3,3,3,3,3,3,3,3,3,3,3,4),(-0.552745378375031,
-0.529682502351911,-0.492625920903535,-0.475852659500376,-0.45955413358707,
-0.42970514462757,-0.40758439098946,-0.390382317972672,-0.340467508816843,
-0.306542269974025,-0.292717807416595,-0.251653204733357,-0.202811154924846,
-0.189814058627298,-0.142360543970473,-0.10567076548842,-0.0926673119182951,
-0.0463336559591476,-0.00283647083604326,0.),.UNSPECIFIED.);
#998=B_SPLINE_CURVE_WITH_KNOTS('',3,(#75273,#75274,#75275,#75276,#75277,
#75278,#75279,#75280),.UNSPECIFIED.,.F.,.F.,(4,1,1,1,1,4),(11.6150328478182,
12.6100681710919,13.6051034943655,14.6001388176392,15.5951741409128,15.7079632679489),
 .UNSPECIFIED.);
#1018=SHAPE_REPRESENTATION_RELATIONSHIP('SRR','None',#76755,#1038);
#1038=ADVANCED_BREP_SHAPE_REPRESENTATION('',(#1078),#76659);
#1058=STYLED_ITEM('',(#76913),#1078);
#1078=MANIFOLD_SOLID_BREP('Socket head screw',#26683);
#1088=TOROIDAL_SURFACE('',#29028,0.3192,0.025);
#1511=CYLINDRICAL_SURFACE('',#28979,0.2942);
#1512=CYLINDRICAL_SURFACE('',#28981,0.2942);
#1513=CYLINDRICAL_SURFACE('',#28982,0.2942);
#1514=CYLINDRICAL_SURFACE('',#28983,0.2942);
#1515=CYLINDRICAL_SURFACE('',#28984,0.2942);
#1516=CYLINDRICAL_SURFACE('',#28985,0.2942);
#1517=CYLINDRICAL_SURFACE('',#28986,0.2942);
#1518=CYLINDRICAL_SURFACE('',#28987,0.2942);
#1519=CYLINDRICAL_SURFACE('',#28988,0.2942);
#1520=CYLINDRICAL_SURFACE('',#28989,0.2942);
#1521=CYLINDRICAL_SURFACE('',#28990,0.2942);
#1522=CYLINDRICAL_SURFACE('',#28991,0.2942);
#1523=CYLINDRICAL_SURFACE('',#28992,0.2942);
#1524=CYLINDRICAL_SURFACE('',#28993,0.2942);
#1525=CYLINDRICAL_SURFACE('',#28994,0.2942);
#1526=CYLINDRICAL_SURFACE('',#28995,0.2942);
#1527=CYLINDRICAL_SURFACE('',#28996,0.2942);
#1528=CYLINDRICAL_SURFACE('',#28997,0.2942);
#1529=CYLINDRICAL_SURFACE('',#28998,0.2942);
#1530=CYLINDRICAL_SURFACE('',#28999,0.2942);
#1531=CYLINDRICAL_SURFACE('',#29001,0.237175);
#1532=CYLINDRICAL_SURFACE('',#29003,0.237175);
#1533=CYLINDRICAL_SURFACE('',#29004,0.237175);
#1534=CYLINDRICAL_SURFACE('',#29005,0.237175);
#1535=CYLINDRICAL_SURFACE('',#29006,0.237175);
#1536=CYLINDRICAL_SURFACE('',#29007,0.237175);
#1537=CYLINDRICAL_SURFACE('',#29008,0.237175);
#1538=CYLINDRICAL_SURFACE('',#29009,0.237175);
#1539=CYLINDRICAL_SURFACE('',#29010,0.237175);
#1540=CYLINDRICAL_SURFACE('',#29011,0.237175);
#1541=CYLINDRICAL_SURFACE('',#29012,0.237175);
#1542=CYLINDRICAL_SURFACE('',#29013,0.237175);
#1543=CYLINDRICAL_SURFACE('',#29014,0.237175);
#1544=CYLINDRICAL_SURFACE('',#29015,0.237175);
#1545=CYLINDRICAL_SURFACE('',#29016,0.237175);
#1546=CYLINDRICAL_SURFACE('',#29017,0.237175);
#1547=CYLINDRICAL_SURFACE('',#29018,0.237175);
#1548=CYLINDRICAL_SURFACE('',#29019,0.237175);
#1549=CYLINDRICAL_SURFACE('',#29020,0.237175);
#1550=CYLINDRICAL_SURFACE('',#29027,0.237175);
#1551=CYLINDRICAL_SURFACE('',#29032,0.2942);
#1552=CYLINDRICAL_SURFACE('',#29277,0.5);
#1654=FACE_BOUND('',#5566,.T.);
#1655=FACE_BOUND('',#5730,.T.);
#2363=PLANE('',#29021);
#2364=PLANE('',#29023);
#2365=PLANE('',#29033);
#2366=PLANE('',#29035);
#2367=PLANE('',#29037);
#2368=PLANE('',#29039);
#2369=PLANE('',#29041);
#2370=PLANE('',#29043);
#2371=PLANE('',#29045);
#2372=PLANE('',#29048);
#2373=PLANE('',#29049);
#2374=PLANE('',#29050);
#2375=PLANE('',#29051);
#2376=PLANE('',#29052);
#2377=PLANE('',#29053);
#2378=PLANE('',#29054);
#2379=PLANE('',#29055);
#2380=PLANE('',#29057);
#2381=PLANE('',#29058);
#2382=PLANE('',#29060);
#2383=PLANE('',#29061);
#2384=PLANE('',#29063);
#2385=PLANE('',#29064);
#2386=PLANE('',#29066);
#2387=PLANE('',#29067);
#2388=PLANE('',#29069);
#2389=PLANE('',#29070);
#2390=PLANE('',#29072);
#2391=PLANE('',#29073);
#2392=PLANE('',#29075);
#2393=PLANE('',#29076);
#2394=PLANE('',#29078);
#2395=PLANE('',#29079);
#2396=PLANE('',#29081);
#2397=PLANE('',#29082);
#2398=PLANE('',#29084);
#2399=PLANE('',#29085);
#2400=PLANE('',#29087);
#2401=PLANE('',#29088);
#2402=PLANE('',#29090);
#2403=PLANE('',#29091);
#2404=PLANE('',#29093);
#2405=PLANE('',#29094);
#2406=PLANE('',#29096);
#2407=PLANE('',#29097);
#2408=PLANE('',#29099);
#2409=PLANE('',#29100);
#2410=PLANE('',#29102);
#2411=PLANE('',#29103);
#2412=PLANE('',#29106);
#2413=PLANE('',#29107);
#2414=PLANE('',#29110);
#2415=PLANE('',#29111);
#2416=PLANE('',#29113);
#2417=PLANE('',#29114);
#2418=PLANE('',#29116);
#2419=PLANE('',#29117);
#2420=PLANE('',#29119);
#2421=PLANE('',#29120);
#2422=PLANE('',#29122);
#2423=PLANE('',#29123);
#2424=PLANE('',#29125);
#2425=PLANE('',#29126);
#2426=PLANE('',#29128);
#2427=PLANE('',#29129);
#2428=PLANE('',#29131);
#2429=PLANE('',#29132);
#2430=PLANE('',#29134);
#2431=PLANE('',#29135);
#2432=PLANE('',#29137);
#2433=PLANE('',#29138);
#2434=PLANE('',#29140);
#2435=PLANE('',#29141);
#2436=PLANE('',#29143);
#2437=PLANE('',#29144);
#2438=PLANE('',#29146);
#2439=PLANE('',#29147);
#2440=PLANE('',#29149);
#2441=PLANE('',#29150);
#2442=PLANE('',#29152);
#2443=PLANE('',#29153);
#2444=PLANE('',#29155);
#2445=PLANE('',#29156);
#2446=PLANE('',#29158);
#2447=PLANE('',#29159);
#2448=PLANE('',#29161);
#2449=PLANE('',#29162);
#2450=PLANE('',#29164);
#2451=PLANE('',#29165);
#2452=PLANE('',#29167);
#2453=PLANE('',#29168);
#2454=PLANE('',#29170);
#2455=PLANE('',#29171);
#2456=PLANE('',#29173);
#2457=PLANE('',#29174);
#2458=PLANE('',#29176);
#2459=PLANE('',#29177);
#2460=PLANE('',#29179);
#2461=PLANE('',#29180);
#2462=PLANE('',#29182);
#2463=PLANE('',#29183);
#2464=PLANE('',#29185);
#2465=PLANE('',#29186);
#2466=PLANE('',#29188);
#2467=PLANE('',#29189);
#2468=PLANE('',#29191);
#2469=PLANE('',#29192);
#2470=PLANE('',#29194);
#2471=PLANE('',#29195);
#2472=PLANE('',#29197);
#2473=PLANE('',#29198);
#2474=PLANE('',#29200);
#2475=PLANE('',#29201);
#2476=PLANE('',#29203);
#2477=PLANE('',#29204);
#2478=PLANE('',#29206);
#2479=PLANE('',#29207);
#2480=PLANE('',#29209);
#2481=PLANE('',#29210);
#2482=PLANE('',#29212);
#2483=PLANE('',#29214);
#2484=PLANE('',#29215);
#2485=PLANE('',#29216);
#2486=PLANE('',#29218);
#2487=PLANE('',#29219);
#2488=PLANE('',#29221);
#2489=PLANE('',#29222);
#2490=PLANE('',#29224);
#2491=PLANE('',#29225);
#2492=PLANE('',#29227);
#2493=PLANE('',#29228);
#2494=PLANE('',#29230);
#2495=PLANE('',#29231);
#2496=PLANE('',#29233);
#2497=PLANE('',#29234);
#2498=PLANE('',#29236);
#2499=PLANE('',#29237);
#2500=PLANE('',#29239);
#2501=PLANE('',#29240);
#2502=PLANE('',#29242);
#2503=PLANE('',#29243);
#2504=PLANE('',#29245);
#2505=PLANE('',#29246);
#2506=PLANE('',#29248);
#2507=PLANE('',#29249);
#2508=PLANE('',#29251);
#2509=PLANE('',#29252);
#2510=PLANE('',#29254);
#2511=PLANE('',#29255);
#2512=PLANE('',#29257);
#2513=PLANE('',#29258);
#2514=PLANE('',#29260);
#2515=PLANE('',#29261);
#2516=PLANE('',#29263);
#2517=PLANE('',#29264);
#2518=PLANE('',#29266);
#2519=PLANE('',#29267);
#2520=PLANE('',#29269);
#2521=PLANE('',#29270);
#2522=PLANE('',#29272);
#2523=PLANE('',#29316);
#3866=FACE_OUTER_BOUND('',#5519,.T.);
#3867=FACE_OUTER_BOUND('',#5520,.T.);
#3868=FACE_OUTER_BOUND('',#5521,.T.);
#3869=FACE_OUTER_BOUND('',#5522,.T.);
#3870=FACE_OUTER_BOUND('',#5523,.T.);
#3871=FACE_OUTER_BOUND('',#5524,.T.);
#3872=FACE_OUTER_BOUND('',#5525,.T.);
#3873=FACE_OUTER_BOUND('',#5526,.T.);
#3874=FACE_OUTER_BOUND('',#5527,.T.);
#3875=FACE_OUTER_BOUND('',#5528,.T.);
#3876=FACE_OUTER_BOUND('',#5529,.T.);
#3877=FACE_OUTER_BOUND('',#5530,.T.);
#3878=FACE_OUTER_BOUND('',#5531,.T.);
#3879=FACE_OUTER_BOUND('',#5532,.T.);
#3880=FACE_OUTER_BOUND('',#5533,.T.);
#3881=FACE_OUTER_BOUND('',#5534,.T.);
#3882=FACE_OUTER_BOUND('',#5535,.T.);
#3883=FACE_OUTER_BOUND('',#5536,.T.);
#3884=FACE_OUTER_BOUND('',#5537,.T.);
#3885=FACE_OUTER_BOUND('',#5538,.T.);
#3886=FACE_OUTER_BOUND('',#5539,.T.);
#3887=FACE_OUTER_BOUND('',#5540,.T.);
#3888=FACE_OUTER_BOUND('',#5541,.T.);
#3889=FACE_OUTER_BOUND('',#5542,.T.);
#3890=FACE_OUTER_BOUND('',#5543,.T.);
#3891=FACE_OUTER_BOUND('',#5544,.T.);
#3892=FACE_OUTER_BOUND('',#5545,.T.);
#3893=FACE_OUTER_BOUND('',#5546,.T.);
#3894=FACE_OUTER_BOUND('',#5547,.T.);
#3895=FACE_OUTER_BOUND('',#5548,.T.);
#3896=FACE_OUTER_BOUND('',#5549,.T.);
#3897=FACE_OUTER_BOUND('',#5550,.T.);
#3898=FACE_OUTER_BOUND('',#5551,.T.);
#3899=FACE_OUTER_BOUND('',#5552,.T.);
#3900=FACE_OUTER_BOUND('',#5553,.T.);
#3901=FACE_OUTER_BOUND('',#5554,.T.);
#3902=FACE_OUTER_BOUND('',#5555,.T.);
#3903=FACE_OUTER_BOUND('',#5556,.T.);
#3904=FACE_OUTER_BOUND('',#5557,.T.);
#3905=FACE_OUTER_BOUND('',#5558,.T.);
#3906=FACE_OUTER_BOUND('',#5559,.T.);
#3907=FACE_OUTER_BOUND('',#5560,.T.);
#3908=FACE_OUTER_BOUND('',#5561,.T.);
#3909=FACE_OUTER_BOUND('',#5562,.T.);
#3910=FACE_OUTER_BOUND('',#5563,.T.);
#3911=FACE_OUTER_BOUND('',#5564,.T.);
#3912=FACE_OUTER_BOUND('',#5565,.T.);
#3913=FACE_OUTER_BOUND('',#5567,.T.);
#3914=FACE_OUTER_BOUND('',#5568,.T.);
#3915=FACE_OUTER_BOUND('',#5569,.T.);
#3916=FACE_OUTER_BOUND('',#5570,.T.);
#3917=FACE_OUTER_BOUND('',#5571,.T.);
#3918=FACE_OUTER_BOUND('',#5572,.T.);
#3919=FACE_OUTER_BOUND('',#5573,.T.);
#3920=FACE_OUTER_BOUND('',#5574,.T.);
#3921=FACE_OUTER_BOUND('',#5575,.T.);
#3922=FACE_OUTER_BOUND('',#5576,.T.);
#3923=FACE_OUTER_BOUND('',#5577,.T.);
#3924=FACE_OUTER_BOUND('',#5578,.T.);
#3925=FACE_OUTER_BOUND('',#5579,.T.);
#3926=FACE_OUTER_BOUND('',#5580,.T.);
#3927=FACE_OUTER_BOUND('',#5581,.T.);
#3928=FACE_OUTER_BOUND('',#5582,.T.);
#3929=FACE_OUTER_BOUND('',#5583,.T.);
#3930=FACE_OUTER_BOUND('',#5584,.T.);
#3931=FACE_OUTER_BOUND('',#5585,.T.);
#3932=FACE_OUTER_BOUND('',#5586,.T.);
#3933=FACE_OUTER_BOUND('',#5587,.T.);
#3934=FACE_OUTER_BOUND('',#5588,.T.);
#3935=FACE_OUTER_BOUND('',#5589,.T.);
#3936=FACE_OUTER_BOUND('',#5590,.T.);
#3937=FACE_OUTER_BOUND('',#5591,.T.);
#3938=FACE_OUTER_BOUND('',#5592,.T.);
#3939=FACE_OUTER_BOUND('',#5593,.T.);
#3940=FACE_OUTER_BOUND('',#5594,.T.);
#3941=FACE_OUTER_BOUND('',#5595,.T.);
#3942=FACE_OUTER_BOUND('',#5596,.T.);
#3943=FACE_OUTER_BOUND('',#5597,.T.);
#3944=FACE_OUTER_BOUND('',#5598,.T.);
#3945=FACE_OUTER_BOUND('',#5599,.T.);
#3946=FACE_OUTER_BOUND('',#5600,.T.);
#3947=FACE_OUTER_BOUND('',#5601,.T.);
#3948=FACE_OUTER_BOUND('',#5602,.T.);
#3949=FACE_OUTER_BOUND('',#5603,.T.);
#3950=FACE_OUTER_BOUND('',#5604,.T.);
#3951=FACE_OUTER_BOUND('',#5605,.T.);
#3952=FACE_OUTER_BOUND('',#5606,.T.);
#3953=FACE_OUTER_BOUND('',#5607,.T.);
#3954=FACE_OUTER_BOUND('',#5608,.T.);
#3955=FACE_OUTER_BOUND('',#5609,.T.);
#3956=FACE_OUTER_BOUND('',#5610,.T.);
#3957=FACE_OUTER_BOUND('',#5611,.T.);
#3958=FACE_OUTER_BOUND('',#5612,.T.);
#3959=FACE_OUTER_BOUND('',#5613,.T.);
#3960=FACE_OUTER_BOUND('',#5614,.T.);
#3961=FACE_OUTER_BOUND('',#5615,.T.);
#3962=FACE_OUTER_BOUND('',#5616,.T.);
#3963=FACE_OUTER_BOUND('',#5617,.T.);
#3964=FACE_OUTER_BOUND('',#5618,.T.);
#3965=FACE_OUTER_BOUND('',#5619,.T.);
#3966=FACE_OUTER_BOUND('',#5620,.T.);
#3967=FACE_OUTER_BOUND('',#5621,.T.);
#3968=FACE_OUTER_BOUND('',#5622,.T.);
#3969=FACE_OUTER_BOUND('',#5623,.T.);
#3970=FACE_OUTER_BOUND('',#5624,.T.);
#3971=FACE_OUTER_BOUND('',#5625,.T.);
#3972=FACE_OUTER_BOUND('',#5626,.T.);
#3973=FACE_OUTER_BOUND('',#5627,.T.);
#3974=FACE_OUTER_BOUND('',#5628,.T.);
#3975=FACE_OUTER_BOUND('',#5629,.T.);
#3976=FACE_OUTER_BOUND('',#5630,.T.);
#3977=FACE_OUTER_BOUND('',#5631,.T.);
#3978=FACE_OUTER_BOUND('',#5632,.T.);
#3979=FACE_OUTER_BOUND('',#5633,.T.);
#3980=FACE_OUTER_BOUND('',#5634,.T.);
#3981=FACE_OUTER_BOUND('',#5635,.T.);
#3982=FACE_OUTER_BOUND('',#5636,.T.);
#3983=FACE_OUTER_BOUND('',#5637,.T.);
#3984=FACE_OUTER_BOUND('',#5638,.T.);
#3985=FACE_OUTER_BOUND('',#5639,.T.);
#3986=FACE_OUTER_BOUND('',#5640,.T.);
#3987=FACE_OUTER_BOUND('',#5641,.T.);
#3988=FACE_OUTER_BOUND('',#5642,.T.);
#3989=FACE_OUTER_BOUND('',#5643,.T.);
#3990=FACE_OUTER_BOUND('',#5644,.T.);
#3991=FACE_OUTER_BOUND('',#5645,.T.);
#3992=FACE_OUTER_BOUND('',#5646,.T.);
#3993=FACE_OUTER_BOUND('',#5647,.T.);
#3994=FACE_OUTER_BOUND('',#5648,.T.);
#3995=FACE_OUTER_BOUND('',#5649,.T.);
#3996=FACE_OUTER_BOUND('',#5650,.T.);
#3997=FACE_OUTER_BOUND('',#5651,.T.);
#3998=FACE_OUTER_BOUND('',#5652,.T.);
#3999=FACE_OUTER_BOUND('',#5653,.T.);
#4000=FACE_OUTER_BOUND('',#5654,.T.);
#4001=FACE_OUTER_BOUND('',#5655,.T.);
#4002=FACE_OUTER_BOUND('',#5656,.T.);
#4003=FACE_OUTER_BOUND('',#5657,.T.);
#4004=FACE_OUTER_BOUND('',#5658,.T.);
#4005=FACE_OUTER_BOUND('',#5659,.T.);
#4006=FACE_OUTER_BOUND('',#5660,.T.);
#4007=FACE_OUTER_BOUND('',#5661,.T.);
#4008=FACE_OUTER_BOUND('',#5662,.T.);
#4009=FACE_OUTER_BOUND('',#5663,.T.);
#4010=FACE_OUTER_BOUND('',#5664,.T.);
#4011=FACE_OUTER_BOUND('',#5665,.T.);
#4012=FACE_OUTER_BOUND('',#5666,.T.);
#4013=FACE_OUTER_BOUND('',#5667,.T.);
#4014=FACE_OUTER_BOUND('',#5668,.T.);
#4015=FACE_OUTER_BOUND('',#5669,.T.);
#4016=FACE_OUTER_BOUND('',#5670,.T.);
#4017=FACE_OUTER_BOUND('',#5671,.T.);
#4018=FACE_OUTER_BOUND('',#5672,.T.);
#4019=FACE_OUTER_BOUND('',#5673,.T.);
#4020=FACE_OUTER_BOUND('',#5674,.T.);
#4021=FACE_OUTER_BOUND('',#5675,.T.);
#4022=FACE_OUTER_BOUND('',#5676,.T.);
#4023=FACE_OUTER_BOUND('',#5677,.T.);
#4024=FACE_OUTER_BOUND('',#5678,.T.);
#4025=FACE_OUTER_BOUND('',#5679,.T.);
#4026=FACE_OUTER_BOUND('',#5680,.T.);
#4027=FACE_OUTER_BOUND('',#5681,.T.);
#4028=FACE_OUTER_BOUND('',#5682,.T.);
#4029=FACE_OUTER_BOUND('',#5683,.T.);
#4030=FACE_OUTER_BOUND('',#5684,.T.);
#4031=FACE_OUTER_BOUND('',#5685,.T.);
#4032=FACE_OUTER_BOUND('',#5686,.T.);
#4033=FACE_OUTER_BOUND('',#5687,.T.);
#4034=FACE_OUTER_BOUND('',#5688,.T.);
#4035=FACE_OUTER_BOUND('',#5689,.T.);
#4036=FACE_OUTER_BOUND('',#5690,.T.);
#4037=FACE_OUTER_BOUND('',#5691,.T.);
#4038=FACE_OUTER_BOUND('',#5692,.T.);
#4039=FACE_OUTER_BOUND('',#5693,.T.);
#4040=FACE_OUTER_BOUND('',#5694,.T.);
#4041=FACE_OUTER_BOUND('',#5695,.T.);
#4042=FACE_OUTER_BOUND('',#5696,.T.);
#4043=FACE_OUTER_BOUND('',#5697,.T.);
#4044=FACE_OUTER_BOUND('',#5698,.T.);
#4045=FACE_OUTER_BOUND('',#5699,.T.);
#4046=FACE_OUTER_BOUND('',#5700,.T.);
#4047=FACE_OUTER_BOUND('',#5701,.T.);
#4048=FACE_OUTER_BOUND('',#5702,.T.);
#4049=FACE_OUTER_BOUND('',#5703,.T.);
#4050=FACE_OUTER_BOUND('',#5704,.T.);
#4051=FACE_OUTER_BOUND('',#5705,.T.);
#4052=FACE_OUTER_BOUND('',#5706,.T.);
#4053=FACE_OUTER_BOUND('',#5707,.T.);
#4054=FACE_OUTER_BOUND('',#5708,.T.);
#4055=FACE_OUTER_BOUND('',#5709,.T.);
#4056=FACE_OUTER_BOUND('',#5710,.T.);
#4057=FACE_OUTER_BOUND('',#5711,.T.);
#4058=FACE_OUTER_BOUND('',#5712,.T.);
#4059=FACE_OUTER_BOUND('',#5713,.T.);
#4060=FACE_OUTER_BOUND('',#5714,.T.);
#4061=FACE_OUTER_BOUND('',#5715,.T.);
#4062=FACE_OUTER_BOUND('',#5716,.T.);
#4063=FACE_OUTER_BOUND('',#5717,.T.);
#4064=FACE_OUTER_BOUND('',#5718,.T.);
#4065=FACE_OUTER_BOUND('',#5719,.T.);
#4066=FACE_OUTER_BOUND('',#5720,.T.);
#4067=FACE_OUTER_BOUND('',#5721,.T.);
#4068=FACE_OUTER_BOUND('',#5722,.T.);
#4069=FACE_OUTER_BOUND('',#5723,.T.);
#4070=FACE_OUTER_BOUND('',#5724,.T.);
#4071=FACE_OUTER_BOUND('',#5725,.T.);
#4072=FACE_OUTER_BOUND('',#5726,.T.);
#4073=FACE_OUTER_BOUND('',#5727,.T.);
#4074=FACE_OUTER_BOUND('',#5728,.T.);
#4075=FACE_OUTER_BOUND('',#5729,.T.);
#5519=EDGE_LOOP('',(#23867,#23868,#23869,#23870));
#5520=EDGE_LOOP('',(#23871,#23872,#23873,#23874));
#5521=EDGE_LOOP('',(#23875,#23876,#23877,#23878));
#5522=EDGE_LOOP('',(#23879,#23880,#23881,#23882));
#5523=EDGE_LOOP('',(#23883,#23884,#23885,#23886));
#5524=EDGE_LOOP('',(#23887,#23888,#23889,#23890));
#5525=EDGE_LOOP('',(#23891,#23892,#23893,#23894));
#5526=EDGE_LOOP('',(#23895,#23896,#23897,#23898));
#5527=EDGE_LOOP('',(#23899,#23900,#23901,#23902));
#5528=EDGE_LOOP('',(#23903,#23904,#23905,#23906));
#5529=EDGE_LOOP('',(#23907,#23908,#23909,#23910));
#5530=EDGE_LOOP('',(#23911,#23912,#23913,#23914));
#5531=EDGE_LOOP('',(#23915,#23916,#23917,#23918));
#5532=EDGE_LOOP('',(#23919,#23920,#23921,#23922));
#5533=EDGE_LOOP('',(#23923,#23924,#23925,#23926));
#5534=EDGE_LOOP('',(#23927,#23928,#23929,#23930));
#5535=EDGE_LOOP('',(#23931,#23932,#23933,#23934));
#5536=EDGE_LOOP('',(#23935,#23936,#23937,#23938));
#5537=EDGE_LOOP('',(#23939,#23940,#23941,#23942));
#5538=EDGE_LOOP('',(#23943,#23944,#23945,#23946,#23947));
#5539=EDGE_LOOP('',(#23948,#23949,#23950,#23951));
#5540=EDGE_LOOP('',(#23952,#23953,#23954,#23955));
#5541=EDGE_LOOP('',(#23956,#23957,#23958,#23959));
#5542=EDGE_LOOP('',(#23960,#23961,#23962,#23963));
#5543=EDGE_LOOP('',(#23964,#23965,#23966,#23967));
#5544=EDGE_LOOP('',(#23968,#23969,#23970,#23971));
#5545=EDGE_LOOP('',(#23972,#23973,#23974,#23975));
#5546=EDGE_LOOP('',(#23976,#23977,#23978,#23979));
#5547=EDGE_LOOP('',(#23980,#23981,#23982,#23983));
#5548=EDGE_LOOP('',(#23984,#23985,#23986,#23987));
#5549=EDGE_LOOP('',(#23988,#23989,#23990,#23991));
#5550=EDGE_LOOP('',(#23992,#23993,#23994,#23995));
#5551=EDGE_LOOP('',(#23996,#23997,#23998,#23999));
#5552=EDGE_LOOP('',(#24000,#24001,#24002,#24003));
#5553=EDGE_LOOP('',(#24004,#24005,#24006,#24007));
#5554=EDGE_LOOP('',(#24008,#24009,#24010,#24011));
#5555=EDGE_LOOP('',(#24012,#24013,#24014,#24015));
#5556=EDGE_LOOP('',(#24016,#24017,#24018,#24019));
#5557=EDGE_LOOP('',(#24020,#24021,#24022,#24023));
#5558=EDGE_LOOP('',(#24024,#24025,#24026,#24027));
#5559=EDGE_LOOP('',(#24028,#24029,#24030,#24031,#24032,#24033,#24034,#24035,
#24036,#24037,#24038,#24039,#24040,#24041,#24042,#24043,#24044,#24045,#24046,
#24047,#24048,#24049,#24050,#24051,#24052,#24053,#24054,#24055,#24056,#24057,
#24058,#24059,#24060,#24061,#24062,#24063,#24064,#24065,#24066,#24067,#24068,
#24069,#24070));
#5560=EDGE_LOOP('',(#24071,#24072,#24073,#24074,#24075));
#5561=EDGE_LOOP('',(#24076,#24077,#24078,#24079));
#5562=EDGE_LOOP('',(#24080,#24081,#24082,#24083,#24084,#24085,#24086,#24087,
#24088,#24089,#24090,#24091,#24092,#24093,#24094,#24095,#24096,#24097,#24098,
#24099,#24100,#24101,#24102,#24103,#24104,#24105,#24106,#24107,#24108,#24109,
#24110,#24111,#24112,#24113,#24114,#24115,#24116,#24117,#24118,#24119,#24120,
#24121));
#5563=EDGE_LOOP('',(#24122,#24123,#24124,#24125,#24126,#24127));
#5564=EDGE_LOOP('',(#24128,#24129,#24130));
#5565=EDGE_LOOP('',(#24131));
#5566=EDGE_LOOP('',(#24132));
#5567=EDGE_LOOP('',(#24133,#24134));
#5568=EDGE_LOOP('',(#24135,#24136));
#5569=EDGE_LOOP('',(#24137,#24138));
#5570=EDGE_LOOP('',(#24139,#24140));
#5571=EDGE_LOOP('',(#24141,#24142));
#5572=EDGE_LOOP('',(#24143,#24144));
#5573=EDGE_LOOP('',(#24145,#24146,#24147,#24148,#24149,#24150,#24151,#24152));
#5574=EDGE_LOOP('',(#24153,#24154,#24155,#24156));
#5575=EDGE_LOOP('',(#24157,#24158,#24159,#24160));
#5576=EDGE_LOOP('',(#24161,#24162,#24163,#24164));
#5577=EDGE_LOOP('',(#24165,#24166,#24167,#24168));
#5578=EDGE_LOOP('',(#24169,#24170,#24171,#24172));
#5579=EDGE_LOOP('',(#24173,#24174,#24175,#24176));
#5580=EDGE_LOOP('',(#24177,#24178,#24179,#24180));
#5581=EDGE_LOOP('',(#24181,#24182,#24183));
#5582=EDGE_LOOP('',(#24184,#24185,#24186,#24187));
#5583=EDGE_LOOP('',(#24188,#24189,#24190));
#5584=EDGE_LOOP('',(#24191,#24192,#24193,#24194));
#5585=EDGE_LOOP('',(#24195,#24196,#24197));
#5586=EDGE_LOOP('',(#24198,#24199,#24200,#24201));
#5587=EDGE_LOOP('',(#24202,#24203,#24204));
#5588=EDGE_LOOP('',(#24205,#24206,#24207,#24208));
#5589=EDGE_LOOP('',(#24209,#24210,#24211));
#5590=EDGE_LOOP('',(#24212,#24213,#24214,#24215));
#5591=EDGE_LOOP('',(#24216,#24217,#24218));
#5592=EDGE_LOOP('',(#24219,#24220,#24221,#24222));
#5593=EDGE_LOOP('',(#24223,#24224,#24225));
#5594=EDGE_LOOP('',(#24226,#24227,#24228,#24229));
#5595=EDGE_LOOP('',(#24230,#24231,#24232));
#5596=EDGE_LOOP('',(#24233,#24234,#24235,#24236));
#5597=EDGE_LOOP('',(#24237,#24238,#24239));
#5598=EDGE_LOOP('',(#24240,#24241,#24242,#24243));
#5599=EDGE_LOOP('',(#24244,#24245,#24246));
#5600=EDGE_LOOP('',(#24247,#24248,#24249,#24250));
#5601=EDGE_LOOP('',(#24251,#24252,#24253));
#5602=EDGE_LOOP('',(#24254,#24255,#24256,#24257));
#5603=EDGE_LOOP('',(#24258,#24259,#24260));
#5604=EDGE_LOOP('',(#24261,#24262,#24263,#24264));
#5605=EDGE_LOOP('',(#24265,#24266,#24267));
#5606=EDGE_LOOP('',(#24268,#24269,#24270,#24271));
#5607=EDGE_LOOP('',(#24272,#24273,#24274));
#5608=EDGE_LOOP('',(#24275,#24276,#24277,#24278));
#5609=EDGE_LOOP('',(#24279,#24280,#24281));
#5610=EDGE_LOOP('',(#24282,#24283,#24284,#24285));
#5611=EDGE_LOOP('',(#24286,#24287,#24288));
#5612=EDGE_LOOP('',(#24289,#24290,#24291,#24292));
#5613=EDGE_LOOP('',(#24293,#24294,#24295,#24296));
#5614=EDGE_LOOP('',(#24297,#24298,#24299,#24300));
#5615=EDGE_LOOP('',(#24301,#24302,#24303,#24304));
#5616=EDGE_LOOP('',(#24305,#24306,#24307,#24308));
#5617=EDGE_LOOP('',(#24309,#24310,#24311));
#5618=EDGE_LOOP('',(#24312,#24313,#24314,#24315));
#5619=EDGE_LOOP('',(#24316,#24317,#24318));
#5620=EDGE_LOOP('',(#24319,#24320,#24321,#24322));
#5621=EDGE_LOOP('',(#24323,#24324,#24325));
#5622=EDGE_LOOP('',(#24326,#24327,#24328,#24329));
#5623=EDGE_LOOP('',(#24330,#24331,#24332));
#5624=EDGE_LOOP('',(#24333,#24334,#24335,#24336));
#5625=EDGE_LOOP('',(#24337,#24338,#24339));
#5626=EDGE_LOOP('',(#24340,#24341,#24342,#24343));
#5627=EDGE_LOOP('',(#24344,#24345,#24346));
#5628=EDGE_LOOP('',(#24347,#24348,#24349,#24350));
#5629=EDGE_LOOP('',(#24351,#24352,#24353));
#5630=EDGE_LOOP('',(#24354,#24355,#24356,#24357));
#5631=EDGE_LOOP('',(#24358,#24359,#24360));
#5632=EDGE_LOOP('',(#24361,#24362,#24363,#24364));
#5633=EDGE_LOOP('',(#24365,#24366,#24367));
#5634=EDGE_LOOP('',(#24368,#24369,#24370,#24371));
#5635=EDGE_LOOP('',(#24372,#24373,#24374));
#5636=EDGE_LOOP('',(#24375,#24376,#24377,#24378));
#5637=EDGE_LOOP('',(#24379,#24380,#24381));
#5638=EDGE_LOOP('',(#24382,#24383,#24384,#24385));
#5639=EDGE_LOOP('',(#24386,#24387,#24388));
#5640=EDGE_LOOP('',(#24389,#24390,#24391,#24392));
#5641=EDGE_LOOP('',(#24393,#24394,#24395));
#5642=EDGE_LOOP('',(#24396,#24397,#24398,#24399));
#5643=EDGE_LOOP('',(#24400,#24401,#24402));
#5644=EDGE_LOOP('',(#24403,#24404,#24405,#24406));
#5645=EDGE_LOOP('',(#24407,#24408,#24409));
#5646=EDGE_LOOP('',(#24410,#24411,#24412,#24413));
#5647=EDGE_LOOP('',(#24414,#24415,#24416));
#5648=EDGE_LOOP('',(#24417,#24418,#24419,#24420));
#5649=EDGE_LOOP('',(#24421,#24422,#24423));
#5650=EDGE_LOOP('',(#24424,#24425,#24426,#24427));
#5651=EDGE_LOOP('',(#24428,#24429,#24430));
#5652=EDGE_LOOP('',(#24431,#24432,#24433,#24434));
#5653=EDGE_LOOP('',(#24435,#24436,#24437));
#5654=EDGE_LOOP('',(#24438,#24439,#24440,#24441));
#5655=EDGE_LOOP('',(#24442,#24443,#24444));
#5656=EDGE_LOOP('',(#24445,#24446,#24447,#24448));
#5657=EDGE_LOOP('',(#24449,#24450,#24451));
#5658=EDGE_LOOP('',(#24452,#24453,#24454,#24455));
#5659=EDGE_LOOP('',(#24456,#24457,#24458));
#5660=EDGE_LOOP('',(#24459,#24460,#24461,#24462));
#5661=EDGE_LOOP('',(#24463,#24464,#24465));
#5662=EDGE_LOOP('',(#24466,#24467,#24468,#24469));
#5663=EDGE_LOOP('',(#24470,#24471,#24472));
#5664=EDGE_LOOP('',(#24473,#24474,#24475,#24476));
#5665=EDGE_LOOP('',(#24477,#24478,#24479));
#5666=EDGE_LOOP('',(#24480,#24481,#24482,#24483));
#5667=EDGE_LOOP('',(#24484,#24485,#24486));
#5668=EDGE_LOOP('',(#24487,#24488,#24489,#24490));
#5669=EDGE_LOOP('',(#24491,#24492,#24493));
#5670=EDGE_LOOP('',(#24494,#24495,#24496,#24497));
#5671=EDGE_LOOP('',(#24498,#24499,#24500));
#5672=EDGE_LOOP('',(#24501,#24502,#24503,#24504));
#5673=EDGE_LOOP('',(#24505,#24506,#24507));
#5674=EDGE_LOOP('',(#24508,#24509,#24510,#24511));
#5675=EDGE_LOOP('',(#24512,#24513,#24514));
#5676=EDGE_LOOP('',(#24515,#24516,#24517,#24518));
#5677=EDGE_LOOP('',(#24519,#24520,#24521));
#5678=EDGE_LOOP('',(#24522,#24523,#24524,#24525));
#5679=EDGE_LOOP('',(#24526,#24527,#24528));
#5680=EDGE_LOOP('',(#24529,#24530,#24531,#24532));
#5681=EDGE_LOOP('',(#24533,#24534,#24535));
#5682=EDGE_LOOP('',(#24536,#24537,#24538,#24539));
#5683=EDGE_LOOP('',(#24540,#24541,#24542));
#5684=EDGE_LOOP('',(#24543,#24544,#24545));
#5685=EDGE_LOOP('',(#24546,#24547,#24548,#24549));
#5686=EDGE_LOOP('',(#24550,#24551,#24552,#24553));
#5687=EDGE_LOOP('',(#24554,#24555,#24556));
#5688=EDGE_LOOP('',(#24557,#24558,#24559,#24560));
#5689=EDGE_LOOP('',(#24561,#24562,#24563));
#5690=EDGE_LOOP('',(#24564,#24565,#24566,#24567));
#5691=EDGE_LOOP('',(#24568,#24569,#24570));
#5692=EDGE_LOOP('',(#24571,#24572,#24573,#24574));
#5693=EDGE_LOOP('',(#24575,#24576,#24577));
#5694=EDGE_LOOP('',(#24578,#24579,#24580,#24581));
#5695=EDGE_LOOP('',(#24582,#24583,#24584));
#5696=EDGE_LOOP('',(#24585,#24586,#24587,#24588));
#5697=EDGE_LOOP('',(#24589,#24590,#24591));
#5698=EDGE_LOOP('',(#24592,#24593,#24594,#24595));
#5699=EDGE_LOOP('',(#24596,#24597,#24598));
#5700=EDGE_LOOP('',(#24599,#24600,#24601,#24602));
#5701=EDGE_LOOP('',(#24603,#24604,#24605));
#5702=EDGE_LOOP('',(#24606,#24607,#24608,#24609));
#5703=EDGE_LOOP('',(#24610,#24611,#24612));
#5704=EDGE_LOOP('',(#24613,#24614,#24615,#24616));
#5705=EDGE_LOOP('',(#24617,#24618,#24619));
#5706=EDGE_LOOP('',(#24620,#24621,#24622,#24623));
#5707=EDGE_LOOP('',(#24624,#24625,#24626));
#5708=EDGE_LOOP('',(#24627,#24628,#24629,#24630));
#5709=EDGE_LOOP('',(#24631,#24632,#24633));
#5710=EDGE_LOOP('',(#24634,#24635,#24636,#24637));
#5711=EDGE_LOOP('',(#24638,#24639,#24640));
#5712=EDGE_LOOP('',(#24641,#24642,#24643,#24644));
#5713=EDGE_LOOP('',(#24645,#24646,#24647));
#5714=EDGE_LOOP('',(#24648,#24649,#24650,#24651));
#5715=EDGE_LOOP('',(#24652,#24653,#24654));
#5716=EDGE_LOOP('',(#24655,#24656,#24657,#24658));
#5717=EDGE_LOOP('',(#24659,#24660,#24661));
#5718=EDGE_LOOP('',(#24662,#24663,#24664,#24665));
#5719=EDGE_LOOP('',(#24666,#24667,#24668));
#5720=EDGE_LOOP('',(#24669,#24670,#24671,#24672));
#5721=EDGE_LOOP('',(#24673,#24674,#24675));
#5722=EDGE_LOOP('',(#24676,#24677,#24678,#24679));
#5723=EDGE_LOOP('',(#24680,#24681,#24682));
#5724=EDGE_LOOP('',(#24683));
#5725=EDGE_LOOP('',(#24684,#24685,#24686,#24687,#24688,#24689));
#5726=EDGE_LOOP('',(#24690,#24691,#24692,#24693));
#5727=EDGE_LOOP('',(#24694,#24695,#24696,#24697,#24698,#24699,#24700,#24701,
#24702,#24703,#24704,#24705,#24706,#24707,#24708,#24709,#24710,#24711,#24712,
#24713,#24714,#24715,#24716,#24717,#24718,#24719,#24720,#24721,#24722,#24723,
#24724,#24725,#24726,#24727,#24728,#24729,#24730,#24731,#24732,#24733,#24734,
#24735,#24736,#24737,#24738,#24739,#24740,#24741,#24742,#24743,#24744,#24745,
#24746,#24747,#24748,#24749,#24750,#24751,#24752,#24753,#24754,#24755,#24756,
#24757,#24758,#24759,#24760,#24761,#24762,#24763,#24764,#24765,#24766,#24767,
#24768,#24769,#24770,#24771,#24772,#24773,#24774,#24775,#24776,#24777,#24778,
#24779,#24780,#24781,#24782,#24783,#24784,#24785,#24786,#24787,#24788,#24789,
#24790,#24791,#24792,#24793,#24794,#24795,#24796,#24797,#24798,#24799,#24800,
#24801,#24802,#24803,#24804,#24805,#24806,#24807,#24808,#24809,#24810,#24811,
#24812,#24813,#24814,#24815,#24816,#24817,#24818,#24819,#24820,#24821,#24822,
#24823,#24824,#24825,#24826,#24827,#24828,#24829,#24830,#24831,#24832,#24833,
#24834,#24835,#24836,#24837,#24838,#24839,#24840,#24841));
#5728=EDGE_LOOP('',(#24842,#24843,#24844,#24845,#24846,#24847,#24848,#24849,
#24850,#24851,#24852,#24853,#24854,#24855,#24856,#24857,#24858,#24859,#24860,
#24861,#24862,#24863,#24864,#24865,#24866,#24867,#24868,#24869,#24870,#24871,
#24872,#24873,#24874,#24875,#24876,#24877,#24878,#24879,#24880,#24881,#24882,
#24883,#24884,#24885,#24886,#24887,#24888,#24889,#24890,#24891,#24892,#24893,
#24894,#24895,#24896,#24897,#24898,#24899,#24900,#24901,#24902,#24903,#24904,
#24905,#24906,#24907,#24908,#24909,#24910,#24911,#24912,#24913,#24914,#24915,
#24916,#24917));
#5729=EDGE_LOOP('',(#24918));
#5730=EDGE_LOOP('',(#24919,#24920,#24921,#24922,#24923,#24924));
#6462=CIRCLE('',#28980,0.2942);
#6463=CIRCLE('',#29000,0.2942);
#6464=CIRCLE('',#29002,0.237175);
#6465=CIRCLE('',#29022,0.2942);
#6466=CIRCLE('',#29024,0.2942);
#6467=CIRCLE('',#29025,0.2942);
#6468=CIRCLE('',#29026,0.237175);
#6469=CIRCLE('',#29029,0.025);
#6470=CIRCLE('',#29030,0.3192);
#6471=CIRCLE('',#29031,0.2942);
#6472=CIRCLE('',#29034,0.47);
#6473=CIRCLE('',#29036,0.288675134594813);
#6474=CIRCLE('',#29038,0.288675134594813);
#6475=CIRCLE('',#29040,0.288675134594813);
#6476=CIRCLE('',#29042,0.288675134594813);
#6477=CIRCLE('',#29044,0.288675134594813);
#6478=CIRCLE('',#29046,0.288675134594813);
#6479=CIRCLE('',#29056,0.5);
#6480=CIRCLE('',#29059,0.5);
#6481=CIRCLE('',#29062,0.5);
#6482=CIRCLE('',#29065,0.5);
#6483=CIRCLE('',#29068,0.5);
#6484=CIRCLE('',#29071,0.5);
#6485=CIRCLE('',#29074,0.5);
#6486=CIRCLE('',#29077,0.5);
#6487=CIRCLE('',#29080,0.5);
#6488=CIRCLE('',#29083,0.5);
#6489=CIRCLE('',#29086,0.5);
#6490=CIRCLE('',#29089,0.5);
#6491=CIRCLE('',#29092,0.5);
#6492=CIRCLE('',#29095,0.5);
#6493=CIRCLE('',#29098,0.5);
#6494=CIRCLE('',#29101,0.5);
#6495=CIRCLE('',#29104,0.5);
#6496=CIRCLE('',#29105,0.5);
#6497=CIRCLE('',#29108,0.5);
#6498=CIRCLE('',#29109,0.5);
#6499=CIRCLE('',#29112,0.5);
#6500=CIRCLE('',#29115,0.5);
#6501=CIRCLE('',#29118,0.5);
#6502=CIRCLE('',#29121,0.5);
#6503=CIRCLE('',#29124,0.5);
#6504=CIRCLE('',#29127,0.5);
#6505=CIRCLE('',#29130,0.5);
#6506=CIRCLE('',#29133,0.5);
#6507=CIRCLE('',#29136,0.5);
#6508=CIRCLE('',#29139,0.5);
#6509=CIRCLE('',#29142,0.5);
#6510=CIRCLE('',#29145,0.5);
#6511=CIRCLE('',#29148,0.5);
#6512=CIRCLE('',#29151,0.5);
#6513=CIRCLE('',#29154,0.5);
#6514=CIRCLE('',#29157,0.5);
#6515=CIRCLE('',#29160,0.5);
#6516=CIRCLE('',#29163,0.5);
#6517=CIRCLE('',#29166,0.5);
#6518=CIRCLE('',#29169,0.5);
#6519=CIRCLE('',#29172,0.5);
#6520=CIRCLE('',#29175,0.5);
#6521=CIRCLE('',#29178,0.5);
#6522=CIRCLE('',#29181,0.5);
#6523=CIRCLE('',#29184,0.5);
#6524=CIRCLE('',#29187,0.5);
#6525=CIRCLE('',#29190,0.5);
#6526=CIRCLE('',#29193,0.5);
#6527=CIRCLE('',#29196,0.5);
#6528=CIRCLE('',#29199,0.5);
#6529=CIRCLE('',#29202,0.5);
#6530=CIRCLE('',#29205,0.5);
#6531=CIRCLE('',#29208,0.5);
#6532=CIRCLE('',#29211,0.5);
#6533=CIRCLE('',#29213,0.5);
#6534=CIRCLE('',#29217,0.5);
#6535=CIRCLE('',#29220,0.5);
#6536=CIRCLE('',#29223,0.5);
#6537=CIRCLE('',#29226,0.5);
#6538=CIRCLE('',#29229,0.5);
#6539=CIRCLE('',#29232,0.5);
#6540=CIRCLE('',#29235,0.5);
#6541=CIRCLE('',#29238,0.5);
#6542=CIRCLE('',#29241,0.5);
#6543=CIRCLE('',#29244,0.5);
#6544=CIRCLE('',#29247,0.5);
#6545=CIRCLE('',#29250,0.5);
#6546=CIRCLE('',#29253,0.5);
#6547=CIRCLE('',#29256,0.5);
#6548=CIRCLE('',#29259,0.5);
#6549=CIRCLE('',#29262,0.5);
#6550=CIRCLE('',#29265,0.5);
#6551=CIRCLE('',#29268,0.5);
#6552=CIRCLE('',#29271,0.5);
#6553=CIRCLE('',#29273,0.25);
#6554=CIRCLE('',#29276,0.5);
#6555=CIRCLE('',#29278,0.5);
#6556=CIRCLE('',#29279,0.5);
#6557=CIRCLE('',#29280,0.5);
#6558=CIRCLE('',#29281,0.5);
#6559=CIRCLE('',#29282,0.5);
#6560=CIRCLE('',#29283,0.5);
#6561=CIRCLE('',#29284,0.5);
#6562=CIRCLE('',#29285,0.5);
#6563=CIRCLE('',#29286,0.5);
#6564=CIRCLE('',#29287,0.5);
#6565=CIRCLE('',#29288,0.5);
#6566=CIRCLE('',#29289,0.5);
#6567=CIRCLE('',#29290,0.5);
#6568=CIRCLE('',#29291,0.5);
#6569=CIRCLE('',#29292,0.5);
#6570=CIRCLE('',#29293,0.5);
#6571=CIRCLE('',#29294,0.5);
#6572=CIRCLE('',#29295,0.5);
#6573=CIRCLE('',#29296,0.5);
#6574=CIRCLE('',#29297,0.5);
#6575=CIRCLE('',#29298,0.5);
#6576=CIRCLE('',#29299,0.5);
#6577=CIRCLE('',#29300,0.5);
#6578=CIRCLE('',#29301,0.5);
#6579=CIRCLE('',#29302,0.5);
#6580=CIRCLE('',#29303,0.5);
#6581=CIRCLE('',#29304,0.5);
#6582=CIRCLE('',#29305,0.5);
#6583=CIRCLE('',#29306,0.5);
#6584=CIRCLE('',#29307,0.5);
#6585=CIRCLE('',#29308,0.5);
#6586=CIRCLE('',#29309,0.5);
#6587=CIRCLE('',#29310,0.5);
#6588=CIRCLE('',#29311,0.5);
#6589=CIRCLE('',#29312,0.5);
#6590=CIRCLE('',#29313,0.5);
#6591=CIRCLE('',#29315,0.45);
#8434=LINE('',#73086,#10590);
#8435=LINE('',#73110,#10591);
#8436=LINE('',#73158,#10592);
#8437=LINE('',#73206,#10593);
#8438=LINE('',#73260,#10594);
#8439=LINE('',#73308,#10595);
#8440=LINE('',#73356,#10596);
#8441=LINE('',#73407,#10597);
#8442=LINE('',#73455,#10598);
#8443=LINE('',#73503,#10599);
#8444=LINE('',#73551,#10600);
#8445=LINE('',#73605,#10601);
#8446=LINE('',#73653,#10602);
#8447=LINE('',#73701,#10603);
#8448=LINE('',#73755,#10604);
#8449=LINE('',#73803,#10605);
#8450=LINE('',#73851,#10606);
#8451=LINE('',#73905,#10607);
#8452=LINE('',#73953,#10608);
#8453=LINE('',#74001,#10609);
#8454=LINE('',#74054,#10610);
#8455=LINE('',#74075,#10611);
#8456=LINE('',#74100,#10612);
#8457=LINE('',#74124,#10613);
#8458=LINE('',#74149,#10614);
#8459=LINE('',#74174,#10615);
#8460=LINE('',#74198,#10616);
#8461=LINE('',#74223,#10617);
#8462=LINE('',#74248,#10618);
#8463=LINE('',#74272,#10619);
#8464=LINE('',#74297,#10620);
#8465=LINE('',#74322,#10621);
#8466=LINE('',#74346,#10622);
#8467=LINE('',#74370,#10623);
#8468=LINE('',#74395,#10624);
#8469=LINE('',#74420,#10625);
#8470=LINE('',#74444,#10626);
#8471=LINE('',#74469,#10627);
#8472=LINE('',#74494,#10628);
#8473=LINE('',#75801,#10629);
#8474=LINE('',#75805,#10630);
#8475=LINE('',#75809,#10631);
#8476=LINE('',#75813,#10632);
#8477=LINE('',#75817,#10633);
#8478=LINE('',#75820,#10634);
#8479=LINE('',#75824,#10635);
#8480=LINE('',#75828,#10636);
#8481=LINE('',#75829,#10637);
#8482=LINE('',#75830,#10638);
#8483=LINE('',#75833,#10639);
#8484=LINE('',#75834,#10640);
#8485=LINE('',#75837,#10641);
#8486=LINE('',#75838,#10642);
#8487=LINE('',#75841,#10643);
#8488=LINE('',#75842,#10644);
#8489=LINE('',#75845,#10645);
#8490=LINE('',#75846,#10646);
#8491=LINE('',#75848,#10647);
#8492=LINE('',#75852,#10648);
#8493=LINE('',#75854,#10649);
#8494=LINE('',#75856,#10650);
#8495=LINE('',#75857,#10651);
#8496=LINE('',#75861,#10652);
#8497=LINE('',#75864,#10653);
#8498=LINE('',#75865,#10654);
#8499=LINE('',#75871,#10655);
#8500=LINE('',#75873,#10656);
#8501=LINE('',#75875,#10657);
#8502=LINE('',#75876,#10658);
#8503=LINE('',#75880,#10659);
#8504=LINE('',#75883,#10660);
#8505=LINE('',#75884,#10661);
#8506=LINE('',#75890,#10662);
#8507=LINE('',#75892,#10663);
#8508=LINE('',#75894,#10664);
#8509=LINE('',#75895,#10665);
#8510=LINE('',#75899,#10666);
#8511=LINE('',#75902,#10667);
#8512=LINE('',#75903,#10668);
#8513=LINE('',#75909,#10669);
#8514=LINE('',#75911,#10670);
#8515=LINE('',#75913,#10671);
#8516=LINE('',#75914,#10672);
#8517=LINE('',#75918,#10673);
#8518=LINE('',#75921,#10674);
#8519=LINE('',#75922,#10675);
#8520=LINE('',#75928,#10676);
#8521=LINE('',#75930,#10677);
#8522=LINE('',#75932,#10678);
#8523=LINE('',#75933,#10679);
#8524=LINE('',#75937,#10680);
#8525=LINE('',#75940,#10681);
#8526=LINE('',#75941,#10682);
#8527=LINE('',#75947,#10683);
#8528=LINE('',#75949,#10684);
#8529=LINE('',#75951,#10685);
#8530=LINE('',#75952,#10686);
#8531=LINE('',#75956,#10687);
#8532=LINE('',#75959,#10688);
#8533=LINE('',#75960,#10689);
#8534=LINE('',#75966,#10690);
#8535=LINE('',#75968,#10691);
#8536=LINE('',#75970,#10692);
#8537=LINE('',#75971,#10693);
#8538=LINE('',#75975,#10694);
#8539=LINE('',#75978,#10695);
#8540=LINE('',#75979,#10696);
#8541=LINE('',#75985,#10697);
#8542=LINE('',#75987,#10698);
#8543=LINE('',#75989,#10699);
#8544=LINE('',#75990,#10700);
#8545=LINE('',#75994,#10701);
#8546=LINE('',#75997,#10702);
#8547=LINE('',#75998,#10703);
#8548=LINE('',#76004,#10704);
#8549=LINE('',#76006,#10705);
#8550=LINE('',#76008,#10706);
#8551=LINE('',#76009,#10707);
#8552=LINE('',#76014,#10708);
#8553=LINE('',#76018,#10709);
#8554=LINE('',#76019,#10710);
#8555=LINE('',#76027,#10711);
#8556=LINE('',#76029,#10712);
#8557=LINE('',#76031,#10713);
#8558=LINE('',#76032,#10714);
#8559=LINE('',#76036,#10715);
#8560=LINE('',#76039,#10716);
#8561=LINE('',#76040,#10717);
#8562=LINE('',#76046,#10718);
#8563=LINE('',#76048,#10719);
#8564=LINE('',#76050,#10720);
#8565=LINE('',#76051,#10721);
#8566=LINE('',#76055,#10722);
#8567=LINE('',#76058,#10723);
#8568=LINE('',#76059,#10724);
#8569=LINE('',#76065,#10725);
#8570=LINE('',#76067,#10726);
#8571=LINE('',#76069,#10727);
#8572=LINE('',#76070,#10728);
#8573=LINE('',#76074,#10729);
#8574=LINE('',#76077,#10730);
#8575=LINE('',#76078,#10731);
#8576=LINE('',#76084,#10732);
#8577=LINE('',#76086,#10733);
#8578=LINE('',#76088,#10734);
#8579=LINE('',#76089,#10735);
#8580=LINE('',#76093,#10736);
#8581=LINE('',#76096,#10737);
#8582=LINE('',#76097,#10738);
#8583=LINE('',#76103,#10739);
#8584=LINE('',#76105,#10740);
#8585=LINE('',#76107,#10741);
#8586=LINE('',#76108,#10742);
#8587=LINE('',#76112,#10743);
#8588=LINE('',#76115,#10744);
#8589=LINE('',#76116,#10745);
#8590=LINE('',#76122,#10746);
#8591=LINE('',#76124,#10747);
#8592=LINE('',#76126,#10748);
#8593=LINE('',#76127,#10749);
#8594=LINE('',#76131,#10750);
#8595=LINE('',#76134,#10751);
#8596=LINE('',#76135,#10752);
#8597=LINE('',#76141,#10753);
#8598=LINE('',#76143,#10754);
#8599=LINE('',#76145,#10755);
#8600=LINE('',#76146,#10756);
#8601=LINE('',#76150,#10757);
#8602=LINE('',#76153,#10758);
#8603=LINE('',#76154,#10759);
#8604=LINE('',#76160,#10760);
#8605=LINE('',#76162,#10761);
#8606=LINE('',#76164,#10762);
#8607=LINE('',#76165,#10763);
#8608=LINE('',#76169,#10764);
#8609=LINE('',#76172,#10765);
#8610=LINE('',#76173,#10766);
#8611=LINE('',#76179,#10767);
#8612=LINE('',#76181,#10768);
#8613=LINE('',#76183,#10769);
#8614=LINE('',#76184,#10770);
#8615=LINE('',#76188,#10771);
#8616=LINE('',#76191,#10772);
#8617=LINE('',#76192,#10773);
#8618=LINE('',#76198,#10774);
#8619=LINE('',#76200,#10775);
#8620=LINE('',#76202,#10776);
#8621=LINE('',#76203,#10777);
#8622=LINE('',#76207,#10778);
#8623=LINE('',#76210,#10779);
#8624=LINE('',#76211,#10780);
#8625=LINE('',#76217,#10781);
#8626=LINE('',#76219,#10782);
#8627=LINE('',#76221,#10783);
#8628=LINE('',#76222,#10784);
#8629=LINE('',#76226,#10785);
#8630=LINE('',#76229,#10786);
#8631=LINE('',#76230,#10787);
#8632=LINE('',#76236,#10788);
#8633=LINE('',#76238,#10789);
#8634=LINE('',#76240,#10790);
#8635=LINE('',#76241,#10791);
#8636=LINE('',#76245,#10792);
#8637=LINE('',#76248,#10793);
#8638=LINE('',#76249,#10794);
#8639=LINE('',#76255,#10795);
#8640=LINE('',#76257,#10796);
#8641=LINE('',#76259,#10797);
#8642=LINE('',#76260,#10798);
#8643=LINE('',#76264,#10799);
#8644=LINE('',#76267,#10800);
#8645=LINE('',#76268,#10801);
#8646=LINE('',#76274,#10802);
#8647=LINE('',#76276,#10803);
#8648=LINE('',#76278,#10804);
#8649=LINE('',#76279,#10805);
#8650=LINE('',#76283,#10806);
#8651=LINE('',#76286,#10807);
#8652=LINE('',#76287,#10808);
#8653=LINE('',#76293,#10809);
#8654=LINE('',#76295,#10810);
#8655=LINE('',#76297,#10811);
#8656=LINE('',#76298,#10812);
#8657=LINE('',#76302,#10813);
#8658=LINE('',#76305,#10814);
#8659=LINE('',#76306,#10815);
#8660=LINE('',#76312,#10816);
#8661=LINE('',#76314,#10817);
#8662=LINE('',#76316,#10818);
#8663=LINE('',#76317,#10819);
#8664=LINE('',#76321,#10820);
#8665=LINE('',#76324,#10821);
#8666=LINE('',#76325,#10822);
#8667=LINE('',#76331,#10823);
#8668=LINE('',#76333,#10824);
#8669=LINE('',#76335,#10825);
#8670=LINE('',#76336,#10826);
#8671=LINE('',#76340,#10827);
#8672=LINE('',#76343,#10828);
#8673=LINE('',#76344,#10829);
#8674=LINE('',#76352,#10830);
#8675=LINE('',#76353,#10831);
#8676=LINE('',#76356,#10832);
#8677=LINE('',#76358,#10833);
#8678=LINE('',#76359,#10834);
#8679=LINE('',#76362,#10835);
#8680=LINE('',#76363,#10836);
#8681=LINE('',#76369,#10837);
#8682=LINE('',#76371,#10838);
#8683=LINE('',#76373,#10839);
#8684=LINE('',#76374,#10840);
#8685=LINE('',#76378,#10841);
#8686=LINE('',#76381,#10842);
#8687=LINE('',#76382,#10843);
#8688=LINE('',#76388,#10844);
#8689=LINE('',#76390,#10845);
#8690=LINE('',#76392,#10846);
#8691=LINE('',#76393,#10847);
#8692=LINE('',#76397,#10848);
#8693=LINE('',#76400,#10849);
#8694=LINE('',#76401,#10850);
#8695=LINE('',#76407,#10851);
#8696=LINE('',#76409,#10852);
#8697=LINE('',#76411,#10853);
#8698=LINE('',#76412,#10854);
#8699=LINE('',#76416,#10855);
#8700=LINE('',#76419,#10856);
#8701=LINE('',#76420,#10857);
#8702=LINE('',#76426,#10858);
#8703=LINE('',#76428,#10859);
#8704=LINE('',#76430,#10860);
#8705=LINE('',#76431,#10861);
#8706=LINE('',#76435,#10862);
#8707=LINE('',#76438,#10863);
#8708=LINE('',#76439,#10864);
#8709=LINE('',#76445,#10865);
#8710=LINE('',#76447,#10866);
#8711=LINE('',#76449,#10867);
#8712=LINE('',#76450,#10868);
#8713=LINE('',#76454,#10869);
#8714=LINE('',#76457,#10870);
#8715=LINE('',#76458,#10871);
#8716=LINE('',#76464,#10872);
#8717=LINE('',#76466,#10873);
#8718=LINE('',#76468,#10874);
#8719=LINE('',#76469,#10875);
#8720=LINE('',#76473,#10876);
#8721=LINE('',#76476,#10877);
#8722=LINE('',#76477,#10878);
#8723=LINE('',#76483,#10879);
#8724=LINE('',#76485,#10880);
#8725=LINE('',#76487,#10881);
#8726=LINE('',#76488,#10882);
#8727=LINE('',#76492,#10883);
#8728=LINE('',#76495,#10884);
#8729=LINE('',#76496,#10885);
#8730=LINE('',#76502,#10886);
#8731=LINE('',#76504,#10887);
#8732=LINE('',#76506,#10888);
#8733=LINE('',#76507,#10889);
#8734=LINE('',#76511,#10890);
#8735=LINE('',#76514,#10891);
#8736=LINE('',#76515,#10892);
#8737=LINE('',#76521,#10893);
#8738=LINE('',#76523,#10894);
#8739=LINE('',#76525,#10895);
#8740=LINE('',#76526,#10896);
#8741=LINE('',#76530,#10897);
#8742=LINE('',#76533,#10898);
#8743=LINE('',#76534,#10899);
#8744=LINE('',#76541,#10900);
#8745=LINE('',#76545,#10901);
#8746=LINE('',#76563,#10902);
#8747=LINE('',#76587,#10903);
#10590=VECTOR('',#35337,0.3);
#10591=VECTOR('',#35342,0.3);
#10592=VECTOR('',#35345,0.3);
#10593=VECTOR('',#35348,0.3);
#10594=VECTOR('',#35351,0.3);
#10595=VECTOR('',#35354,0.3);
#10596=VECTOR('',#35357,0.3);
#10597=VECTOR('',#35360,0.3);
#10598=VECTOR('',#35363,0.3);
#10599=VECTOR('',#35366,0.3);
#10600=VECTOR('',#35369,0.3);
#10601=VECTOR('',#35372,0.3);
#10602=VECTOR('',#35375,0.3);
#10603=VECTOR('',#35378,0.3);
#10604=VECTOR('',#35381,0.3);
#10605=VECTOR('',#35384,0.3);
#10606=VECTOR('',#35387,0.3);
#10607=VECTOR('',#35390,0.3);
#10608=VECTOR('',#35393,0.3);
#10609=VECTOR('',#35396,0.3);
#10610=VECTOR('',#35401,0.237175);
#10611=VECTOR('',#35406,0.237175);
#10612=VECTOR('',#35409,0.237175);
#10613=VECTOR('',#35412,0.237175);
#10614=VECTOR('',#35415,0.237175);
#10615=VECTOR('',#35418,0.237175);
#10616=VECTOR('',#35421,0.237175);
#10617=VECTOR('',#35424,0.237175);
#10618=VECTOR('',#35427,0.237175);
#10619=VECTOR('',#35430,0.237175);
#10620=VECTOR('',#35433,0.237175);
#10621=VECTOR('',#35436,0.237175);
#10622=VECTOR('',#35439,0.237175);
#10623=VECTOR('',#35442,0.237175);
#10624=VECTOR('',#35445,0.237175);
#10625=VECTOR('',#35448,0.237175);
#10626=VECTOR('',#35451,0.237175);
#10627=VECTOR('',#35454,0.237175);
#10628=VECTOR('',#35457,0.237175);
#10629=VECTOR('',#35488,1.);
#10630=VECTOR('',#35493,1.);
#10631=VECTOR('',#35498,1.);
#10632=VECTOR('',#35503,1.);
#10633=VECTOR('',#35508,1.);
#10634=VECTOR('',#35513,1.);
#10635=VECTOR('',#35518,0.144337567297406);
#10636=VECTOR('',#35521,1.);
#10637=VECTOR('',#35522,1.);
#10638=VECTOR('',#35523,1.);
#10639=VECTOR('',#35526,1.);
#10640=VECTOR('',#35527,1.);
#10641=VECTOR('',#35530,1.);
#10642=VECTOR('',#35531,1.);
#10643=VECTOR('',#35534,1.);
#10644=VECTOR('',#35535,1.);
#10645=VECTOR('',#35538,1.);
#10646=VECTOR('',#35539,1.);
#10647=VECTOR('',#35542,1.);
#10648=VECTOR('',#35545,1.);
#10649=VECTOR('',#35546,1.);
#10650=VECTOR('',#35547,1.);
#10651=VECTOR('',#35548,1.);
#10652=VECTOR('',#35553,1.);
#10653=VECTOR('',#35556,1.);
#10654=VECTOR('',#35557,1.);
#10655=VECTOR('',#35564,1.);
#10656=VECTOR('',#35565,1.);
#10657=VECTOR('',#35566,1.);
#10658=VECTOR('',#35567,1.);
#10659=VECTOR('',#35572,1.);
#10660=VECTOR('',#35575,1.);
#10661=VECTOR('',#35576,1.);
#10662=VECTOR('',#35583,1.);
#10663=VECTOR('',#35584,1.);
#10664=VECTOR('',#35585,1.);
#10665=VECTOR('',#35586,1.);
#10666=VECTOR('',#35591,1.);
#10667=VECTOR('',#35594,1.);
#10668=VECTOR('',#35595,1.);
#10669=VECTOR('',#35602,1.);
#10670=VECTOR('',#35603,1.);
#10671=VECTOR('',#35604,1.);
#10672=VECTOR('',#35605,1.);
#10673=VECTOR('',#35610,1.);
#10674=VECTOR('',#35613,1.);
#10675=VECTOR('',#35614,1.);
#10676=VECTOR('',#35621,1.);
#10677=VECTOR('',#35622,1.);
#10678=VECTOR('',#35623,1.);
#10679=VECTOR('',#35624,1.);
#10680=VECTOR('',#35629,1.);
#10681=VECTOR('',#35632,1.);
#10682=VECTOR('',#35633,1.);
#10683=VECTOR('',#35640,1.);
#10684=VECTOR('',#35641,1.);
#10685=VECTOR('',#35642,1.);
#10686=VECTOR('',#35643,1.);
#10687=VECTOR('',#35648,1.);
#10688=VECTOR('',#35651,1.);
#10689=VECTOR('',#35652,1.);
#10690=VECTOR('',#35659,1.);
#10691=VECTOR('',#35660,1.);
#10692=VECTOR('',#35661,1.);
#10693=VECTOR('',#35662,1.);
#10694=VECTOR('',#35667,1.);
#10695=VECTOR('',#35670,1.);
#10696=VECTOR('',#35671,1.);
#10697=VECTOR('',#35678,1.);
#10698=VECTOR('',#35679,1.);
#10699=VECTOR('',#35680,1.);
#10700=VECTOR('',#35681,1.);
#10701=VECTOR('',#35686,1.);
#10702=VECTOR('',#35689,1.);
#10703=VECTOR('',#35690,1.);
#10704=VECTOR('',#35697,1.);
#10705=VECTOR('',#35698,1.);
#10706=VECTOR('',#35699,1.);
#10707=VECTOR('',#35700,1.);
#10708=VECTOR('',#35705,1.);
#10709=VECTOR('',#35710,1.);
#10710=VECTOR('',#35711,1.);
#10711=VECTOR('',#35720,1.);
#10712=VECTOR('',#35721,1.);
#10713=VECTOR('',#35722,1.);
#10714=VECTOR('',#35723,1.);
#10715=VECTOR('',#35728,1.);
#10716=VECTOR('',#35731,1.);
#10717=VECTOR('',#35732,1.);
#10718=VECTOR('',#35739,1.);
#10719=VECTOR('',#35740,1.);
#10720=VECTOR('',#35741,1.);
#10721=VECTOR('',#35742,1.);
#10722=VECTOR('',#35747,1.);
#10723=VECTOR('',#35750,1.);
#10724=VECTOR('',#35751,1.);
#10725=VECTOR('',#35758,1.);
#10726=VECTOR('',#35759,1.);
#10727=VECTOR('',#35760,1.);
#10728=VECTOR('',#35761,1.);
#10729=VECTOR('',#35766,1.);
#10730=VECTOR('',#35769,1.);
#10731=VECTOR('',#35770,1.);
#10732=VECTOR('',#35777,1.);
#10733=VECTOR('',#35778,1.);
#10734=VECTOR('',#35779,1.);
#10735=VECTOR('',#35780,1.);
#10736=VECTOR('',#35785,1.);
#10737=VECTOR('',#35788,1.);
#10738=VECTOR('',#35789,1.);
#10739=VECTOR('',#35796,1.);
#10740=VECTOR('',#35797,1.);
#10741=VECTOR('',#35798,1.);
#10742=VECTOR('',#35799,1.);
#10743=VECTOR('',#35804,1.);
#10744=VECTOR('',#35807,1.);
#10745=VECTOR('',#35808,1.);
#10746=VECTOR('',#35815,1.);
#10747=VECTOR('',#35816,1.);
#10748=VECTOR('',#35817,1.);
#10749=VECTOR('',#35818,1.);
#10750=VECTOR('',#35823,1.);
#10751=VECTOR('',#35826,1.);
#10752=VECTOR('',#35827,1.);
#10753=VECTOR('',#35834,1.);
#10754=VECTOR('',#35835,1.);
#10755=VECTOR('',#35836,1.);
#10756=VECTOR('',#35837,1.);
#10757=VECTOR('',#35842,1.);
#10758=VECTOR('',#35845,1.);
#10759=VECTOR('',#35846,1.);
#10760=VECTOR('',#35853,1.);
#10761=VECTOR('',#35854,1.);
#10762=VECTOR('',#35855,1.);
#10763=VECTOR('',#35856,1.);
#10764=VECTOR('',#35861,1.);
#10765=VECTOR('',#35864,1.);
#10766=VECTOR('',#35865,1.);
#10767=VECTOR('',#35872,1.);
#10768=VECTOR('',#35873,1.);
#10769=VECTOR('',#35874,1.);
#10770=VECTOR('',#35875,1.);
#10771=VECTOR('',#35880,1.);
#10772=VECTOR('',#35883,1.);
#10773=VECTOR('',#35884,1.);
#10774=VECTOR('',#35891,1.);
#10775=VECTOR('',#35892,1.);
#10776=VECTOR('',#35893,1.);
#10777=VECTOR('',#35894,1.);
#10778=VECTOR('',#35899,1.);
#10779=VECTOR('',#35902,1.);
#10780=VECTOR('',#35903,1.);
#10781=VECTOR('',#35910,1.);
#10782=VECTOR('',#35911,1.);
#10783=VECTOR('',#35912,1.);
#10784=VECTOR('',#35913,1.);
#10785=VECTOR('',#35918,1.);
#10786=VECTOR('',#35921,1.);
#10787=VECTOR('',#35922,1.);
#10788=VECTOR('',#35929,1.);
#10789=VECTOR('',#35930,1.);
#10790=VECTOR('',#35931,1.);
#10791=VECTOR('',#35932,1.);
#10792=VECTOR('',#35937,1.);
#10793=VECTOR('',#35940,1.);
#10794=VECTOR('',#35941,1.);
#10795=VECTOR('',#35948,1.);
#10796=VECTOR('',#35949,1.);
#10797=VECTOR('',#35950,1.);
#10798=VECTOR('',#35951,1.);
#10799=VECTOR('',#35956,1.);
#10800=VECTOR('',#35959,1.);
#10801=VECTOR('',#35960,1.);
#10802=VECTOR('',#35967,1.);
#10803=VECTOR('',#35968,1.);
#10804=VECTOR('',#35969,1.);
#10805=VECTOR('',#35970,1.);
#10806=VECTOR('',#35975,1.);
#10807=VECTOR('',#35978,1.);
#10808=VECTOR('',#35979,1.);
#10809=VECTOR('',#35986,1.);
#10810=VECTOR('',#35987,1.);
#10811=VECTOR('',#35988,1.);
#10812=VECTOR('',#35989,1.);
#10813=VECTOR('',#35994,1.);
#10814=VECTOR('',#35997,1.);
#10815=VECTOR('',#35998,1.);
#10816=VECTOR('',#36005,1.);
#10817=VECTOR('',#36006,1.);
#10818=VECTOR('',#36007,1.);
#10819=VECTOR('',#36008,1.);
#10820=VECTOR('',#36013,1.);
#10821=VECTOR('',#36016,1.);
#10822=VECTOR('',#36017,1.);
#10823=VECTOR('',#36024,1.);
#10824=VECTOR('',#36025,1.);
#10825=VECTOR('',#36026,1.);
#10826=VECTOR('',#36027,1.);
#10827=VECTOR('',#36032,1.);
#10828=VECTOR('',#36035,1.);
#10829=VECTOR('',#36036,1.);
#10830=VECTOR('',#36045,1.);
#10831=VECTOR('',#36046,1.);
#10832=VECTOR('',#36049,1.);
#10833=VECTOR('',#36050,1.);
#10834=VECTOR('',#36051,1.);
#10835=VECTOR('',#36054,1.);
#10836=VECTOR('',#36055,1.);
#10837=VECTOR('',#36062,1.);
#10838=VECTOR('',#36063,1.);
#10839=VECTOR('',#36064,1.);
#10840=VECTOR('',#36065,1.);
#10841=VECTOR('',#36070,1.);
#10842=VECTOR('',#36073,1.);
#10843=VECTOR('',#36074,1.);
#10844=VECTOR('',#36081,1.);
#10845=VECTOR('',#36082,1.);
#10846=VECTOR('',#36083,1.);
#10847=VECTOR('',#36084,1.);
#10848=VECTOR('',#36089,1.);
#10849=VECTOR('',#36092,1.);
#10850=VECTOR('',#36093,1.);
#10851=VECTOR('',#36100,1.);
#10852=VECTOR('',#36101,1.);
#10853=VECTOR('',#36102,1.);
#10854=VECTOR('',#36103,1.);
#10855=VECTOR('',#36108,1.);
#10856=VECTOR('',#36111,1.);
#10857=VECTOR('',#36112,1.);
#10858=VECTOR('',#36119,1.);
#10859=VECTOR('',#36120,1.);
#10860=VECTOR('',#36121,1.);
#10861=VECTOR('',#36122,1.);
#10862=VECTOR('',#36127,1.);
#10863=VECTOR('',#36130,1.);
#10864=VECTOR('',#36131,1.);
#10865=VECTOR('',#36138,1.);
#10866=VECTOR('',#36139,1.);
#10867=VECTOR('',#36140,1.);
#10868=VECTOR('',#36141,1.);
#10869=VECTOR('',#36146,1.);
#10870=VECTOR('',#36149,1.);
#10871=VECTOR('',#36150,1.);
#10872=VECTOR('',#36157,1.);
#10873=VECTOR('',#36158,1.);
#10874=VECTOR('',#36159,1.);
#10875=VECTOR('',#36160,1.);
#10876=VECTOR('',#36165,1.);
#10877=VECTOR('',#36168,1.);
#10878=VECTOR('',#36169,1.);
#10879=VECTOR('',#36176,1.);
#10880=VECTOR('',#36177,1.);
#10881=VECTOR('',#36178,1.);
#10882=VECTOR('',#36179,1.);
#10883=VECTOR('',#36184,1.);
#10884=VECTOR('',#36187,1.);
#10885=VECTOR('',#36188,1.);
#10886=VECTOR('',#36195,1.);
#10887=VECTOR('',#36196,1.);
#10888=VECTOR('',#36197,1.);
#10889=VECTOR('',#36198,1.);
#10890=VECTOR('',#36203,1.);
#10891=VECTOR('',#36206,1.);
#10892=VECTOR('',#36207,1.);
#10893=VECTOR('',#36214,1.);
#10894=VECTOR('',#36215,1.);
#10895=VECTOR('',#36216,1.);
#10896=VECTOR('',#36217,1.);
#10897=VECTOR('',#36222,1.);
#10898=VECTOR('',#36225,1.);
#10899=VECTOR('',#36226,1.);
#10900=VECTOR('',#36237,0.275);
#10901=VECTOR('',#36242,0.485);
#10902=VECTOR('',#36277,0.5);
#10903=VECTOR('',#36322,0.475);
#12992=VERTEX_POINT('',#73084);
#12993=VERTEX_POINT('',#73085);
#12994=VERTEX_POINT('',#73087);
#12995=VERTEX_POINT('',#73098);
#12996=VERTEX_POINT('',#73108);
#12997=VERTEX_POINT('',#73109);
#12998=VERTEX_POINT('',#73156);
#12999=VERTEX_POINT('',#73157);
#13000=VERTEX_POINT('',#73204);
#13001=VERTEX_POINT('',#73205);
#13002=VERTEX_POINT('',#73258);
#13003=VERTEX_POINT('',#73259);
#13004=VERTEX_POINT('',#73306);
#13005=VERTEX_POINT('',#73307);
#13006=VERTEX_POINT('',#73354);
#13007=VERTEX_POINT('',#73355);
#13008=VERTEX_POINT('',#73405);
#13009=VERTEX_POINT('',#73406);
#13010=VERTEX_POINT('',#73453);
#13011=VERTEX_POINT('',#73454);
#13012=VERTEX_POINT('',#73501);
#13013=VERTEX_POINT('',#73502);
#13014=VERTEX_POINT('',#73549);
#13015=VERTEX_POINT('',#73550);
#13016=VERTEX_POINT('',#73603);
#13017=VERTEX_POINT('',#73604);
#13018=VERTEX_POINT('',#73651);
#13019=VERTEX_POINT('',#73652);
#13020=VERTEX_POINT('',#73699);
#13021=VERTEX_POINT('',#73700);
#13022=VERTEX_POINT('',#73753);
#13023=VERTEX_POINT('',#73754);
#13024=VERTEX_POINT('',#73801);
#13025=VERTEX_POINT('',#73802);
#13026=VERTEX_POINT('',#73849);
#13027=VERTEX_POINT('',#73850);
#13028=VERTEX_POINT('',#73903);
#13029=VERTEX_POINT('',#73904);
#13030=VERTEX_POINT('',#73951);
#13031=VERTEX_POINT('',#73952);
#13032=VERTEX_POINT('',#73999);
#13033=VERTEX_POINT('',#74000);
#13034=VERTEX_POINT('',#74002);
#13035=VERTEX_POINT('',#74052);
#13036=VERTEX_POINT('',#74053);
#13037=VERTEX_POINT('',#74055);
#13038=VERTEX_POINT('',#74064);
#13039=VERTEX_POINT('',#74073);
#13040=VERTEX_POINT('',#74074);
#13041=VERTEX_POINT('',#74098);
#13042=VERTEX_POINT('',#74099);
#13043=VERTEX_POINT('',#74122);
#13044=VERTEX_POINT('',#74123);
#13045=VERTEX_POINT('',#74147);
#13046=VERTEX_POINT('',#74148);
#13047=VERTEX_POINT('',#74172);
#13048=VERTEX_POINT('',#74173);
#13049=VERTEX_POINT('',#74196);
#13050=VERTEX_POINT('',#74197);
#13051=VERTEX_POINT('',#74221);
#13052=VERTEX_POINT('',#74222);
#13053=VERTEX_POINT('',#74246);
#13054=VERTEX_POINT('',#74247);
#13055=VERTEX_POINT('',#74270);
#13056=VERTEX_POINT('',#74271);
#13057=VERTEX_POINT('',#74295);
#13058=VERTEX_POINT('',#74296);
#13059=VERTEX_POINT('',#74320);
#13060=VERTEX_POINT('',#74321);
#13061=VERTEX_POINT('',#74344);
#13062=VERTEX_POINT('',#74345);
#13063=VERTEX_POINT('',#74368);
#13064=VERTEX_POINT('',#74369);
#13065=VERTEX_POINT('',#74393);
#13066=VERTEX_POINT('',#74394);
#13067=VERTEX_POINT('',#74418);
#13068=VERTEX_POINT('',#74419);
#13069=VERTEX_POINT('',#74442);
#13070=VERTEX_POINT('',#74443);
#13071=VERTEX_POINT('',#74467);
#13072=VERTEX_POINT('',#74468);
#13073=VERTEX_POINT('',#74492);
#13074=VERTEX_POINT('',#74493);
#13075=VERTEX_POINT('',#74571);
#13076=VERTEX_POINT('',#75143);
#13077=VERTEX_POINT('',#75209);
#13078=VERTEX_POINT('',#75212);
#13079=VERTEX_POINT('',#75790);
#13080=VERTEX_POINT('',#75796);
#13081=VERTEX_POINT('',#75799);
#13082=VERTEX_POINT('',#75800);
#13083=VERTEX_POINT('',#75804);
#13084=VERTEX_POINT('',#75808);
#13085=VERTEX_POINT('',#75812);
#13086=VERTEX_POINT('',#75816);
#13087=VERTEX_POINT('',#75823);
#13088=VERTEX_POINT('',#75826);
#13089=VERTEX_POINT('',#75827);
#13090=VERTEX_POINT('',#75832);
#13091=VERTEX_POINT('',#75836);
#13092=VERTEX_POINT('',#75840);
#13093=VERTEX_POINT('',#75844);
#13094=VERTEX_POINT('',#75850);
#13095=VERTEX_POINT('',#75851);
#13096=VERTEX_POINT('',#75853);
#13097=VERTEX_POINT('',#75855);
#13098=VERTEX_POINT('',#75859);
#13099=VERTEX_POINT('',#75863);
#13100=VERTEX_POINT('',#75869);
#13101=VERTEX_POINT('',#75870);
#13102=VERTEX_POINT('',#75872);
#13103=VERTEX_POINT('',#75874);
#13104=VERTEX_POINT('',#75878);
#13105=VERTEX_POINT('',#75882);
#13106=VERTEX_POINT('',#75888);
#13107=VERTEX_POINT('',#75889);
#13108=VERTEX_POINT('',#75891);
#13109=VERTEX_POINT('',#75893);
#13110=VERTEX_POINT('',#75897);
#13111=VERTEX_POINT('',#75901);
#13112=VERTEX_POINT('',#75907);
#13113=VERTEX_POINT('',#75908);
#13114=VERTEX_POINT('',#75910);
#13115=VERTEX_POINT('',#75912);
#13116=VERTEX_POINT('',#75916);
#13117=VERTEX_POINT('',#75920);
#13118=VERTEX_POINT('',#75926);
#13119=VERTEX_POINT('',#75927);
#13120=VERTEX_POINT('',#75929);
#13121=VERTEX_POINT('',#75931);
#13122=VERTEX_POINT('',#75935);
#13123=VERTEX_POINT('',#75939);
#13124=VERTEX_POINT('',#75945);
#13125=VERTEX_POINT('',#75946);
#13126=VERTEX_POINT('',#75948);
#13127=VERTEX_POINT('',#75950);
#13128=VERTEX_POINT('',#75954);
#13129=VERTEX_POINT('',#75958);
#13130=VERTEX_POINT('',#75964);
#13131=VERTEX_POINT('',#75965);
#13132=VERTEX_POINT('',#75967);
#13133=VERTEX_POINT('',#75969);
#13134=VERTEX_POINT('',#75973);
#13135=VERTEX_POINT('',#75977);
#13136=VERTEX_POINT('',#75983);
#13137=VERTEX_POINT('',#75984);
#13138=VERTEX_POINT('',#75986);
#13139=VERTEX_POINT('',#75988);
#13140=VERTEX_POINT('',#75992);
#13141=VERTEX_POINT('',#75996);
#13142=VERTEX_POINT('',#76002);
#13143=VERTEX_POINT('',#76003);
#13144=VERTEX_POINT('',#76005);
#13145=VERTEX_POINT('',#76007);
#13146=VERTEX_POINT('',#76011);
#13147=VERTEX_POINT('',#76013);
#13148=VERTEX_POINT('',#76017);
#13149=VERTEX_POINT('',#76021);
#13150=VERTEX_POINT('',#76025);
#13151=VERTEX_POINT('',#76026);
#13152=VERTEX_POINT('',#76028);
#13153=VERTEX_POINT('',#76030);
#13154=VERTEX_POINT('',#76034);
#13155=VERTEX_POINT('',#76038);
#13156=VERTEX_POINT('',#76044);
#13157=VERTEX_POINT('',#76045);
#13158=VERTEX_POINT('',#76047);
#13159=VERTEX_POINT('',#76049);
#13160=VERTEX_POINT('',#76053);
#13161=VERTEX_POINT('',#76057);
#13162=VERTEX_POINT('',#76063);
#13163=VERTEX_POINT('',#76064);
#13164=VERTEX_POINT('',#76066);
#13165=VERTEX_POINT('',#76068);
#13166=VERTEX_POINT('',#76072);
#13167=VERTEX_POINT('',#76076);
#13168=VERTEX_POINT('',#76082);
#13169=VERTEX_POINT('',#76083);
#13170=VERTEX_POINT('',#76085);
#13171=VERTEX_POINT('',#76087);
#13172=VERTEX_POINT('',#76091);
#13173=VERTEX_POINT('',#76095);
#13174=VERTEX_POINT('',#76101);
#13175=VERTEX_POINT('',#76102);
#13176=VERTEX_POINT('',#76104);
#13177=VERTEX_POINT('',#76106);
#13178=VERTEX_POINT('',#76110);
#13179=VERTEX_POINT('',#76114);
#13180=VERTEX_POINT('',#76120);
#13181=VERTEX_POINT('',#76121);
#13182=VERTEX_POINT('',#76123);
#13183=VERTEX_POINT('',#76125);
#13184=VERTEX_POINT('',#76129);
#13185=VERTEX_POINT('',#76133);
#13186=VERTEX_POINT('',#76139);
#13187=VERTEX_POINT('',#76140);
#13188=VERTEX_POINT('',#76142);
#13189=VERTEX_POINT('',#76144);
#13190=VERTEX_POINT('',#76148);
#13191=VERTEX_POINT('',#76152);
#13192=VERTEX_POINT('',#76158);
#13193=VERTEX_POINT('',#76159);
#13194=VERTEX_POINT('',#76161);
#13195=VERTEX_POINT('',#76163);
#13196=VERTEX_POINT('',#76167);
#13197=VERTEX_POINT('',#76171);
#13198=VERTEX_POINT('',#76177);
#13199=VERTEX_POINT('',#76178);
#13200=VERTEX_POINT('',#76180);
#13201=VERTEX_POINT('',#76182);
#13202=VERTEX_POINT('',#76186);
#13203=VERTEX_POINT('',#76190);
#13204=VERTEX_POINT('',#76196);
#13205=VERTEX_POINT('',#76197);
#13206=VERTEX_POINT('',#76199);
#13207=VERTEX_POINT('',#76201);
#13208=VERTEX_POINT('',#76205);
#13209=VERTEX_POINT('',#76209);
#13210=VERTEX_POINT('',#76215);
#13211=VERTEX_POINT('',#76216);
#13212=VERTEX_POINT('',#76218);
#13213=VERTEX_POINT('',#76220);
#13214=VERTEX_POINT('',#76224);
#13215=VERTEX_POINT('',#76228);
#13216=VERTEX_POINT('',#76234);
#13217=VERTEX_POINT('',#76235);
#13218=VERTEX_POINT('',#76237);
#13219=VERTEX_POINT('',#76239);
#13220=VERTEX_POINT('',#76243);
#13221=VERTEX_POINT('',#76247);
#13222=VERTEX_POINT('',#76253);
#13223=VERTEX_POINT('',#76254);
#13224=VERTEX_POINT('',#76256);
#13225=VERTEX_POINT('',#76258);
#13226=VERTEX_POINT('',#76262);
#13227=VERTEX_POINT('',#76266);
#13228=VERTEX_POINT('',#76272);
#13229=VERTEX_POINT('',#76273);
#13230=VERTEX_POINT('',#76275);
#13231=VERTEX_POINT('',#76277);
#13232=VERTEX_POINT('',#76281);
#13233=VERTEX_POINT('',#76285);
#13234=VERTEX_POINT('',#76291);
#13235=VERTEX_POINT('',#76292);
#13236=VERTEX_POINT('',#76294);
#13237=VERTEX_POINT('',#76296);
#13238=VERTEX_POINT('',#76300);
#13239=VERTEX_POINT('',#76304);
#13240=VERTEX_POINT('',#76310);
#13241=VERTEX_POINT('',#76311);
#13242=VERTEX_POINT('',#76313);
#13243=VERTEX_POINT('',#76315);
#13244=VERTEX_POINT('',#76319);
#13245=VERTEX_POINT('',#76323);
#13246=VERTEX_POINT('',#76329);
#13247=VERTEX_POINT('',#76330);
#13248=VERTEX_POINT('',#76332);
#13249=VERTEX_POINT('',#76334);
#13250=VERTEX_POINT('',#76338);
#13251=VERTEX_POINT('',#76342);
#13252=VERTEX_POINT('',#76348);
#13253=VERTEX_POINT('',#76349);
#13254=VERTEX_POINT('',#76351);
#13255=VERTEX_POINT('',#76355);
#13256=VERTEX_POINT('',#76357);
#13257=VERTEX_POINT('',#76361);
#13258=VERTEX_POINT('',#76367);
#13259=VERTEX_POINT('',#76368);
#13260=VERTEX_POINT('',#76370);
#13261=VERTEX_POINT('',#76372);
#13262=VERTEX_POINT('',#76376);
#13263=VERTEX_POINT('',#76380);
#13264=VERTEX_POINT('',#76386);
#13265=VERTEX_POINT('',#76387);
#13266=VERTEX_POINT('',#76389);
#13267=VERTEX_POINT('',#76391);
#13268=VERTEX_POINT('',#76395);
#13269=VERTEX_POINT('',#76399);
#13270=VERTEX_POINT('',#76405);
#13271=VERTEX_POINT('',#76406);
#13272=VERTEX_POINT('',#76408);
#13273=VERTEX_POINT('',#76410);
#13274=VERTEX_POINT('',#76414);
#13275=VERTEX_POINT('',#76418);
#13276=VERTEX_POINT('',#76424);
#13277=VERTEX_POINT('',#76425);
#13278=VERTEX_POINT('',#76427);
#13279=VERTEX_POINT('',#76429);
#13280=VERTEX_POINT('',#76433);
#13281=VERTEX_POINT('',#76437);
#13282=VERTEX_POINT('',#76443);
#13283=VERTEX_POINT('',#76444);
#13284=VERTEX_POINT('',#76446);
#13285=VERTEX_POINT('',#76448);
#13286=VERTEX_POINT('',#76452);
#13287=VERTEX_POINT('',#76456);
#13288=VERTEX_POINT('',#76462);
#13289=VERTEX_POINT('',#76463);
#13290=VERTEX_POINT('',#76465);
#13291=VERTEX_POINT('',#76467);
#13292=VERTEX_POINT('',#76471);
#13293=VERTEX_POINT('',#76475);
#13294=VERTEX_POINT('',#76481);
#13295=VERTEX_POINT('',#76482);
#13296=VERTEX_POINT('',#76484);
#13297=VERTEX_POINT('',#76486);
#13298=VERTEX_POINT('',#76490);
#13299=VERTEX_POINT('',#76494);
#13300=VERTEX_POINT('',#76500);
#13301=VERTEX_POINT('',#76501);
#13302=VERTEX_POINT('',#76503);
#13303=VERTEX_POINT('',#76505);
#13304=VERTEX_POINT('',#76509);
#13305=VERTEX_POINT('',#76513);
#13306=VERTEX_POINT('',#76519);
#13307=VERTEX_POINT('',#76520);
#13308=VERTEX_POINT('',#76522);
#13309=VERTEX_POINT('',#76524);
#13310=VERTEX_POINT('',#76528);
#13311=VERTEX_POINT('',#76532);
#13312=VERTEX_POINT('',#76538);
#13313=VERTEX_POINT('',#76543);
#13314=VERTEX_POINT('',#76585);
#16656=EDGE_CURVE('',#12992,#12993,#8434,.T.);
#16657=EDGE_CURVE('',#12992,#12994,#914,.T.);
#16658=EDGE_CURVE('',#12994,#12995,#6462,.T.);
#16659=EDGE_CURVE('',#12995,#12993,#915,.T.);
#16660=EDGE_CURVE('',#12996,#12997,#8435,.T.);
#16661=EDGE_CURVE('',#12996,#12992,#916,.T.);
#16662=EDGE_CURVE('',#12993,#12997,#917,.T.);
#16663=EDGE_CURVE('',#12998,#12999,#8436,.T.);
#16664=EDGE_CURVE('',#12998,#12996,#918,.T.);
#16665=EDGE_CURVE('',#12997,#12999,#919,.T.);
#16666=EDGE_CURVE('',#13000,#13001,#8437,.T.);
#16667=EDGE_CURVE('',#13000,#12998,#920,.T.);
#16668=EDGE_CURVE('',#12999,#13001,#921,.T.);
#16669=EDGE_CURVE('',#13002,#13003,#8438,.T.);
#16670=EDGE_CURVE('',#13002,#13000,#922,.T.);
#16671=EDGE_CURVE('',#13001,#13003,#923,.T.);
#16672=EDGE_CURVE('',#13004,#13005,#8439,.T.);
#16673=EDGE_CURVE('',#13004,#13002,#924,.T.);
#16674=EDGE_CURVE('',#13003,#13005,#925,.T.);
#16675=EDGE_CURVE('',#13006,#13007,#8440,.T.);
#16676=EDGE_CURVE('',#13006,#13004,#926,.T.);
#16677=EDGE_CURVE('',#13005,#13007,#927,.T.);
#16678=EDGE_CURVE('',#13008,#13009,#8441,.T.);
#16679=EDGE_CURVE('',#13008,#13006,#928,.T.);
#16680=EDGE_CURVE('',#13007,#13009,#929,.T.);
#16681=EDGE_CURVE('',#13010,#13011,#8442,.T.);
#16682=EDGE_CURVE('',#13010,#13008,#930,.T.);
#16683=EDGE_CURVE('',#13009,#13011,#931,.T.);
#16684=EDGE_CURVE('',#13012,#13013,#8443,.T.);
#16685=EDGE_CURVE('',#13012,#13010,#932,.T.);
#16686=EDGE_CURVE('',#13011,#13013,#933,.T.);
#16687=EDGE_CURVE('',#13014,#13015,#8444,.T.);
#16688=EDGE_CURVE('',#13014,#13012,#934,.T.);
#16689=EDGE_CURVE('',#13013,#13015,#935,.T.);
#16690=EDGE_CURVE('',#13016,#13017,#8445,.T.);
#16691=EDGE_CURVE('',#13016,#13014,#936,.T.);
#16692=EDGE_CURVE('',#13015,#13017,#937,.T.);
#16693=EDGE_CURVE('',#13018,#13019,#8446,.T.);
#16694=EDGE_CURVE('',#13018,#13016,#938,.T.);
#16695=EDGE_CURVE('',#13017,#13019,#939,.T.);
#16696=EDGE_CURVE('',#13020,#13021,#8447,.T.);
#16697=EDGE_CURVE('',#13020,#13018,#940,.T.);
#16698=EDGE_CURVE('',#13019,#13021,#941,.T.);
#16699=EDGE_CURVE('',#13022,#13023,#8448,.T.);
#16700=EDGE_CURVE('',#13022,#13020,#942,.T.);
#16701=EDGE_CURVE('',#13021,#13023,#943,.T.);
#16702=EDGE_CURVE('',#13024,#13025,#8449,.T.);
#16703=EDGE_CURVE('',#13024,#13022,#944,.T.);
#16704=EDGE_CURVE('',#13023,#13025,#945,.T.);
#16705=EDGE_CURVE('',#13026,#13027,#8450,.T.);
#16706=EDGE_CURVE('',#13026,#13024,#946,.T.);
#16707=EDGE_CURVE('',#13025,#13027,#947,.T.);
#16708=EDGE_CURVE('',#13028,#13029,#8451,.T.);
#16709=EDGE_CURVE('',#13028,#13026,#948,.T.);
#16710=EDGE_CURVE('',#13027,#13029,#949,.T.);
#16711=EDGE_CURVE('',#13030,#13031,#8452,.T.);
#16712=EDGE_CURVE('',#13030,#13028,#950,.T.);
#16713=EDGE_CURVE('',#13029,#13031,#951,.T.);
#16714=EDGE_CURVE('',#13032,#13033,#8453,.T.);
#16715=EDGE_CURVE('',#13034,#13032,#6463,.T.);
#16716=EDGE_CURVE('',#13034,#13030,#952,.T.);
#16717=EDGE_CURVE('',#13031,#13033,#953,.T.);
#16718=EDGE_CURVE('',#13035,#13036,#8454,.T.);
#16719=EDGE_CURVE('',#13035,#13037,#954,.T.);
#16720=EDGE_CURVE('',#13038,#13037,#6464,.T.);
#16721=EDGE_CURVE('',#13036,#13038,#955,.T.);
#16722=EDGE_CURVE('',#13039,#13040,#8455,.T.);
#16723=EDGE_CURVE('',#13039,#13035,#956,.T.);
#16724=EDGE_CURVE('',#13040,#13036,#957,.T.);
#16725=EDGE_CURVE('',#13041,#13042,#8456,.T.);
#16726=EDGE_CURVE('',#13041,#13039,#958,.T.);
#16727=EDGE_CURVE('',#13042,#13040,#959,.T.);
#16728=EDGE_CURVE('',#13043,#13044,#8457,.T.);
#16729=EDGE_CURVE('',#13043,#13041,#960,.T.);
#16730=EDGE_CURVE('',#13044,#13042,#961,.T.);
#16731=EDGE_CURVE('',#13045,#13046,#8458,.T.);
#16732=EDGE_CURVE('',#13045,#13043,#962,.T.);
#16733=EDGE_CURVE('',#13046,#13044,#963,.T.);
#16734=EDGE_CURVE('',#13047,#13048,#8459,.T.);
#16735=EDGE_CURVE('',#13047,#13045,#964,.T.);
#16736=EDGE_CURVE('',#13048,#13046,#965,.T.);
#16737=EDGE_CURVE('',#13049,#13050,#8460,.T.);
#16738=EDGE_CURVE('',#13049,#13047,#966,.T.);
#16739=EDGE_CURVE('',#13050,#13048,#967,.T.);
#16740=EDGE_CURVE('',#13051,#13052,#8461,.T.);
#16741=EDGE_CURVE('',#13051,#13049,#968,.T.);
#16742=EDGE_CURVE('',#13052,#13050,#969,.T.);
#16743=EDGE_CURVE('',#13053,#13054,#8462,.T.);
#16744=EDGE_CURVE('',#13053,#13051,#970,.T.);
#16745=EDGE_CURVE('',#13054,#13052,#971,.T.);
#16746=EDGE_CURVE('',#13055,#13056,#8463,.T.);
#16747=EDGE_CURVE('',#13055,#13053,#972,.T.);
#16748=EDGE_CURVE('',#13056,#13054,#973,.T.);
#16749=EDGE_CURVE('',#13057,#13058,#8464,.T.);
#16750=EDGE_CURVE('',#13057,#13055,#974,.T.);
#16751=EDGE_CURVE('',#13058,#13056,#975,.T.);
#16752=EDGE_CURVE('',#13059,#13060,#8465,.T.);
#16753=EDGE_CURVE('',#13059,#13057,#976,.T.);
#16754=EDGE_CURVE('',#13060,#13058,#977,.T.);
#16755=EDGE_CURVE('',#13061,#13062,#8466,.T.);
#16756=EDGE_CURVE('',#13061,#13059,#978,.T.);
#16757=EDGE_CURVE('',#13062,#13060,#979,.T.);
#16758=EDGE_CURVE('',#13063,#13064,#8467,.T.);
#16759=EDGE_CURVE('',#13063,#13061,#980,.T.);
#16760=EDGE_CURVE('',#13064,#13062,#981,.T.);
#16761=EDGE_CURVE('',#13065,#13066,#8468,.T.);
#16762=EDGE_CURVE('',#13065,#13063,#982,.T.);
#16763=EDGE_CURVE('',#13066,#13064,#983,.T.);
#16764=EDGE_CURVE('',#13067,#13068,#8469,.T.);
#16765=EDGE_CURVE('',#13067,#13065,#984,.T.);
#16766=EDGE_CURVE('',#13068,#13066,#985,.T.);
#16767=EDGE_CURVE('',#13069,#13070,#8470,.T.);
#16768=EDGE_CURVE('',#13069,#13067,#986,.T.);
#16769=EDGE_CURVE('',#13070,#13068,#987,.T.);
#16770=EDGE_CURVE('',#13071,#13072,#8471,.T.);
#16771=EDGE_CURVE('',#13071,#13069,#988,.T.);
#16772=EDGE_CURVE('',#13072,#13070,#989,.T.);
#16773=EDGE_CURVE('',#13073,#13074,#8472,.T.);
#16774=EDGE_CURVE('',#13073,#13071,#990,.T.);
#16775=EDGE_CURVE('',#13074,#13072,#991,.T.);
#16776=EDGE_CURVE('',#13037,#13034,#992,.T.);
#16777=EDGE_CURVE('',#13075,#13034,#6465,.T.);
#16778=EDGE_CURVE('',#13075,#13038,#993,.T.);
#16779=EDGE_CURVE('',#13033,#13075,#994,.T.);
#16780=EDGE_CURVE('',#13076,#12995,#995,.T.);
#16781=EDGE_CURVE('',#13076,#13074,#996,.T.);
#16782=EDGE_CURVE('',#12995,#13077,#6466,.T.);
#16783=EDGE_CURVE('',#13077,#12994,#6467,.T.);
#16784=EDGE_CURVE('',#12994,#13078,#997,.T.);
#16785=EDGE_CURVE('',#13078,#13076,#6468,.T.);
#16786=EDGE_CURVE('',#13078,#13073,#998,.T.);
#16787=EDGE_CURVE('',#13032,#13079,#6469,.T.);
#16788=EDGE_CURVE('',#13079,#13079,#6470,.T.);
#16789=EDGE_CURVE('',#13032,#13075,#6471,.T.);
#16790=EDGE_CURVE('',#13080,#13080,#6472,.T.);
#16791=EDGE_CURVE('',#13081,#13082,#8473,.T.);
#16792=EDGE_CURVE('',#13082,#13081,#6473,.T.);
#16793=EDGE_CURVE('',#13082,#13083,#8474,.T.);
#16794=EDGE_CURVE('',#13083,#13082,#6474,.T.);
#16795=EDGE_CURVE('',#13083,#13084,#8475,.T.);
#16796=EDGE_CURVE('',#13084,#13083,#6475,.T.);
#16797=EDGE_CURVE('',#13084,#13085,#8476,.T.);
#16798=EDGE_CURVE('',#13085,#13084,#6476,.T.);
#16799=EDGE_CURVE('',#13085,#13086,#8477,.T.);
#16800=EDGE_CURVE('',#13086,#13085,#6477,.T.);
#16801=EDGE_CURVE('',#13086,#13081,#8478,.T.);
#16802=EDGE_CURVE('',#13081,#13086,#6478,.T.);
#16803=EDGE_CURVE('',#13087,#13085,#8479,.T.);
#16804=EDGE_CURVE('',#13088,#13089,#8480,.T.);
#16805=EDGE_CURVE('',#13088,#13081,#8481,.T.);
#16806=EDGE_CURVE('',#13089,#13082,#8482,.T.);
#16807=EDGE_CURVE('',#13090,#13088,#8483,.T.);
#16808=EDGE_CURVE('',#13090,#13086,#8484,.T.);
#16809=EDGE_CURVE('',#13091,#13090,#8485,.T.);
#16810=EDGE_CURVE('',#13091,#13085,#8486,.T.);
#16811=EDGE_CURVE('',#13092,#13091,#8487,.T.);
#16812=EDGE_CURVE('',#13092,#13084,#8488,.T.);
#16813=EDGE_CURVE('',#13093,#13092,#8489,.T.);
#16814=EDGE_CURVE('',#13093,#13083,#8490,.T.);
#16815=EDGE_CURVE('',#13089,#13093,#8491,.T.);
#16816=EDGE_CURVE('',#13094,#13095,#8492,.T.);
#16817=EDGE_CURVE('',#13094,#13096,#8493,.T.);
#16818=EDGE_CURVE('',#13097,#13096,#8494,.T.);
#16819=EDGE_CURVE('',#13095,#13097,#8495,.T.);
#16820=EDGE_CURVE('',#13095,#13098,#6479,.T.);
#16821=EDGE_CURVE('',#13097,#13098,#8496,.T.);
#16822=EDGE_CURVE('',#13098,#13099,#8497,.T.);
#16823=EDGE_CURVE('',#13096,#13099,#8498,.T.);
#16824=EDGE_CURVE('',#13099,#13094,#6480,.T.);
#16825=EDGE_CURVE('',#13100,#13101,#8499,.T.);
#16826=EDGE_CURVE('',#13100,#13102,#8500,.T.);
#16827=EDGE_CURVE('',#13103,#13102,#8501,.T.);
#16828=EDGE_CURVE('',#13101,#13103,#8502,.T.);
#16829=EDGE_CURVE('',#13101,#13104,#6481,.T.);
#16830=EDGE_CURVE('',#13103,#13104,#8503,.T.);
#16831=EDGE_CURVE('',#13104,#13105,#8504,.T.);
#16832=EDGE_CURVE('',#13102,#13105,#8505,.T.);
#16833=EDGE_CURVE('',#13105,#13100,#6482,.T.);
#16834=EDGE_CURVE('',#13106,#13107,#8506,.T.);
#16835=EDGE_CURVE('',#13106,#13108,#8507,.T.);
#16836=EDGE_CURVE('',#13109,#13108,#8508,.T.);
#16837=EDGE_CURVE('',#13107,#13109,#8509,.T.);
#16838=EDGE_CURVE('',#13107,#13110,#6483,.T.);
#16839=EDGE_CURVE('',#13109,#13110,#8510,.T.);
#16840=EDGE_CURVE('',#13110,#13111,#8511,.T.);
#16841=EDGE_CURVE('',#13108,#13111,#8512,.T.);
#16842=EDGE_CURVE('',#13111,#13106,#6484,.T.);
#16843=EDGE_CURVE('',#13112,#13113,#8513,.T.);
#16844=EDGE_CURVE('',#13112,#13114,#8514,.T.);
#16845=EDGE_CURVE('',#13115,#13114,#8515,.T.);
#16846=EDGE_CURVE('',#13113,#13115,#8516,.T.);
#16847=EDGE_CURVE('',#13113,#13116,#6485,.T.);
#16848=EDGE_CURVE('',#13115,#13116,#8517,.T.);
#16849=EDGE_CURVE('',#13116,#13117,#8518,.T.);
#16850=EDGE_CURVE('',#13114,#13117,#8519,.T.);
#16851=EDGE_CURVE('',#13117,#13112,#6486,.T.);
#16852=EDGE_CURVE('',#13118,#13119,#8520,.T.);
#16853=EDGE_CURVE('',#13118,#13120,#8521,.T.);
#16854=EDGE_CURVE('',#13121,#13120,#8522,.T.);
#16855=EDGE_CURVE('',#13119,#13121,#8523,.T.);
#16856=EDGE_CURVE('',#13119,#13122,#6487,.T.);
#16857=EDGE_CURVE('',#13121,#13122,#8524,.T.);
#16858=EDGE_CURVE('',#13122,#13123,#8525,.T.);
#16859=EDGE_CURVE('',#13120,#13123,#8526,.T.);
#16860=EDGE_CURVE('',#13123,#13118,#6488,.T.);
#16861=EDGE_CURVE('',#13124,#13125,#8527,.T.);
#16862=EDGE_CURVE('',#13124,#13126,#8528,.T.);
#16863=EDGE_CURVE('',#13127,#13126,#8529,.T.);
#16864=EDGE_CURVE('',#13125,#13127,#8530,.T.);
#16865=EDGE_CURVE('',#13125,#13128,#6489,.T.);
#16866=EDGE_CURVE('',#13127,#13128,#8531,.T.);
#16867=EDGE_CURVE('',#13128,#13129,#8532,.T.);
#16868=EDGE_CURVE('',#13126,#13129,#8533,.T.);
#16869=EDGE_CURVE('',#13129,#13124,#6490,.T.);
#16870=EDGE_CURVE('',#13130,#13131,#8534,.T.);
#16871=EDGE_CURVE('',#13130,#13132,#8535,.T.);
#16872=EDGE_CURVE('',#13133,#13132,#8536,.T.);
#16873=EDGE_CURVE('',#13131,#13133,#8537,.T.);
#16874=EDGE_CURVE('',#13131,#13134,#6491,.T.);
#16875=EDGE_CURVE('',#13133,#13134,#8538,.T.);
#16876=EDGE_CURVE('',#13134,#13135,#8539,.T.);
#16877=EDGE_CURVE('',#13132,#13135,#8540,.T.);
#16878=EDGE_CURVE('',#13135,#13130,#6492,.T.);
#16879=EDGE_CURVE('',#13136,#13137,#8541,.T.);
#16880=EDGE_CURVE('',#13136,#13138,#8542,.T.);
#16881=EDGE_CURVE('',#13139,#13138,#8543,.T.);
#16882=EDGE_CURVE('',#13137,#13139,#8544,.T.);
#16883=EDGE_CURVE('',#13137,#13140,#6493,.T.);
#16884=EDGE_CURVE('',#13139,#13140,#8545,.T.);
#16885=EDGE_CURVE('',#13140,#13141,#8546,.T.);
#16886=EDGE_CURVE('',#13138,#13141,#8547,.T.);
#16887=EDGE_CURVE('',#13141,#13136,#6494,.T.);
#16888=EDGE_CURVE('',#13142,#13143,#8548,.T.);
#16889=EDGE_CURVE('',#13142,#13144,#8549,.T.);
#16890=EDGE_CURVE('',#13145,#13144,#8550,.T.);
#16891=EDGE_CURVE('',#13143,#13145,#8551,.T.);
#16892=EDGE_CURVE('',#13143,#13146,#6495,.T.);
#16893=EDGE_CURVE('',#13145,#13147,#8552,.T.);
#16894=EDGE_CURVE('',#13146,#13147,#6496,.T.);
#16895=EDGE_CURVE('',#13147,#13148,#8553,.T.);
#16896=EDGE_CURVE('',#13144,#13148,#8554,.T.);
#16897=EDGE_CURVE('',#13148,#13149,#6497,.T.);
#16898=EDGE_CURVE('',#13149,#13142,#6498,.T.);
#16899=EDGE_CURVE('',#13150,#13151,#8555,.T.);
#16900=EDGE_CURVE('',#13150,#13152,#8556,.T.);
#16901=EDGE_CURVE('',#13153,#13152,#8557,.T.);
#16902=EDGE_CURVE('',#13151,#13153,#8558,.T.);
#16903=EDGE_CURVE('',#13151,#13154,#6499,.T.);
#16904=EDGE_CURVE('',#13153,#13154,#8559,.T.);
#16905=EDGE_CURVE('',#13154,#13155,#8560,.T.);
#16906=EDGE_CURVE('',#13152,#13155,#8561,.T.);
#16907=EDGE_CURVE('',#13155,#13150,#6500,.T.);
#16908=EDGE_CURVE('',#13156,#13157,#8562,.T.);
#16909=EDGE_CURVE('',#13156,#13158,#8563,.T.);
#16910=EDGE_CURVE('',#13159,#13158,#8564,.T.);
#16911=EDGE_CURVE('',#13157,#13159,#8565,.T.);
#16912=EDGE_CURVE('',#13157,#13160,#6501,.T.);
#16913=EDGE_CURVE('',#13159,#13160,#8566,.T.);
#16914=EDGE_CURVE('',#13160,#13161,#8567,.T.);
#16915=EDGE_CURVE('',#13158,#13161,#8568,.T.);
#16916=EDGE_CURVE('',#13161,#13156,#6502,.T.);
#16917=EDGE_CURVE('',#13162,#13163,#8569,.T.);
#16918=EDGE_CURVE('',#13162,#13164,#8570,.T.);
#16919=EDGE_CURVE('',#13165,#13164,#8571,.T.);
#16920=EDGE_CURVE('',#13163,#13165,#8572,.T.);
#16921=EDGE_CURVE('',#13163,#13166,#6503,.T.);
#16922=EDGE_CURVE('',#13165,#13166,#8573,.T.);
#16923=EDGE_CURVE('',#13166,#13167,#8574,.T.);
#16924=EDGE_CURVE('',#13164,#13167,#8575,.T.);
#16925=EDGE_CURVE('',#13167,#13162,#6504,.T.);
#16926=EDGE_CURVE('',#13168,#13169,#8576,.T.);
#16927=EDGE_CURVE('',#13168,#13170,#8577,.T.);
#16928=EDGE_CURVE('',#13171,#13170,#8578,.T.);
#16929=EDGE_CURVE('',#13169,#13171,#8579,.T.);
#16930=EDGE_CURVE('',#13169,#13172,#6505,.T.);
#16931=EDGE_CURVE('',#13171,#13172,#8580,.T.);
#16932=EDGE_CURVE('',#13172,#13173,#8581,.T.);
#16933=EDGE_CURVE('',#13170,#13173,#8582,.T.);
#16934=EDGE_CURVE('',#13173,#13168,#6506,.T.);
#16935=EDGE_CURVE('',#13174,#13175,#8583,.T.);
#16936=EDGE_CURVE('',#13174,#13176,#8584,.T.);
#16937=EDGE_CURVE('',#13177,#13176,#8585,.T.);
#16938=EDGE_CURVE('',#13175,#13177,#8586,.T.);
#16939=EDGE_CURVE('',#13175,#13178,#6507,.T.);
#16940=EDGE_CURVE('',#13177,#13178,#8587,.T.);
#16941=EDGE_CURVE('',#13178,#13179,#8588,.T.);
#16942=EDGE_CURVE('',#13176,#13179,#8589,.T.);
#16943=EDGE_CURVE('',#13179,#13174,#6508,.T.);
#16944=EDGE_CURVE('',#13180,#13181,#8590,.T.);
#16945=EDGE_CURVE('',#13180,#13182,#8591,.T.);
#16946=EDGE_CURVE('',#13183,#13182,#8592,.T.);
#16947=EDGE_CURVE('',#13181,#13183,#8593,.T.);
#16948=EDGE_CURVE('',#13181,#13184,#6509,.T.);
#16949=EDGE_CURVE('',#13183,#13184,#8594,.T.);
#16950=EDGE_CURVE('',#13184,#13185,#8595,.T.);
#16951=EDGE_CURVE('',#13182,#13185,#8596,.T.);
#16952=EDGE_CURVE('',#13185,#13180,#6510,.T.);
#16953=EDGE_CURVE('',#13186,#13187,#8597,.T.);
#16954=EDGE_CURVE('',#13186,#13188,#8598,.T.);
#16955=EDGE_CURVE('',#13189,#13188,#8599,.T.);
#16956=EDGE_CURVE('',#13187,#13189,#8600,.T.);
#16957=EDGE_CURVE('',#13187,#13190,#6511,.T.);
#16958=EDGE_CURVE('',#13189,#13190,#8601,.T.);
#16959=EDGE_CURVE('',#13190,#13191,#8602,.T.);
#16960=EDGE_CURVE('',#13188,#13191,#8603,.T.);
#16961=EDGE_CURVE('',#13191,#13186,#6512,.T.);
#16962=EDGE_CURVE('',#13192,#13193,#8604,.T.);
#16963=EDGE_CURVE('',#13192,#13194,#8605,.T.);
#16964=EDGE_CURVE('',#13195,#13194,#8606,.T.);
#16965=EDGE_CURVE('',#13193,#13195,#8607,.T.);
#16966=EDGE_CURVE('',#13193,#13196,#6513,.T.);
#16967=EDGE_CURVE('',#13195,#13196,#8608,.T.);
#16968=EDGE_CURVE('',#13196,#13197,#8609,.T.);
#16969=EDGE_CURVE('',#13194,#13197,#8610,.T.);
#16970=EDGE_CURVE('',#13197,#13192,#6514,.T.);
#16971=EDGE_CURVE('',#13198,#13199,#8611,.T.);
#16972=EDGE_CURVE('',#13198,#13200,#8612,.T.);
#16973=EDGE_CURVE('',#13201,#13200,#8613,.T.);
#16974=EDGE_CURVE('',#13199,#13201,#8614,.T.);
#16975=EDGE_CURVE('',#13199,#13202,#6515,.T.);
#16976=EDGE_CURVE('',#13201,#13202,#8615,.T.);
#16977=EDGE_CURVE('',#13202,#13203,#8616,.T.);
#16978=EDGE_CURVE('',#13200,#13203,#8617,.T.);
#16979=EDGE_CURVE('',#13203,#13198,#6516,.T.);
#16980=EDGE_CURVE('',#13204,#13205,#8618,.T.);
#16981=EDGE_CURVE('',#13204,#13206,#8619,.T.);
#16982=EDGE_CURVE('',#13207,#13206,#8620,.T.);
#16983=EDGE_CURVE('',#13205,#13207,#8621,.T.);
#16984=EDGE_CURVE('',#13205,#13208,#6517,.T.);
#16985=EDGE_CURVE('',#13207,#13208,#8622,.T.);
#16986=EDGE_CURVE('',#13208,#13209,#8623,.T.);
#16987=EDGE_CURVE('',#13206,#13209,#8624,.T.);
#16988=EDGE_CURVE('',#13209,#13204,#6518,.T.);
#16989=EDGE_CURVE('',#13210,#13211,#8625,.T.);
#16990=EDGE_CURVE('',#13210,#13212,#8626,.T.);
#16991=EDGE_CURVE('',#13213,#13212,#8627,.T.);
#16992=EDGE_CURVE('',#13211,#13213,#8628,.T.);
#16993=EDGE_CURVE('',#13211,#13214,#6519,.T.);
#16994=EDGE_CURVE('',#13213,#13214,#8629,.T.);
#16995=EDGE_CURVE('',#13214,#13215,#8630,.T.);
#16996=EDGE_CURVE('',#13212,#13215,#8631,.T.);
#16997=EDGE_CURVE('',#13215,#13210,#6520,.T.);
#16998=EDGE_CURVE('',#13216,#13217,#8632,.T.);
#16999=EDGE_CURVE('',#13216,#13218,#8633,.T.);
#17000=EDGE_CURVE('',#13219,#13218,#8634,.T.);
#17001=EDGE_CURVE('',#13217,#13219,#8635,.T.);
#17002=EDGE_CURVE('',#13217,#13220,#6521,.T.);
#17003=EDGE_CURVE('',#13219,#13220,#8636,.T.);
#17004=EDGE_CURVE('',#13220,#13221,#8637,.T.);
#17005=EDGE_CURVE('',#13218,#13221,#8638,.T.);
#17006=EDGE_CURVE('',#13221,#13216,#6522,.T.);
#17007=EDGE_CURVE('',#13222,#13223,#8639,.T.);
#17008=EDGE_CURVE('',#13222,#13224,#8640,.T.);
#17009=EDGE_CURVE('',#13225,#13224,#8641,.T.);
#17010=EDGE_CURVE('',#13223,#13225,#8642,.T.);
#17011=EDGE_CURVE('',#13223,#13226,#6523,.T.);
#17012=EDGE_CURVE('',#13225,#13226,#8643,.T.);
#17013=EDGE_CURVE('',#13226,#13227,#8644,.T.);
#17014=EDGE_CURVE('',#13224,#13227,#8645,.T.);
#17015=EDGE_CURVE('',#13227,#13222,#6524,.T.);
#17016=EDGE_CURVE('',#13228,#13229,#8646,.T.);
#17017=EDGE_CURVE('',#13228,#13230,#8647,.T.);
#17018=EDGE_CURVE('',#13231,#13230,#8648,.T.);
#17019=EDGE_CURVE('',#13229,#13231,#8649,.T.);
#17020=EDGE_CURVE('',#13229,#13232,#6525,.T.);
#17021=EDGE_CURVE('',#13231,#13232,#8650,.T.);
#17022=EDGE_CURVE('',#13232,#13233,#8651,.T.);
#17023=EDGE_CURVE('',#13230,#13233,#8652,.T.);
#17024=EDGE_CURVE('',#13233,#13228,#6526,.T.);
#17025=EDGE_CURVE('',#13234,#13235,#8653,.T.);
#17026=EDGE_CURVE('',#13234,#13236,#8654,.T.);
#17027=EDGE_CURVE('',#13237,#13236,#8655,.T.);
#17028=EDGE_CURVE('',#13235,#13237,#8656,.T.);
#17029=EDGE_CURVE('',#13235,#13238,#6527,.T.);
#17030=EDGE_CURVE('',#13237,#13238,#8657,.T.);
#17031=EDGE_CURVE('',#13238,#13239,#8658,.T.);
#17032=EDGE_CURVE('',#13236,#13239,#8659,.T.);
#17033=EDGE_CURVE('',#13239,#13234,#6528,.T.);
#17034=EDGE_CURVE('',#13240,#13241,#8660,.T.);
#17035=EDGE_CURVE('',#13240,#13242,#8661,.T.);
#17036=EDGE_CURVE('',#13243,#13242,#8662,.T.);
#17037=EDGE_CURVE('',#13241,#13243,#8663,.T.);
#17038=EDGE_CURVE('',#13241,#13244,#6529,.T.);
#17039=EDGE_CURVE('',#13243,#13244,#8664,.T.);
#17040=EDGE_CURVE('',#13244,#13245,#8665,.T.);
#17041=EDGE_CURVE('',#13242,#13245,#8666,.T.);
#17042=EDGE_CURVE('',#13245,#13240,#6530,.T.);
#17043=EDGE_CURVE('',#13246,#13247,#8667,.T.);
#17044=EDGE_CURVE('',#13246,#13248,#8668,.T.);
#17045=EDGE_CURVE('',#13249,#13248,#8669,.T.);
#17046=EDGE_CURVE('',#13247,#13249,#8670,.T.);
#17047=EDGE_CURVE('',#13247,#13250,#6531,.T.);
#17048=EDGE_CURVE('',#13249,#13250,#8671,.T.);
#17049=EDGE_CURVE('',#13250,#13251,#8672,.T.);
#17050=EDGE_CURVE('',#13248,#13251,#8673,.T.);
#17051=EDGE_CURVE('',#13251,#13246,#6532,.T.);
#17052=EDGE_CURVE('',#13252,#13253,#6533,.T.);
#17053=EDGE_CURVE('',#13252,#13254,#8674,.T.);
#17054=EDGE_CURVE('',#13254,#13253,#8675,.T.);
#17055=EDGE_CURVE('',#13255,#13252,#8676,.T.);
#17056=EDGE_CURVE('',#13255,#13256,#8677,.T.);
#17057=EDGE_CURVE('',#13254,#13256,#8678,.T.);
#17058=EDGE_CURVE('',#13253,#13257,#8679,.T.);
#17059=EDGE_CURVE('',#13256,#13257,#8680,.T.);
#17060=EDGE_CURVE('',#13257,#13255,#6534,.T.);
#17061=EDGE_CURVE('',#13258,#13259,#8681,.T.);
#17062=EDGE_CURVE('',#13258,#13260,#8682,.T.);
#17063=EDGE_CURVE('',#13261,#13260,#8683,.T.);
#17064=EDGE_CURVE('',#13259,#13261,#8684,.T.);
#17065=EDGE_CURVE('',#13259,#13262,#6535,.T.);
#17066=EDGE_CURVE('',#13261,#13262,#8685,.T.);
#17067=EDGE_CURVE('',#13262,#13263,#8686,.T.);
#17068=EDGE_CURVE('',#13260,#13263,#8687,.T.);
#17069=EDGE_CURVE('',#13263,#13258,#6536,.T.);
#17070=EDGE_CURVE('',#13264,#13265,#8688,.T.);
#17071=EDGE_CURVE('',#13264,#13266,#8689,.T.);
#17072=EDGE_CURVE('',#13267,#13266,#8690,.T.);
#17073=EDGE_CURVE('',#13265,#13267,#8691,.T.);
#17074=EDGE_CURVE('',#13265,#13268,#6537,.T.);
#17075=EDGE_CURVE('',#13267,#13268,#8692,.T.);
#17076=EDGE_CURVE('',#13268,#13269,#8693,.T.);
#17077=EDGE_CURVE('',#13266,#13269,#8694,.T.);
#17078=EDGE_CURVE('',#13269,#13264,#6538,.T.);
#17079=EDGE_CURVE('',#13270,#13271,#8695,.T.);
#17080=EDGE_CURVE('',#13270,#13272,#8696,.T.);
#17081=EDGE_CURVE('',#13273,#13272,#8697,.T.);
#17082=EDGE_CURVE('',#13271,#13273,#8698,.T.);
#17083=EDGE_CURVE('',#13271,#13274,#6539,.T.);
#17084=EDGE_CURVE('',#13273,#13274,#8699,.T.);
#17085=EDGE_CURVE('',#13274,#13275,#8700,.T.);
#17086=EDGE_CURVE('',#13272,#13275,#8701,.T.);
#17087=EDGE_CURVE('',#13275,#13270,#6540,.T.);
#17088=EDGE_CURVE('',#13276,#13277,#8702,.T.);
#17089=EDGE_CURVE('',#13276,#13278,#8703,.T.);
#17090=EDGE_CURVE('',#13279,#13278,#8704,.T.);
#17091=EDGE_CURVE('',#13277,#13279,#8705,.T.);
#17092=EDGE_CURVE('',#13277,#13280,#6541,.T.);
#17093=EDGE_CURVE('',#13279,#13280,#8706,.T.);
#17094=EDGE_CURVE('',#13280,#13281,#8707,.T.);
#17095=EDGE_CURVE('',#13278,#13281,#8708,.T.);
#17096=EDGE_CURVE('',#13281,#13276,#6542,.T.);
#17097=EDGE_CURVE('',#13282,#13283,#8709,.T.);
#17098=EDGE_CURVE('',#13282,#13284,#8710,.T.);
#17099=EDGE_CURVE('',#13285,#13284,#8711,.T.);
#17100=EDGE_CURVE('',#13283,#13285,#8712,.T.);
#17101=EDGE_CURVE('',#13283,#13286,#6543,.T.);
#17102=EDGE_CURVE('',#13285,#13286,#8713,.T.);
#17103=EDGE_CURVE('',#13286,#13287,#8714,.T.);
#17104=EDGE_CURVE('',#13284,#13287,#8715,.T.);
#17105=EDGE_CURVE('',#13287,#13282,#6544,.T.);
#17106=EDGE_CURVE('',#13288,#13289,#8716,.T.);
#17107=EDGE_CURVE('',#13288,#13290,#8717,.T.);
#17108=EDGE_CURVE('',#13291,#13290,#8718,.T.);
#17109=EDGE_CURVE('',#13289,#13291,#8719,.T.);
#17110=EDGE_CURVE('',#13289,#13292,#6545,.T.);
#17111=EDGE_CURVE('',#13291,#13292,#8720,.T.);
#17112=EDGE_CURVE('',#13292,#13293,#8721,.T.);
#17113=EDGE_CURVE('',#13290,#13293,#8722,.T.);
#17114=EDGE_CURVE('',#13293,#13288,#6546,.T.);
#17115=EDGE_CURVE('',#13294,#13295,#8723,.T.);
#17116=EDGE_CURVE('',#13294,#13296,#8724,.T.);
#17117=EDGE_CURVE('',#13297,#13296,#8725,.T.);
#17118=EDGE_CURVE('',#13295,#13297,#8726,.T.);
#17119=EDGE_CURVE('',#13295,#13298,#6547,.T.);
#17120=EDGE_CURVE('',#13297,#13298,#8727,.T.);
#17121=EDGE_CURVE('',#13298,#13299,#8728,.T.);
#17122=EDGE_CURVE('',#13296,#13299,#8729,.T.);
#17123=EDGE_CURVE('',#13299,#13294,#6548,.T.);
#17124=EDGE_CURVE('',#13300,#13301,#8730,.T.);
#17125=EDGE_CURVE('',#13300,#13302,#8731,.T.);
#17126=EDGE_CURVE('',#13303,#13302,#8732,.T.);
#17127=EDGE_CURVE('',#13301,#13303,#8733,.T.);
#17128=EDGE_CURVE('',#13301,#13304,#6549,.T.);
#17129=EDGE_CURVE('',#13303,#13304,#8734,.T.);
#17130=EDGE_CURVE('',#13304,#13305,#8735,.T.);
#17131=EDGE_CURVE('',#13302,#13305,#8736,.T.);
#17132=EDGE_CURVE('',#13305,#13300,#6550,.T.);
#17133=EDGE_CURVE('',#13306,#13307,#8737,.T.);
#17134=EDGE_CURVE('',#13306,#13308,#8738,.T.);
#17135=EDGE_CURVE('',#13309,#13308,#8739,.T.);
#17136=EDGE_CURVE('',#13307,#13309,#8740,.T.);
#17137=EDGE_CURVE('',#13307,#13310,#6551,.T.);
#17138=EDGE_CURVE('',#13309,#13310,#8741,.T.);
#17139=EDGE_CURVE('',#13310,#13311,#8742,.T.);
#17140=EDGE_CURVE('',#13308,#13311,#8743,.T.);
#17141=EDGE_CURVE('',#13311,#13306,#6552,.T.);
#17142=EDGE_CURVE('',#13312,#13312,#6553,.T.);
#17143=EDGE_CURVE('',#13077,#13312,#8744,.T.);
#17144=EDGE_CURVE('',#13313,#13313,#6554,.T.);
#17145=EDGE_CURVE('',#13313,#13080,#8745,.T.);
#17146=EDGE_CURVE('',#13304,#13095,#6555,.T.);
#17147=EDGE_CURVE('',#13104,#13301,#6556,.T.);
#17148=EDGE_CURVE('',#13298,#13101,#6557,.T.);
#17149=EDGE_CURVE('',#13110,#13295,#6558,.T.);
#17150=EDGE_CURVE('',#13292,#13107,#6559,.T.);
#17151=EDGE_CURVE('',#13116,#13289,#6560,.T.);
#17152=EDGE_CURVE('',#13286,#13113,#6561,.T.);
#17153=EDGE_CURVE('',#13122,#13283,#6562,.T.);
#17154=EDGE_CURVE('',#13280,#13119,#6563,.T.);
#17155=EDGE_CURVE('',#13128,#13277,#6564,.T.);
#17156=EDGE_CURVE('',#13274,#13125,#6565,.T.);
#17157=EDGE_CURVE('',#13134,#13271,#6566,.T.);
#17158=EDGE_CURVE('',#13268,#13131,#6567,.T.);
#17159=EDGE_CURVE('',#13140,#13265,#6568,.T.);
#17160=EDGE_CURVE('',#13262,#13137,#6569,.T.);
#17161=EDGE_CURVE('',#13147,#13259,#6570,.T.);
#17162=EDGE_CURVE('',#13149,#13313,#8746,.T.);
#17163=EDGE_CURVE('',#13154,#13143,#6571,.T.);
#17164=EDGE_CURVE('',#13250,#13151,#6572,.T.);
#17165=EDGE_CURVE('',#13160,#13247,#6573,.T.);
#17166=EDGE_CURVE('',#13244,#13157,#6574,.T.);
#17167=EDGE_CURVE('',#13166,#13241,#6575,.T.);
#17168=EDGE_CURVE('',#13238,#13163,#6576,.T.);
#17169=EDGE_CURVE('',#13172,#13235,#6577,.T.);
#17170=EDGE_CURVE('',#13232,#13169,#6578,.T.);
#17171=EDGE_CURVE('',#13178,#13229,#6579,.T.);
#17172=EDGE_CURVE('',#13226,#13175,#6580,.T.);
#17173=EDGE_CURVE('',#13184,#13223,#6581,.T.);
#17174=EDGE_CURVE('',#13220,#13181,#6582,.T.);
#17175=EDGE_CURVE('',#13190,#13217,#6583,.T.);
#17176=EDGE_CURVE('',#13214,#13187,#6584,.T.);
#17177=EDGE_CURVE('',#13196,#13211,#6585,.T.);
#17178=EDGE_CURVE('',#13208,#13193,#6586,.T.);
#17179=EDGE_CURVE('',#13202,#13205,#6587,.T.);
#17180=EDGE_CURVE('',#13253,#13199,#6588,.T.);
#17181=EDGE_CURVE('',#13310,#13252,#6589,.T.);
#17182=EDGE_CURVE('',#13098,#13307,#6590,.T.);
#17183=EDGE_CURVE('',#13314,#13314,#6591,.T.);
#17184=EDGE_CURVE('',#13314,#13146,#8747,.T.);
#23867=ORIENTED_EDGE('',*,*,#16656,.F.);
#23868=ORIENTED_EDGE('',*,*,#16657,.T.);
#23869=ORIENTED_EDGE('',*,*,#16658,.T.);
#23870=ORIENTED_EDGE('',*,*,#16659,.T.);
#23871=ORIENTED_EDGE('',*,*,#16660,.F.);
#23872=ORIENTED_EDGE('',*,*,#16661,.T.);
#23873=ORIENTED_EDGE('',*,*,#16656,.T.);
#23874=ORIENTED_EDGE('',*,*,#16662,.T.);
#23875=ORIENTED_EDGE('',*,*,#16663,.F.);
#23876=ORIENTED_EDGE('',*,*,#16664,.T.);
#23877=ORIENTED_EDGE('',*,*,#16660,.T.);
#23878=ORIENTED_EDGE('',*,*,#16665,.T.);
#23879=ORIENTED_EDGE('',*,*,#16666,.F.);
#23880=ORIENTED_EDGE('',*,*,#16667,.T.);
#23881=ORIENTED_EDGE('',*,*,#16663,.T.);
#23882=ORIENTED_EDGE('',*,*,#16668,.T.);
#23883=ORIENTED_EDGE('',*,*,#16669,.F.);
#23884=ORIENTED_EDGE('',*,*,#16670,.T.);
#23885=ORIENTED_EDGE('',*,*,#16666,.T.);
#23886=ORIENTED_EDGE('',*,*,#16671,.T.);
#23887=ORIENTED_EDGE('',*,*,#16672,.F.);
#23888=ORIENTED_EDGE('',*,*,#16673,.T.);
#23889=ORIENTED_EDGE('',*,*,#16669,.T.);
#23890=ORIENTED_EDGE('',*,*,#16674,.T.);
#23891=ORIENTED_EDGE('',*,*,#16675,.F.);
#23892=ORIENTED_EDGE('',*,*,#16676,.T.);
#23893=ORIENTED_EDGE('',*,*,#16672,.T.);
#23894=ORIENTED_EDGE('',*,*,#16677,.T.);
#23895=ORIENTED_EDGE('',*,*,#16678,.F.);
#23896=ORIENTED_EDGE('',*,*,#16679,.T.);
#23897=ORIENTED_EDGE('',*,*,#16675,.T.);
#23898=ORIENTED_EDGE('',*,*,#16680,.T.);
#23899=ORIENTED_EDGE('',*,*,#16681,.F.);
#23900=ORIENTED_EDGE('',*,*,#16682,.T.);
#23901=ORIENTED_EDGE('',*,*,#16678,.T.);
#23902=ORIENTED_EDGE('',*,*,#16683,.T.);
#23903=ORIENTED_EDGE('',*,*,#16684,.F.);
#23904=ORIENTED_EDGE('',*,*,#16685,.T.);
#23905=ORIENTED_EDGE('',*,*,#16681,.T.);
#23906=ORIENTED_EDGE('',*,*,#16686,.T.);
#23907=ORIENTED_EDGE('',*,*,#16687,.F.);
#23908=ORIENTED_EDGE('',*,*,#16688,.T.);
#23909=ORIENTED_EDGE('',*,*,#16684,.T.);
#23910=ORIENTED_EDGE('',*,*,#16689,.T.);
#23911=ORIENTED_EDGE('',*,*,#16690,.F.);
#23912=ORIENTED_EDGE('',*,*,#16691,.T.);
#23913=ORIENTED_EDGE('',*,*,#16687,.T.);
#23914=ORIENTED_EDGE('',*,*,#16692,.T.);
#23915=ORIENTED_EDGE('',*,*,#16693,.F.);
#23916=ORIENTED_EDGE('',*,*,#16694,.T.);
#23917=ORIENTED_EDGE('',*,*,#16690,.T.);
#23918=ORIENTED_EDGE('',*,*,#16695,.T.);
#23919=ORIENTED_EDGE('',*,*,#16696,.F.);
#23920=ORIENTED_EDGE('',*,*,#16697,.T.);
#23921=ORIENTED_EDGE('',*,*,#16693,.T.);
#23922=ORIENTED_EDGE('',*,*,#16698,.T.);
#23923=ORIENTED_EDGE('',*,*,#16699,.F.);
#23924=ORIENTED_EDGE('',*,*,#16700,.T.);
#23925=ORIENTED_EDGE('',*,*,#16696,.T.);
#23926=ORIENTED_EDGE('',*,*,#16701,.T.);
#23927=ORIENTED_EDGE('',*,*,#16702,.F.);
#23928=ORIENTED_EDGE('',*,*,#16703,.T.);
#23929=ORIENTED_EDGE('',*,*,#16699,.T.);
#23930=ORIENTED_EDGE('',*,*,#16704,.T.);
#23931=ORIENTED_EDGE('',*,*,#16705,.F.);
#23932=ORIENTED_EDGE('',*,*,#16706,.T.);
#23933=ORIENTED_EDGE('',*,*,#16702,.T.);
#23934=ORIENTED_EDGE('',*,*,#16707,.T.);
#23935=ORIENTED_EDGE('',*,*,#16708,.F.);
#23936=ORIENTED_EDGE('',*,*,#16709,.T.);
#23937=ORIENTED_EDGE('',*,*,#16705,.T.);
#23938=ORIENTED_EDGE('',*,*,#16710,.T.);
#23939=ORIENTED_EDGE('',*,*,#16711,.F.);
#23940=ORIENTED_EDGE('',*,*,#16712,.T.);
#23941=ORIENTED_EDGE('',*,*,#16708,.T.);
#23942=ORIENTED_EDGE('',*,*,#16713,.T.);
#23943=ORIENTED_EDGE('',*,*,#16714,.F.);
#23944=ORIENTED_EDGE('',*,*,#16715,.F.);
#23945=ORIENTED_EDGE('',*,*,#16716,.T.);
#23946=ORIENTED_EDGE('',*,*,#16711,.T.);
#23947=ORIENTED_EDGE('',*,*,#16717,.T.);
#23948=ORIENTED_EDGE('',*,*,#16718,.F.);
#23949=ORIENTED_EDGE('',*,*,#16719,.T.);
#23950=ORIENTED_EDGE('',*,*,#16720,.F.);
#23951=ORIENTED_EDGE('',*,*,#16721,.F.);
#23952=ORIENTED_EDGE('',*,*,#16722,.F.);
#23953=ORIENTED_EDGE('',*,*,#16723,.T.);
#23954=ORIENTED_EDGE('',*,*,#16718,.T.);
#23955=ORIENTED_EDGE('',*,*,#16724,.F.);
#23956=ORIENTED_EDGE('',*,*,#16725,.F.);
#23957=ORIENTED_EDGE('',*,*,#16726,.T.);
#23958=ORIENTED_EDGE('',*,*,#16722,.T.);
#23959=ORIENTED_EDGE('',*,*,#16727,.F.);
#23960=ORIENTED_EDGE('',*,*,#16728,.F.);
#23961=ORIENTED_EDGE('',*,*,#16729,.T.);
#23962=ORIENTED_EDGE('',*,*,#16725,.T.);
#23963=ORIENTED_EDGE('',*,*,#16730,.F.);
#23964=ORIENTED_EDGE('',*,*,#16731,.F.);
#23965=ORIENTED_EDGE('',*,*,#16732,.T.);
#23966=ORIENTED_EDGE('',*,*,#16728,.T.);
#23967=ORIENTED_EDGE('',*,*,#16733,.F.);
#23968=ORIENTED_EDGE('',*,*,#16734,.F.);
#23969=ORIENTED_EDGE('',*,*,#16735,.T.);
#23970=ORIENTED_EDGE('',*,*,#16731,.T.);
#23971=ORIENTED_EDGE('',*,*,#16736,.F.);
#23972=ORIENTED_EDGE('',*,*,#16737,.F.);
#23973=ORIENTED_EDGE('',*,*,#16738,.T.);
#23974=ORIENTED_EDGE('',*,*,#16734,.T.);
#23975=ORIENTED_EDGE('',*,*,#16739,.F.);
#23976=ORIENTED_EDGE('',*,*,#16740,.F.);
#23977=ORIENTED_EDGE('',*,*,#16741,.T.);
#23978=ORIENTED_EDGE('',*,*,#16737,.T.);
#23979=ORIENTED_EDGE('',*,*,#16742,.F.);
#23980=ORIENTED_EDGE('',*,*,#16743,.F.);
#23981=ORIENTED_EDGE('',*,*,#16744,.T.);
#23982=ORIENTED_EDGE('',*,*,#16740,.T.);
#23983=ORIENTED_EDGE('',*,*,#16745,.F.);
#23984=ORIENTED_EDGE('',*,*,#16746,.F.);
#23985=ORIENTED_EDGE('',*,*,#16747,.T.);
#23986=ORIENTED_EDGE('',*,*,#16743,.T.);
#23987=ORIENTED_EDGE('',*,*,#16748,.F.);
#23988=ORIENTED_EDGE('',*,*,#16749,.F.);
#23989=ORIENTED_EDGE('',*,*,#16750,.T.);
#23990=ORIENTED_EDGE('',*,*,#16746,.T.);
#23991=ORIENTED_EDGE('',*,*,#16751,.F.);
#23992=ORIENTED_EDGE('',*,*,#16752,.F.);
#23993=ORIENTED_EDGE('',*,*,#16753,.T.);
#23994=ORIENTED_EDGE('',*,*,#16749,.T.);
#23995=ORIENTED_EDGE('',*,*,#16754,.F.);
#23996=ORIENTED_EDGE('',*,*,#16755,.F.);
#23997=ORIENTED_EDGE('',*,*,#16756,.T.);
#23998=ORIENTED_EDGE('',*,*,#16752,.T.);
#23999=ORIENTED_EDGE('',*,*,#16757,.F.);
#24000=ORIENTED_EDGE('',*,*,#16758,.F.);
#24001=ORIENTED_EDGE('',*,*,#16759,.T.);
#24002=ORIENTED_EDGE('',*,*,#16755,.T.);
#24003=ORIENTED_EDGE('',*,*,#16760,.F.);
#24004=ORIENTED_EDGE('',*,*,#16761,.F.);
#24005=ORIENTED_EDGE('',*,*,#16762,.T.);
#24006=ORIENTED_EDGE('',*,*,#16758,.T.);
#24007=ORIENTED_EDGE('',*,*,#16763,.F.);
#24008=ORIENTED_EDGE('',*,*,#16764,.F.);
#24009=ORIENTED_EDGE('',*,*,#16765,.T.);
#24010=ORIENTED_EDGE('',*,*,#16761,.T.);
#24011=ORIENTED_EDGE('',*,*,#16766,.F.);
#24012=ORIENTED_EDGE('',*,*,#16767,.F.);
#24013=ORIENTED_EDGE('',*,*,#16768,.T.);
#24014=ORIENTED_EDGE('',*,*,#16764,.T.);
#24015=ORIENTED_EDGE('',*,*,#16769,.F.);
#24016=ORIENTED_EDGE('',*,*,#16770,.F.);
#24017=ORIENTED_EDGE('',*,*,#16771,.T.);
#24018=ORIENTED_EDGE('',*,*,#16767,.T.);
#24019=ORIENTED_EDGE('',*,*,#16772,.F.);
#24020=ORIENTED_EDGE('',*,*,#16773,.F.);
#24021=ORIENTED_EDGE('',*,*,#16774,.T.);
#24022=ORIENTED_EDGE('',*,*,#16770,.T.);
#24023=ORIENTED_EDGE('',*,*,#16775,.F.);
#24024=ORIENTED_EDGE('',*,*,#16720,.T.);
#24025=ORIENTED_EDGE('',*,*,#16776,.T.);
#24026=ORIENTED_EDGE('',*,*,#16777,.F.);
#24027=ORIENTED_EDGE('',*,*,#16778,.T.);
#24028=ORIENTED_EDGE('',*,*,#16778,.F.);
#24029=ORIENTED_EDGE('',*,*,#16779,.F.);
#24030=ORIENTED_EDGE('',*,*,#16717,.F.);
#24031=ORIENTED_EDGE('',*,*,#16713,.F.);
#24032=ORIENTED_EDGE('',*,*,#16710,.F.);
#24033=ORIENTED_EDGE('',*,*,#16707,.F.);
#24034=ORIENTED_EDGE('',*,*,#16704,.F.);
#24035=ORIENTED_EDGE('',*,*,#16701,.F.);
#24036=ORIENTED_EDGE('',*,*,#16698,.F.);
#24037=ORIENTED_EDGE('',*,*,#16695,.F.);
#24038=ORIENTED_EDGE('',*,*,#16692,.F.);
#24039=ORIENTED_EDGE('',*,*,#16689,.F.);
#24040=ORIENTED_EDGE('',*,*,#16686,.F.);
#24041=ORIENTED_EDGE('',*,*,#16683,.F.);
#24042=ORIENTED_EDGE('',*,*,#16680,.F.);
#24043=ORIENTED_EDGE('',*,*,#16677,.F.);
#24044=ORIENTED_EDGE('',*,*,#16674,.F.);
#24045=ORIENTED_EDGE('',*,*,#16671,.F.);
#24046=ORIENTED_EDGE('',*,*,#16668,.F.);
#24047=ORIENTED_EDGE('',*,*,#16665,.F.);
#24048=ORIENTED_EDGE('',*,*,#16662,.F.);
#24049=ORIENTED_EDGE('',*,*,#16659,.F.);
#24050=ORIENTED_EDGE('',*,*,#16780,.F.);
#24051=ORIENTED_EDGE('',*,*,#16781,.T.);
#24052=ORIENTED_EDGE('',*,*,#16775,.T.);
#24053=ORIENTED_EDGE('',*,*,#16772,.T.);
#24054=ORIENTED_EDGE('',*,*,#16769,.T.);
#24055=ORIENTED_EDGE('',*,*,#16766,.T.);
#24056=ORIENTED_EDGE('',*,*,#16763,.T.);
#24057=ORIENTED_EDGE('',*,*,#16760,.T.);
#24058=ORIENTED_EDGE('',*,*,#16757,.T.);
#24059=ORIENTED_EDGE('',*,*,#16754,.T.);
#24060=ORIENTED_EDGE('',*,*,#16751,.T.);
#24061=ORIENTED_EDGE('',*,*,#16748,.T.);
#24062=ORIENTED_EDGE('',*,*,#16745,.T.);
#24063=ORIENTED_EDGE('',*,*,#16742,.T.);
#24064=ORIENTED_EDGE('',*,*,#16739,.T.);
#24065=ORIENTED_EDGE('',*,*,#16736,.T.);
#24066=ORIENTED_EDGE('',*,*,#16733,.T.);
#24067=ORIENTED_EDGE('',*,*,#16730,.T.);
#24068=ORIENTED_EDGE('',*,*,#16727,.T.);
#24069=ORIENTED_EDGE('',*,*,#16724,.T.);
#24070=ORIENTED_EDGE('',*,*,#16721,.T.);
#24071=ORIENTED_EDGE('',*,*,#16782,.T.);
#24072=ORIENTED_EDGE('',*,*,#16783,.T.);
#24073=ORIENTED_EDGE('',*,*,#16784,.T.);
#24074=ORIENTED_EDGE('',*,*,#16785,.T.);
#24075=ORIENTED_EDGE('',*,*,#16780,.T.);
#24076=ORIENTED_EDGE('',*,*,#16773,.T.);
#24077=ORIENTED_EDGE('',*,*,#16781,.F.);
#24078=ORIENTED_EDGE('',*,*,#16785,.F.);
#24079=ORIENTED_EDGE('',*,*,#16786,.T.);
#24080=ORIENTED_EDGE('',*,*,#16776,.F.);
#24081=ORIENTED_EDGE('',*,*,#16719,.F.);
#24082=ORIENTED_EDGE('',*,*,#16723,.F.);
#24083=ORIENTED_EDGE('',*,*,#16726,.F.);
#24084=ORIENTED_EDGE('',*,*,#16729,.F.);
#24085=ORIENTED_EDGE('',*,*,#16732,.F.);
#24086=ORIENTED_EDGE('',*,*,#16735,.F.);
#24087=ORIENTED_EDGE('',*,*,#16738,.F.);
#24088=ORIENTED_EDGE('',*,*,#16741,.F.);
#24089=ORIENTED_EDGE('',*,*,#16744,.F.);
#24090=ORIENTED_EDGE('',*,*,#16747,.F.);
#24091=ORIENTED_EDGE('',*,*,#16750,.F.);
#24092=ORIENTED_EDGE('',*,*,#16753,.F.);
#24093=ORIENTED_EDGE('',*,*,#16756,.F.);
#24094=ORIENTED_EDGE('',*,*,#16759,.F.);
#24095=ORIENTED_EDGE('',*,*,#16762,.F.);
#24096=ORIENTED_EDGE('',*,*,#16765,.F.);
#24097=ORIENTED_EDGE('',*,*,#16768,.F.);
#24098=ORIENTED_EDGE('',*,*,#16771,.F.);
#24099=ORIENTED_EDGE('',*,*,#16774,.F.);
#24100=ORIENTED_EDGE('',*,*,#16786,.F.);
#24101=ORIENTED_EDGE('',*,*,#16784,.F.);
#24102=ORIENTED_EDGE('',*,*,#16657,.F.);
#24103=ORIENTED_EDGE('',*,*,#16661,.F.);
#24104=ORIENTED_EDGE('',*,*,#16664,.F.);
#24105=ORIENTED_EDGE('',*,*,#16667,.F.);
#24106=ORIENTED_EDGE('',*,*,#16670,.F.);
#24107=ORIENTED_EDGE('',*,*,#16673,.F.);
#24108=ORIENTED_EDGE('',*,*,#16676,.F.);
#24109=ORIENTED_EDGE('',*,*,#16679,.F.);
#24110=ORIENTED_EDGE('',*,*,#16682,.F.);
#24111=ORIENTED_EDGE('',*,*,#16685,.F.);
#24112=ORIENTED_EDGE('',*,*,#16688,.F.);
#24113=ORIENTED_EDGE('',*,*,#16691,.F.);
#24114=ORIENTED_EDGE('',*,*,#16694,.F.);
#24115=ORIENTED_EDGE('',*,*,#16697,.F.);
#24116=ORIENTED_EDGE('',*,*,#16700,.F.);
#24117=ORIENTED_EDGE('',*,*,#16703,.F.);
#24118=ORIENTED_EDGE('',*,*,#16706,.F.);
#24119=ORIENTED_EDGE('',*,*,#16709,.F.);
#24120=ORIENTED_EDGE('',*,*,#16712,.F.);
#24121=ORIENTED_EDGE('',*,*,#16716,.F.);
#24122=ORIENTED_EDGE('',*,*,#16715,.T.);
#24123=ORIENTED_EDGE('',*,*,#16787,.T.);
#24124=ORIENTED_EDGE('',*,*,#16788,.T.);
#24125=ORIENTED_EDGE('',*,*,#16787,.F.);
#24126=ORIENTED_EDGE('',*,*,#16789,.T.);
#24127=ORIENTED_EDGE('',*,*,#16777,.T.);
#24128=ORIENTED_EDGE('',*,*,#16714,.T.);
#24129=ORIENTED_EDGE('',*,*,#16779,.T.);
#24130=ORIENTED_EDGE('',*,*,#16789,.F.);
#24131=ORIENTED_EDGE('',*,*,#16790,.F.);
#24132=ORIENTED_EDGE('',*,*,#16788,.F.);
#24133=ORIENTED_EDGE('',*,*,#16791,.F.);
#24134=ORIENTED_EDGE('',*,*,#16792,.F.);
#24135=ORIENTED_EDGE('',*,*,#16793,.F.);
#24136=ORIENTED_EDGE('',*,*,#16794,.F.);
#24137=ORIENTED_EDGE('',*,*,#16795,.F.);
#24138=ORIENTED_EDGE('',*,*,#16796,.F.);
#24139=ORIENTED_EDGE('',*,*,#16797,.F.);
#24140=ORIENTED_EDGE('',*,*,#16798,.F.);
#24141=ORIENTED_EDGE('',*,*,#16799,.F.);
#24142=ORIENTED_EDGE('',*,*,#16800,.F.);
#24143=ORIENTED_EDGE('',*,*,#16801,.F.);
#24144=ORIENTED_EDGE('',*,*,#16802,.F.);
#24145=ORIENTED_EDGE('',*,*,#16803,.T.);
#24146=ORIENTED_EDGE('',*,*,#16798,.T.);
#24147=ORIENTED_EDGE('',*,*,#16796,.T.);
#24148=ORIENTED_EDGE('',*,*,#16794,.T.);
#24149=ORIENTED_EDGE('',*,*,#16792,.T.);
#24150=ORIENTED_EDGE('',*,*,#16802,.T.);
#24151=ORIENTED_EDGE('',*,*,#16800,.T.);
#24152=ORIENTED_EDGE('',*,*,#16803,.F.);
#24153=ORIENTED_EDGE('',*,*,#16804,.F.);
#24154=ORIENTED_EDGE('',*,*,#16805,.T.);
#24155=ORIENTED_EDGE('',*,*,#16791,.T.);
#24156=ORIENTED_EDGE('',*,*,#16806,.F.);
#24157=ORIENTED_EDGE('',*,*,#16807,.F.);
#24158=ORIENTED_EDGE('',*,*,#16808,.T.);
#24159=ORIENTED_EDGE('',*,*,#16801,.T.);
#24160=ORIENTED_EDGE('',*,*,#16805,.F.);
#24161=ORIENTED_EDGE('',*,*,#16809,.F.);
#24162=ORIENTED_EDGE('',*,*,#16810,.T.);
#24163=ORIENTED_EDGE('',*,*,#16799,.T.);
#24164=ORIENTED_EDGE('',*,*,#16808,.F.);
#24165=ORIENTED_EDGE('',*,*,#16811,.F.);
#24166=ORIENTED_EDGE('',*,*,#16812,.T.);
#24167=ORIENTED_EDGE('',*,*,#16797,.T.);
#24168=ORIENTED_EDGE('',*,*,#16810,.F.);
#24169=ORIENTED_EDGE('',*,*,#16813,.F.);
#24170=ORIENTED_EDGE('',*,*,#16814,.T.);
#24171=ORIENTED_EDGE('',*,*,#16795,.T.);
#24172=ORIENTED_EDGE('',*,*,#16812,.F.);
#24173=ORIENTED_EDGE('',*,*,#16815,.F.);
#24174=ORIENTED_EDGE('',*,*,#16806,.T.);
#24175=ORIENTED_EDGE('',*,*,#16793,.T.);
#24176=ORIENTED_EDGE('',*,*,#16814,.F.);
#24177=ORIENTED_EDGE('',*,*,#16816,.F.);
#24178=ORIENTED_EDGE('',*,*,#16817,.T.);
#24179=ORIENTED_EDGE('',*,*,#16818,.F.);
#24180=ORIENTED_EDGE('',*,*,#16819,.F.);
#24181=ORIENTED_EDGE('',*,*,#16820,.F.);
#24182=ORIENTED_EDGE('',*,*,#16819,.T.);
#24183=ORIENTED_EDGE('',*,*,#16821,.T.);
#24184=ORIENTED_EDGE('',*,*,#16822,.F.);
#24185=ORIENTED_EDGE('',*,*,#16821,.F.);
#24186=ORIENTED_EDGE('',*,*,#16818,.T.);
#24187=ORIENTED_EDGE('',*,*,#16823,.T.);
#24188=ORIENTED_EDGE('',*,*,#16824,.F.);
#24189=ORIENTED_EDGE('',*,*,#16823,.F.);
#24190=ORIENTED_EDGE('',*,*,#16817,.F.);
#24191=ORIENTED_EDGE('',*,*,#16825,.F.);
#24192=ORIENTED_EDGE('',*,*,#16826,.T.);
#24193=ORIENTED_EDGE('',*,*,#16827,.F.);
#24194=ORIENTED_EDGE('',*,*,#16828,.F.);
#24195=ORIENTED_EDGE('',*,*,#16829,.F.);
#24196=ORIENTED_EDGE('',*,*,#16828,.T.);
#24197=ORIENTED_EDGE('',*,*,#16830,.T.);
#24198=ORIENTED_EDGE('',*,*,#16831,.F.);
#24199=ORIENTED_EDGE('',*,*,#16830,.F.);
#24200=ORIENTED_EDGE('',*,*,#16827,.T.);
#24201=ORIENTED_EDGE('',*,*,#16832,.T.);
#24202=ORIENTED_EDGE('',*,*,#16833,.F.);
#24203=ORIENTED_EDGE('',*,*,#16832,.F.);
#24204=ORIENTED_EDGE('',*,*,#16826,.F.);
#24205=ORIENTED_EDGE('',*,*,#16834,.F.);
#24206=ORIENTED_EDGE('',*,*,#16835,.T.);
#24207=ORIENTED_EDGE('',*,*,#16836,.F.);
#24208=ORIENTED_EDGE('',*,*,#16837,.F.);
#24209=ORIENTED_EDGE('',*,*,#16838,.F.);
#24210=ORIENTED_EDGE('',*,*,#16837,.T.);
#24211=ORIENTED_EDGE('',*,*,#16839,.T.);
#24212=ORIENTED_EDGE('',*,*,#16840,.F.);
#24213=ORIENTED_EDGE('',*,*,#16839,.F.);
#24214=ORIENTED_EDGE('',*,*,#16836,.T.);
#24215=ORIENTED_EDGE('',*,*,#16841,.T.);
#24216=ORIENTED_EDGE('',*,*,#16842,.F.);
#24217=ORIENTED_EDGE('',*,*,#16841,.F.);
#24218=ORIENTED_EDGE('',*,*,#16835,.F.);
#24219=ORIENTED_EDGE('',*,*,#16843,.F.);
#24220=ORIENTED_EDGE('',*,*,#16844,.T.);
#24221=ORIENTED_EDGE('',*,*,#16845,.F.);
#24222=ORIENTED_EDGE('',*,*,#16846,.F.);
#24223=ORIENTED_EDGE('',*,*,#16847,.F.);
#24224=ORIENTED_EDGE('',*,*,#16846,.T.);
#24225=ORIENTED_EDGE('',*,*,#16848,.T.);
#24226=ORIENTED_EDGE('',*,*,#16849,.F.);
#24227=ORIENTED_EDGE('',*,*,#16848,.F.);
#24228=ORIENTED_EDGE('',*,*,#16845,.T.);
#24229=ORIENTED_EDGE('',*,*,#16850,.T.);
#24230=ORIENTED_EDGE('',*,*,#16851,.F.);
#24231=ORIENTED_EDGE('',*,*,#16850,.F.);
#24232=ORIENTED_EDGE('',*,*,#16844,.F.);
#24233=ORIENTED_EDGE('',*,*,#16852,.F.);
#24234=ORIENTED_EDGE('',*,*,#16853,.T.);
#24235=ORIENTED_EDGE('',*,*,#16854,.F.);
#24236=ORIENTED_EDGE('',*,*,#16855,.F.);
#24237=ORIENTED_EDGE('',*,*,#16856,.F.);
#24238=ORIENTED_EDGE('',*,*,#16855,.T.);
#24239=ORIENTED_EDGE('',*,*,#16857,.T.);
#24240=ORIENTED_EDGE('',*,*,#16858,.F.);
#24241=ORIENTED_EDGE('',*,*,#16857,.F.);
#24242=ORIENTED_EDGE('',*,*,#16854,.T.);
#24243=ORIENTED_EDGE('',*,*,#16859,.T.);
#24244=ORIENTED_EDGE('',*,*,#16860,.F.);
#24245=ORIENTED_EDGE('',*,*,#16859,.F.);
#24246=ORIENTED_EDGE('',*,*,#16853,.F.);
#24247=ORIENTED_EDGE('',*,*,#16861,.F.);
#24248=ORIENTED_EDGE('',*,*,#16862,.T.);
#24249=ORIENTED_EDGE('',*,*,#16863,.F.);
#24250=ORIENTED_EDGE('',*,*,#16864,.F.);
#24251=ORIENTED_EDGE('',*,*,#16865,.F.);
#24252=ORIENTED_EDGE('',*,*,#16864,.T.);
#24253=ORIENTED_EDGE('',*,*,#16866,.T.);
#24254=ORIENTED_EDGE('',*,*,#16867,.F.);
#24255=ORIENTED_EDGE('',*,*,#16866,.F.);
#24256=ORIENTED_EDGE('',*,*,#16863,.T.);
#24257=ORIENTED_EDGE('',*,*,#16868,.T.);
#24258=ORIENTED_EDGE('',*,*,#16869,.F.);
#24259=ORIENTED_EDGE('',*,*,#16868,.F.);
#24260=ORIENTED_EDGE('',*,*,#16862,.F.);
#24261=ORIENTED_EDGE('',*,*,#16870,.F.);
#24262=ORIENTED_EDGE('',*,*,#16871,.T.);
#24263=ORIENTED_EDGE('',*,*,#16872,.F.);
#24264=ORIENTED_EDGE('',*,*,#16873,.F.);
#24265=ORIENTED_EDGE('',*,*,#16874,.F.);
#24266=ORIENTED_EDGE('',*,*,#16873,.T.);
#24267=ORIENTED_EDGE('',*,*,#16875,.T.);
#24268=ORIENTED_EDGE('',*,*,#16876,.F.);
#24269=ORIENTED_EDGE('',*,*,#16875,.F.);
#24270=ORIENTED_EDGE('',*,*,#16872,.T.);
#24271=ORIENTED_EDGE('',*,*,#16877,.T.);
#24272=ORIENTED_EDGE('',*,*,#16878,.F.);
#24273=ORIENTED_EDGE('',*,*,#16877,.F.);
#24274=ORIENTED_EDGE('',*,*,#16871,.F.);
#24275=ORIENTED_EDGE('',*,*,#16879,.F.);
#24276=ORIENTED_EDGE('',*,*,#16880,.T.);
#24277=ORIENTED_EDGE('',*,*,#16881,.F.);
#24278=ORIENTED_EDGE('',*,*,#16882,.F.);
#24279=ORIENTED_EDGE('',*,*,#16883,.F.);
#24280=ORIENTED_EDGE('',*,*,#16882,.T.);
#24281=ORIENTED_EDGE('',*,*,#16884,.T.);
#24282=ORIENTED_EDGE('',*,*,#16885,.F.);
#24283=ORIENTED_EDGE('',*,*,#16884,.F.);
#24284=ORIENTED_EDGE('',*,*,#16881,.T.);
#24285=ORIENTED_EDGE('',*,*,#16886,.T.);
#24286=ORIENTED_EDGE('',*,*,#16887,.F.);
#24287=ORIENTED_EDGE('',*,*,#16886,.F.);
#24288=ORIENTED_EDGE('',*,*,#16880,.F.);
#24289=ORIENTED_EDGE('',*,*,#16888,.F.);
#24290=ORIENTED_EDGE('',*,*,#16889,.T.);
#24291=ORIENTED_EDGE('',*,*,#16890,.F.);
#24292=ORIENTED_EDGE('',*,*,#16891,.F.);
#24293=ORIENTED_EDGE('',*,*,#16892,.F.);
#24294=ORIENTED_EDGE('',*,*,#16891,.T.);
#24295=ORIENTED_EDGE('',*,*,#16893,.T.);
#24296=ORIENTED_EDGE('',*,*,#16894,.F.);
#24297=ORIENTED_EDGE('',*,*,#16895,.F.);
#24298=ORIENTED_EDGE('',*,*,#16893,.F.);
#24299=ORIENTED_EDGE('',*,*,#16890,.T.);
#24300=ORIENTED_EDGE('',*,*,#16896,.T.);
#24301=ORIENTED_EDGE('',*,*,#16897,.F.);
#24302=ORIENTED_EDGE('',*,*,#16896,.F.);
#24303=ORIENTED_EDGE('',*,*,#16889,.F.);
#24304=ORIENTED_EDGE('',*,*,#16898,.F.);
#24305=ORIENTED_EDGE('',*,*,#16899,.F.);
#24306=ORIENTED_EDGE('',*,*,#16900,.T.);
#24307=ORIENTED_EDGE('',*,*,#16901,.F.);
#24308=ORIENTED_EDGE('',*,*,#16902,.F.);
#24309=ORIENTED_EDGE('',*,*,#16903,.F.);
#24310=ORIENTED_EDGE('',*,*,#16902,.T.);
#24311=ORIENTED_EDGE('',*,*,#16904,.T.);
#24312=ORIENTED_EDGE('',*,*,#16905,.F.);
#24313=ORIENTED_EDGE('',*,*,#16904,.F.);
#24314=ORIENTED_EDGE('',*,*,#16901,.T.);
#24315=ORIENTED_EDGE('',*,*,#16906,.T.);
#24316=ORIENTED_EDGE('',*,*,#16907,.F.);
#24317=ORIENTED_EDGE('',*,*,#16906,.F.);
#24318=ORIENTED_EDGE('',*,*,#16900,.F.);
#24319=ORIENTED_EDGE('',*,*,#16908,.F.);
#24320=ORIENTED_EDGE('',*,*,#16909,.T.);
#24321=ORIENTED_EDGE('',*,*,#16910,.F.);
#24322=ORIENTED_EDGE('',*,*,#16911,.F.);
#24323=ORIENTED_EDGE('',*,*,#16912,.F.);
#24324=ORIENTED_EDGE('',*,*,#16911,.T.);
#24325=ORIENTED_EDGE('',*,*,#16913,.T.);
#24326=ORIENTED_EDGE('',*,*,#16914,.F.);
#24327=ORIENTED_EDGE('',*,*,#16913,.F.);
#24328=ORIENTED_EDGE('',*,*,#16910,.T.);
#24329=ORIENTED_EDGE('',*,*,#16915,.T.);
#24330=ORIENTED_EDGE('',*,*,#16916,.F.);
#24331=ORIENTED_EDGE('',*,*,#16915,.F.);
#24332=ORIENTED_EDGE('',*,*,#16909,.F.);
#24333=ORIENTED_EDGE('',*,*,#16917,.F.);
#24334=ORIENTED_EDGE('',*,*,#16918,.T.);
#24335=ORIENTED_EDGE('',*,*,#16919,.F.);
#24336=ORIENTED_EDGE('',*,*,#16920,.F.);
#24337=ORIENTED_EDGE('',*,*,#16921,.F.);
#24338=ORIENTED_EDGE('',*,*,#16920,.T.);
#24339=ORIENTED_EDGE('',*,*,#16922,.T.);
#24340=ORIENTED_EDGE('',*,*,#16923,.F.);
#24341=ORIENTED_EDGE('',*,*,#16922,.F.);
#24342=ORIENTED_EDGE('',*,*,#16919,.T.);
#24343=ORIENTED_EDGE('',*,*,#16924,.T.);
#24344=ORIENTED_EDGE('',*,*,#16925,.F.);
#24345=ORIENTED_EDGE('',*,*,#16924,.F.);
#24346=ORIENTED_EDGE('',*,*,#16918,.F.);
#24347=ORIENTED_EDGE('',*,*,#16926,.F.);
#24348=ORIENTED_EDGE('',*,*,#16927,.T.);
#24349=ORIENTED_EDGE('',*,*,#16928,.F.);
#24350=ORIENTED_EDGE('',*,*,#16929,.F.);
#24351=ORIENTED_EDGE('',*,*,#16930,.F.);
#24352=ORIENTED_EDGE('',*,*,#16929,.T.);
#24353=ORIENTED_EDGE('',*,*,#16931,.T.);
#24354=ORIENTED_EDGE('',*,*,#16932,.F.);
#24355=ORIENTED_EDGE('',*,*,#16931,.F.);
#24356=ORIENTED_EDGE('',*,*,#16928,.T.);
#24357=ORIENTED_EDGE('',*,*,#16933,.T.);
#24358=ORIENTED_EDGE('',*,*,#16934,.F.);
#24359=ORIENTED_EDGE('',*,*,#16933,.F.);
#24360=ORIENTED_EDGE('',*,*,#16927,.F.);
#24361=ORIENTED_EDGE('',*,*,#16935,.F.);
#24362=ORIENTED_EDGE('',*,*,#16936,.T.);
#24363=ORIENTED_EDGE('',*,*,#16937,.F.);
#24364=ORIENTED_EDGE('',*,*,#16938,.F.);
#24365=ORIENTED_EDGE('',*,*,#16939,.F.);
#24366=ORIENTED_EDGE('',*,*,#16938,.T.);
#24367=ORIENTED_EDGE('',*,*,#16940,.T.);
#24368=ORIENTED_EDGE('',*,*,#16941,.F.);
#24369=ORIENTED_EDGE('',*,*,#16940,.F.);
#24370=ORIENTED_EDGE('',*,*,#16937,.T.);
#24371=ORIENTED_EDGE('',*,*,#16942,.T.);
#24372=ORIENTED_EDGE('',*,*,#16943,.F.);
#24373=ORIENTED_EDGE('',*,*,#16942,.F.);
#24374=ORIENTED_EDGE('',*,*,#16936,.F.);
#24375=ORIENTED_EDGE('',*,*,#16944,.F.);
#24376=ORIENTED_EDGE('',*,*,#16945,.T.);
#24377=ORIENTED_EDGE('',*,*,#16946,.F.);
#24378=ORIENTED_EDGE('',*,*,#16947,.F.);
#24379=ORIENTED_EDGE('',*,*,#16948,.F.);
#24380=ORIENTED_EDGE('',*,*,#16947,.T.);
#24381=ORIENTED_EDGE('',*,*,#16949,.T.);
#24382=ORIENTED_EDGE('',*,*,#16950,.F.);
#24383=ORIENTED_EDGE('',*,*,#16949,.F.);
#24384=ORIENTED_EDGE('',*,*,#16946,.T.);
#24385=ORIENTED_EDGE('',*,*,#16951,.T.);
#24386=ORIENTED_EDGE('',*,*,#16952,.F.);
#24387=ORIENTED_EDGE('',*,*,#16951,.F.);
#24388=ORIENTED_EDGE('',*,*,#16945,.F.);
#24389=ORIENTED_EDGE('',*,*,#16953,.F.);
#24390=ORIENTED_EDGE('',*,*,#16954,.T.);
#24391=ORIENTED_EDGE('',*,*,#16955,.F.);
#24392=ORIENTED_EDGE('',*,*,#16956,.F.);
#24393=ORIENTED_EDGE('',*,*,#16957,.F.);
#24394=ORIENTED_EDGE('',*,*,#16956,.T.);
#24395=ORIENTED_EDGE('',*,*,#16958,.T.);
#24396=ORIENTED_EDGE('',*,*,#16959,.F.);
#24397=ORIENTED_EDGE('',*,*,#16958,.F.);
#24398=ORIENTED_EDGE('',*,*,#16955,.T.);
#24399=ORIENTED_EDGE('',*,*,#16960,.T.);
#24400=ORIENTED_EDGE('',*,*,#16961,.F.);
#24401=ORIENTED_EDGE('',*,*,#16960,.F.);
#24402=ORIENTED_EDGE('',*,*,#16954,.F.);
#24403=ORIENTED_EDGE('',*,*,#16962,.F.);
#24404=ORIENTED_EDGE('',*,*,#16963,.T.);
#24405=ORIENTED_EDGE('',*,*,#16964,.F.);
#24406=ORIENTED_EDGE('',*,*,#16965,.F.);
#24407=ORIENTED_EDGE('',*,*,#16966,.F.);
#24408=ORIENTED_EDGE('',*,*,#16965,.T.);
#24409=ORIENTED_EDGE('',*,*,#16967,.T.);
#24410=ORIENTED_EDGE('',*,*,#16968,.F.);
#24411=ORIENTED_EDGE('',*,*,#16967,.F.);
#24412=ORIENTED_EDGE('',*,*,#16964,.T.);
#24413=ORIENTED_EDGE('',*,*,#16969,.T.);
#24414=ORIENTED_EDGE('',*,*,#16970,.F.);
#24415=ORIENTED_EDGE('',*,*,#16969,.F.);
#24416=ORIENTED_EDGE('',*,*,#16963,.F.);
#24417=ORIENTED_EDGE('',*,*,#16971,.F.);
#24418=ORIENTED_EDGE('',*,*,#16972,.T.);
#24419=ORIENTED_EDGE('',*,*,#16973,.F.);
#24420=ORIENTED_EDGE('',*,*,#16974,.F.);
#24421=ORIENTED_EDGE('',*,*,#16975,.F.);
#24422=ORIENTED_EDGE('',*,*,#16974,.T.);
#24423=ORIENTED_EDGE('',*,*,#16976,.T.);
#24424=ORIENTED_EDGE('',*,*,#16977,.F.);
#24425=ORIENTED_EDGE('',*,*,#16976,.F.);
#24426=ORIENTED_EDGE('',*,*,#16973,.T.);
#24427=ORIENTED_EDGE('',*,*,#16978,.T.);
#24428=ORIENTED_EDGE('',*,*,#16979,.F.);
#24429=ORIENTED_EDGE('',*,*,#16978,.F.);
#24430=ORIENTED_EDGE('',*,*,#16972,.F.);
#24431=ORIENTED_EDGE('',*,*,#16980,.F.);
#24432=ORIENTED_EDGE('',*,*,#16981,.T.);
#24433=ORIENTED_EDGE('',*,*,#16982,.F.);
#24434=ORIENTED_EDGE('',*,*,#16983,.F.);
#24435=ORIENTED_EDGE('',*,*,#16984,.F.);
#24436=ORIENTED_EDGE('',*,*,#16983,.T.);
#24437=ORIENTED_EDGE('',*,*,#16985,.T.);
#24438=ORIENTED_EDGE('',*,*,#16986,.F.);
#24439=ORIENTED_EDGE('',*,*,#16985,.F.);
#24440=ORIENTED_EDGE('',*,*,#16982,.T.);
#24441=ORIENTED_EDGE('',*,*,#16987,.T.);
#24442=ORIENTED_EDGE('',*,*,#16988,.F.);
#24443=ORIENTED_EDGE('',*,*,#16987,.F.);
#24444=ORIENTED_EDGE('',*,*,#16981,.F.);
#24445=ORIENTED_EDGE('',*,*,#16989,.F.);
#24446=ORIENTED_EDGE('',*,*,#16990,.T.);
#24447=ORIENTED_EDGE('',*,*,#16991,.F.);
#24448=ORIENTED_EDGE('',*,*,#16992,.F.);
#24449=ORIENTED_EDGE('',*,*,#16993,.F.);
#24450=ORIENTED_EDGE('',*,*,#16992,.T.);
#24451=ORIENTED_EDGE('',*,*,#16994,.T.);
#24452=ORIENTED_EDGE('',*,*,#16995,.F.);
#24453=ORIENTED_EDGE('',*,*,#16994,.F.);
#24454=ORIENTED_EDGE('',*,*,#16991,.T.);
#24455=ORIENTED_EDGE('',*,*,#16996,.T.);
#24456=ORIENTED_EDGE('',*,*,#16997,.F.);
#24457=ORIENTED_EDGE('',*,*,#16996,.F.);
#24458=ORIENTED_EDGE('',*,*,#16990,.F.);
#24459=ORIENTED_EDGE('',*,*,#16998,.F.);
#24460=ORIENTED_EDGE('',*,*,#16999,.T.);
#24461=ORIENTED_EDGE('',*,*,#17000,.F.);
#24462=ORIENTED_EDGE('',*,*,#17001,.F.);
#24463=ORIENTED_EDGE('',*,*,#17002,.F.);
#24464=ORIENTED_EDGE('',*,*,#17001,.T.);
#24465=ORIENTED_EDGE('',*,*,#17003,.T.);
#24466=ORIENTED_EDGE('',*,*,#17004,.F.);
#24467=ORIENTED_EDGE('',*,*,#17003,.F.);
#24468=ORIENTED_EDGE('',*,*,#17000,.T.);
#24469=ORIENTED_EDGE('',*,*,#17005,.T.);
#24470=ORIENTED_EDGE('',*,*,#17006,.F.);
#24471=ORIENTED_EDGE('',*,*,#17005,.F.);
#24472=ORIENTED_EDGE('',*,*,#16999,.F.);
#24473=ORIENTED_EDGE('',*,*,#17007,.F.);
#24474=ORIENTED_EDGE('',*,*,#17008,.T.);
#24475=ORIENTED_EDGE('',*,*,#17009,.F.);
#24476=ORIENTED_EDGE('',*,*,#17010,.F.);
#24477=ORIENTED_EDGE('',*,*,#17011,.F.);
#24478=ORIENTED_EDGE('',*,*,#17010,.T.);
#24479=ORIENTED_EDGE('',*,*,#17012,.T.);
#24480=ORIENTED_EDGE('',*,*,#17013,.F.);
#24481=ORIENTED_EDGE('',*,*,#17012,.F.);
#24482=ORIENTED_EDGE('',*,*,#17009,.T.);
#24483=ORIENTED_EDGE('',*,*,#17014,.T.);
#24484=ORIENTED_EDGE('',*,*,#17015,.F.);
#24485=ORIENTED_EDGE('',*,*,#17014,.F.);
#24486=ORIENTED_EDGE('',*,*,#17008,.F.);
#24487=ORIENTED_EDGE('',*,*,#17016,.F.);
#24488=ORIENTED_EDGE('',*,*,#17017,.T.);
#24489=ORIENTED_EDGE('',*,*,#17018,.F.);
#24490=ORIENTED_EDGE('',*,*,#17019,.F.);
#24491=ORIENTED_EDGE('',*,*,#17020,.F.);
#24492=ORIENTED_EDGE('',*,*,#17019,.T.);
#24493=ORIENTED_EDGE('',*,*,#17021,.T.);
#24494=ORIENTED_EDGE('',*,*,#17022,.F.);
#24495=ORIENTED_EDGE('',*,*,#17021,.F.);
#24496=ORIENTED_EDGE('',*,*,#17018,.T.);
#24497=ORIENTED_EDGE('',*,*,#17023,.T.);
#24498=ORIENTED_EDGE('',*,*,#17024,.F.);
#24499=ORIENTED_EDGE('',*,*,#17023,.F.);
#24500=ORIENTED_EDGE('',*,*,#17017,.F.);
#24501=ORIENTED_EDGE('',*,*,#17025,.F.);
#24502=ORIENTED_EDGE('',*,*,#17026,.T.);
#24503=ORIENTED_EDGE('',*,*,#17027,.F.);
#24504=ORIENTED_EDGE('',*,*,#17028,.F.);
#24505=ORIENTED_EDGE('',*,*,#17029,.F.);
#24506=ORIENTED_EDGE('',*,*,#17028,.T.);
#24507=ORIENTED_EDGE('',*,*,#17030,.T.);
#24508=ORIENTED_EDGE('',*,*,#17031,.F.);
#24509=ORIENTED_EDGE('',*,*,#17030,.F.);
#24510=ORIENTED_EDGE('',*,*,#17027,.T.);
#24511=ORIENTED_EDGE('',*,*,#17032,.T.);
#24512=ORIENTED_EDGE('',*,*,#17033,.F.);
#24513=ORIENTED_EDGE('',*,*,#17032,.F.);
#24514=ORIENTED_EDGE('',*,*,#17026,.F.);
#24515=ORIENTED_EDGE('',*,*,#17034,.F.);
#24516=ORIENTED_EDGE('',*,*,#17035,.T.);
#24517=ORIENTED_EDGE('',*,*,#17036,.F.);
#24518=ORIENTED_EDGE('',*,*,#17037,.F.);
#24519=ORIENTED_EDGE('',*,*,#17038,.F.);
#24520=ORIENTED_EDGE('',*,*,#17037,.T.);
#24521=ORIENTED_EDGE('',*,*,#17039,.T.);
#24522=ORIENTED_EDGE('',*,*,#17040,.F.);
#24523=ORIENTED_EDGE('',*,*,#17039,.F.);
#24524=ORIENTED_EDGE('',*,*,#17036,.T.);
#24525=ORIENTED_EDGE('',*,*,#17041,.T.);
#24526=ORIENTED_EDGE('',*,*,#17042,.F.);
#24527=ORIENTED_EDGE('',*,*,#17041,.F.);
#24528=ORIENTED_EDGE('',*,*,#17035,.F.);
#24529=ORIENTED_EDGE('',*,*,#17043,.F.);
#24530=ORIENTED_EDGE('',*,*,#17044,.T.);
#24531=ORIENTED_EDGE('',*,*,#17045,.F.);
#24532=ORIENTED_EDGE('',*,*,#17046,.F.);
#24533=ORIENTED_EDGE('',*,*,#17047,.F.);
#24534=ORIENTED_EDGE('',*,*,#17046,.T.);
#24535=ORIENTED_EDGE('',*,*,#17048,.T.);
#24536=ORIENTED_EDGE('',*,*,#17049,.F.);
#24537=ORIENTED_EDGE('',*,*,#17048,.F.);
#24538=ORIENTED_EDGE('',*,*,#17045,.T.);
#24539=ORIENTED_EDGE('',*,*,#17050,.T.);
#24540=ORIENTED_EDGE('',*,*,#17051,.F.);
#24541=ORIENTED_EDGE('',*,*,#17050,.F.);
#24542=ORIENTED_EDGE('',*,*,#17044,.F.);
#24543=ORIENTED_EDGE('',*,*,#17052,.F.);
#24544=ORIENTED_EDGE('',*,*,#17053,.T.);
#24545=ORIENTED_EDGE('',*,*,#17054,.T.);
#24546=ORIENTED_EDGE('',*,*,#17055,.F.);
#24547=ORIENTED_EDGE('',*,*,#17056,.T.);
#24548=ORIENTED_EDGE('',*,*,#17057,.F.);
#24549=ORIENTED_EDGE('',*,*,#17053,.F.);
#24550=ORIENTED_EDGE('',*,*,#17058,.F.);
#24551=ORIENTED_EDGE('',*,*,#17054,.F.);
#24552=ORIENTED_EDGE('',*,*,#17057,.T.);
#24553=ORIENTED_EDGE('',*,*,#17059,.T.);
#24554=ORIENTED_EDGE('',*,*,#17060,.F.);
#24555=ORIENTED_EDGE('',*,*,#17059,.F.);
#24556=ORIENTED_EDGE('',*,*,#17056,.F.);
#24557=ORIENTED_EDGE('',*,*,#17061,.F.);
#24558=ORIENTED_EDGE('',*,*,#17062,.T.);
#24559=ORIENTED_EDGE('',*,*,#17063,.F.);
#24560=ORIENTED_EDGE('',*,*,#17064,.F.);
#24561=ORIENTED_EDGE('',*,*,#17065,.F.);
#24562=ORIENTED_EDGE('',*,*,#17064,.T.);
#24563=ORIENTED_EDGE('',*,*,#17066,.T.);
#24564=ORIENTED_EDGE('',*,*,#17067,.F.);
#24565=ORIENTED_EDGE('',*,*,#17066,.F.);
#24566=ORIENTED_EDGE('',*,*,#17063,.T.);
#24567=ORIENTED_EDGE('',*,*,#17068,.T.);
#24568=ORIENTED_EDGE('',*,*,#17069,.F.);
#24569=ORIENTED_EDGE('',*,*,#17068,.F.);
#24570=ORIENTED_EDGE('',*,*,#17062,.F.);
#24571=ORIENTED_EDGE('',*,*,#17070,.F.);
#24572=ORIENTED_EDGE('',*,*,#17071,.T.);
#24573=ORIENTED_EDGE('',*,*,#17072,.F.);
#24574=ORIENTED_EDGE('',*,*,#17073,.F.);
#24575=ORIENTED_EDGE('',*,*,#17074,.F.);
#24576=ORIENTED_EDGE('',*,*,#17073,.T.);
#24577=ORIENTED_EDGE('',*,*,#17075,.T.);
#24578=ORIENTED_EDGE('',*,*,#17076,.F.);
#24579=ORIENTED_EDGE('',*,*,#17075,.F.);
#24580=ORIENTED_EDGE('',*,*,#17072,.T.);
#24581=ORIENTED_EDGE('',*,*,#17077,.T.);
#24582=ORIENTED_EDGE('',*,*,#17078,.F.);
#24583=ORIENTED_EDGE('',*,*,#17077,.F.);
#24584=ORIENTED_EDGE('',*,*,#17071,.F.);
#24585=ORIENTED_EDGE('',*,*,#17079,.F.);
#24586=ORIENTED_EDGE('',*,*,#17080,.T.);
#24587=ORIENTED_EDGE('',*,*,#17081,.F.);
#24588=ORIENTED_EDGE('',*,*,#17082,.F.);
#24589=ORIENTED_EDGE('',*,*,#17083,.F.);
#24590=ORIENTED_EDGE('',*,*,#17082,.T.);
#24591=ORIENTED_EDGE('',*,*,#17084,.T.);
#24592=ORIENTED_EDGE('',*,*,#17085,.F.);
#24593=ORIENTED_EDGE('',*,*,#17084,.F.);
#24594=ORIENTED_EDGE('',*,*,#17081,.T.);
#24595=ORIENTED_EDGE('',*,*,#17086,.T.);
#24596=ORIENTED_EDGE('',*,*,#17087,.F.);
#24597=ORIENTED_EDGE('',*,*,#17086,.F.);
#24598=ORIENTED_EDGE('',*,*,#17080,.F.);
#24599=ORIENTED_EDGE('',*,*,#17088,.F.);
#24600=ORIENTED_EDGE('',*,*,#17089,.T.);
#24601=ORIENTED_EDGE('',*,*,#17090,.F.);
#24602=ORIENTED_EDGE('',*,*,#17091,.F.);
#24603=ORIENTED_EDGE('',*,*,#17092,.F.);
#24604=ORIENTED_EDGE('',*,*,#17091,.T.);
#24605=ORIENTED_EDGE('',*,*,#17093,.T.);
#24606=ORIENTED_EDGE('',*,*,#17094,.F.);
#24607=ORIENTED_EDGE('',*,*,#17093,.F.);
#24608=ORIENTED_EDGE('',*,*,#17090,.T.);
#24609=ORIENTED_EDGE('',*,*,#17095,.T.);
#24610=ORIENTED_EDGE('',*,*,#17096,.F.);
#24611=ORIENTED_EDGE('',*,*,#17095,.F.);
#24612=ORIENTED_EDGE('',*,*,#17089,.F.);
#24613=ORIENTED_EDGE('',*,*,#17097,.F.);
#24614=ORIENTED_EDGE('',*,*,#17098,.T.);
#24615=ORIENTED_EDGE('',*,*,#17099,.F.);
#24616=ORIENTED_EDGE('',*,*,#17100,.F.);
#24617=ORIENTED_EDGE('',*,*,#17101,.F.);
#24618=ORIENTED_EDGE('',*,*,#17100,.T.);
#24619=ORIENTED_EDGE('',*,*,#17102,.T.);
#24620=ORIENTED_EDGE('',*,*,#17103,.F.);
#24621=ORIENTED_EDGE('',*,*,#17102,.F.);
#24622=ORIENTED_EDGE('',*,*,#17099,.T.);
#24623=ORIENTED_EDGE('',*,*,#17104,.T.);
#24624=ORIENTED_EDGE('',*,*,#17105,.F.);
#24625=ORIENTED_EDGE('',*,*,#17104,.F.);
#24626=ORIENTED_EDGE('',*,*,#17098,.F.);
#24627=ORIENTED_EDGE('',*,*,#17106,.F.);
#24628=ORIENTED_EDGE('',*,*,#17107,.T.);
#24629=ORIENTED_EDGE('',*,*,#17108,.F.);
#24630=ORIENTED_EDGE('',*,*,#17109,.F.);
#24631=ORIENTED_EDGE('',*,*,#17110,.F.);
#24632=ORIENTED_EDGE('',*,*,#17109,.T.);
#24633=ORIENTED_EDGE('',*,*,#17111,.T.);
#24634=ORIENTED_EDGE('',*,*,#17112,.F.);
#24635=ORIENTED_EDGE('',*,*,#17111,.F.);
#24636=ORIENTED_EDGE('',*,*,#17108,.T.);
#24637=ORIENTED_EDGE('',*,*,#17113,.T.);
#24638=ORIENTED_EDGE('',*,*,#17114,.F.);
#24639=ORIENTED_EDGE('',*,*,#17113,.F.);
#24640=ORIENTED_EDGE('',*,*,#17107,.F.);
#24641=ORIENTED_EDGE('',*,*,#17115,.F.);
#24642=ORIENTED_EDGE('',*,*,#17116,.T.);
#24643=ORIENTED_EDGE('',*,*,#17117,.F.);
#24644=ORIENTED_EDGE('',*,*,#17118,.F.);
#24645=ORIENTED_EDGE('',*,*,#17119,.F.);
#24646=ORIENTED_EDGE('',*,*,#17118,.T.);
#24647=ORIENTED_EDGE('',*,*,#17120,.T.);
#24648=ORIENTED_EDGE('',*,*,#17121,.F.);
#24649=ORIENTED_EDGE('',*,*,#17120,.F.);
#24650=ORIENTED_EDGE('',*,*,#17117,.T.);
#24651=ORIENTED_EDGE('',*,*,#17122,.T.);
#24652=ORIENTED_EDGE('',*,*,#17123,.F.);
#24653=ORIENTED_EDGE('',*,*,#17122,.F.);
#24654=ORIENTED_EDGE('',*,*,#17116,.F.);
#24655=ORIENTED_EDGE('',*,*,#17124,.F.);
#24656=ORIENTED_EDGE('',*,*,#17125,.T.);
#24657=ORIENTED_EDGE('',*,*,#17126,.F.);
#24658=ORIENTED_EDGE('',*,*,#17127,.F.);
#24659=ORIENTED_EDGE('',*,*,#17128,.F.);
#24660=ORIENTED_EDGE('',*,*,#17127,.T.);
#24661=ORIENTED_EDGE('',*,*,#17129,.T.);
#24662=ORIENTED_EDGE('',*,*,#17130,.F.);
#24663=ORIENTED_EDGE('',*,*,#17129,.F.);
#24664=ORIENTED_EDGE('',*,*,#17126,.T.);
#24665=ORIENTED_EDGE('',*,*,#17131,.T.);
#24666=ORIENTED_EDGE('',*,*,#17132,.F.);
#24667=ORIENTED_EDGE('',*,*,#17131,.F.);
#24668=ORIENTED_EDGE('',*,*,#17125,.F.);
#24669=ORIENTED_EDGE('',*,*,#17133,.F.);
#24670=ORIENTED_EDGE('',*,*,#17134,.T.);
#24671=ORIENTED_EDGE('',*,*,#17135,.F.);
#24672=ORIENTED_EDGE('',*,*,#17136,.F.);
#24673=ORIENTED_EDGE('',*,*,#17137,.F.);
#24674=ORIENTED_EDGE('',*,*,#17136,.T.);
#24675=ORIENTED_EDGE('',*,*,#17138,.T.);
#24676=ORIENTED_EDGE('',*,*,#17139,.F.);
#24677=ORIENTED_EDGE('',*,*,#17138,.F.);
#24678=ORIENTED_EDGE('',*,*,#17135,.T.);
#24679=ORIENTED_EDGE('',*,*,#17140,.T.);
#24680=ORIENTED_EDGE('',*,*,#17141,.F.);
#24681=ORIENTED_EDGE('',*,*,#17140,.F.);
#24682=ORIENTED_EDGE('',*,*,#17134,.F.);
#24683=ORIENTED_EDGE('',*,*,#17142,.F.);
#24684=ORIENTED_EDGE('',*,*,#16782,.F.);
#24685=ORIENTED_EDGE('',*,*,#16658,.F.);
#24686=ORIENTED_EDGE('',*,*,#16783,.F.);
#24687=ORIENTED_EDGE('',*,*,#17143,.T.);
#24688=ORIENTED_EDGE('',*,*,#17142,.T.);
#24689=ORIENTED_EDGE('',*,*,#17143,.F.);
#24690=ORIENTED_EDGE('',*,*,#17144,.F.);
#24691=ORIENTED_EDGE('',*,*,#17145,.T.);
#24692=ORIENTED_EDGE('',*,*,#16790,.T.);
#24693=ORIENTED_EDGE('',*,*,#17145,.F.);
#24694=ORIENTED_EDGE('',*,*,#16816,.T.);
#24695=ORIENTED_EDGE('',*,*,#17146,.F.);
#24696=ORIENTED_EDGE('',*,*,#17130,.T.);
#24697=ORIENTED_EDGE('',*,*,#17132,.T.);
#24698=ORIENTED_EDGE('',*,*,#17124,.T.);
#24699=ORIENTED_EDGE('',*,*,#17147,.F.);
#24700=ORIENTED_EDGE('',*,*,#16831,.T.);
#24701=ORIENTED_EDGE('',*,*,#16833,.T.);
#24702=ORIENTED_EDGE('',*,*,#16825,.T.);
#24703=ORIENTED_EDGE('',*,*,#17148,.F.);
#24704=ORIENTED_EDGE('',*,*,#17121,.T.);
#24705=ORIENTED_EDGE('',*,*,#17123,.T.);
#24706=ORIENTED_EDGE('',*,*,#17115,.T.);
#24707=ORIENTED_EDGE('',*,*,#17149,.F.);
#24708=ORIENTED_EDGE('',*,*,#16840,.T.);
#24709=ORIENTED_EDGE('',*,*,#16842,.T.);
#24710=ORIENTED_EDGE('',*,*,#16834,.T.);
#24711=ORIENTED_EDGE('',*,*,#17150,.F.);
#24712=ORIENTED_EDGE('',*,*,#17112,.T.);
#24713=ORIENTED_EDGE('',*,*,#17114,.T.);
#24714=ORIENTED_EDGE('',*,*,#17106,.T.);
#24715=ORIENTED_EDGE('',*,*,#17151,.F.);
#24716=ORIENTED_EDGE('',*,*,#16849,.T.);
#24717=ORIENTED_EDGE('',*,*,#16851,.T.);
#24718=ORIENTED_EDGE('',*,*,#16843,.T.);
#24719=ORIENTED_EDGE('',*,*,#17152,.F.);
#24720=ORIENTED_EDGE('',*,*,#17103,.T.);
#24721=ORIENTED_EDGE('',*,*,#17105,.T.);
#24722=ORIENTED_EDGE('',*,*,#17097,.T.);
#24723=ORIENTED_EDGE('',*,*,#17153,.F.);
#24724=ORIENTED_EDGE('',*,*,#16858,.T.);
#24725=ORIENTED_EDGE('',*,*,#16860,.T.);
#24726=ORIENTED_EDGE('',*,*,#16852,.T.);
#24727=ORIENTED_EDGE('',*,*,#17154,.F.);
#24728=ORIENTED_EDGE('',*,*,#17094,.T.);
#24729=ORIENTED_EDGE('',*,*,#17096,.T.);
#24730=ORIENTED_EDGE('',*,*,#17088,.T.);
#24731=ORIENTED_EDGE('',*,*,#17155,.F.);
#24732=ORIENTED_EDGE('',*,*,#16867,.T.);
#24733=ORIENTED_EDGE('',*,*,#16869,.T.);
#24734=ORIENTED_EDGE('',*,*,#16861,.T.);
#24735=ORIENTED_EDGE('',*,*,#17156,.F.);
#24736=ORIENTED_EDGE('',*,*,#17085,.T.);
#24737=ORIENTED_EDGE('',*,*,#17087,.T.);
#24738=ORIENTED_EDGE('',*,*,#17079,.T.);
#24739=ORIENTED_EDGE('',*,*,#17157,.F.);
#24740=ORIENTED_EDGE('',*,*,#16876,.T.);
#24741=ORIENTED_EDGE('',*,*,#16878,.T.);
#24742=ORIENTED_EDGE('',*,*,#16870,.T.);
#24743=ORIENTED_EDGE('',*,*,#17158,.F.);
#24744=ORIENTED_EDGE('',*,*,#17076,.T.);
#24745=ORIENTED_EDGE('',*,*,#17078,.T.);
#24746=ORIENTED_EDGE('',*,*,#17070,.T.);
#24747=ORIENTED_EDGE('',*,*,#17159,.F.);
#24748=ORIENTED_EDGE('',*,*,#16885,.T.);
#24749=ORIENTED_EDGE('',*,*,#16887,.T.);
#24750=ORIENTED_EDGE('',*,*,#16879,.T.);
#24751=ORIENTED_EDGE('',*,*,#17160,.F.);
#24752=ORIENTED_EDGE('',*,*,#17067,.T.);
#24753=ORIENTED_EDGE('',*,*,#17069,.T.);
#24754=ORIENTED_EDGE('',*,*,#17061,.T.);
#24755=ORIENTED_EDGE('',*,*,#17161,.F.);
#24756=ORIENTED_EDGE('',*,*,#16895,.T.);
#24757=ORIENTED_EDGE('',*,*,#16897,.T.);
#24758=ORIENTED_EDGE('',*,*,#17162,.T.);
#24759=ORIENTED_EDGE('',*,*,#17144,.T.);
#24760=ORIENTED_EDGE('',*,*,#17162,.F.);
#24761=ORIENTED_EDGE('',*,*,#16898,.T.);
#24762=ORIENTED_EDGE('',*,*,#16888,.T.);
#24763=ORIENTED_EDGE('',*,*,#17163,.F.);
#24764=ORIENTED_EDGE('',*,*,#16905,.T.);
#24765=ORIENTED_EDGE('',*,*,#16907,.T.);
#24766=ORIENTED_EDGE('',*,*,#16899,.T.);
#24767=ORIENTED_EDGE('',*,*,#17164,.F.);
#24768=ORIENTED_EDGE('',*,*,#17049,.T.);
#24769=ORIENTED_EDGE('',*,*,#17051,.T.);
#24770=ORIENTED_EDGE('',*,*,#17043,.T.);
#24771=ORIENTED_EDGE('',*,*,#17165,.F.);
#24772=ORIENTED_EDGE('',*,*,#16914,.T.);
#24773=ORIENTED_EDGE('',*,*,#16916,.T.);
#24774=ORIENTED_EDGE('',*,*,#16908,.T.);
#24775=ORIENTED_EDGE('',*,*,#17166,.F.);
#24776=ORIENTED_EDGE('',*,*,#17040,.T.);
#24777=ORIENTED_EDGE('',*,*,#17042,.T.);
#24778=ORIENTED_EDGE('',*,*,#17034,.T.);
#24779=ORIENTED_EDGE('',*,*,#17167,.F.);
#24780=ORIENTED_EDGE('',*,*,#16923,.T.);
#24781=ORIENTED_EDGE('',*,*,#16925,.T.);
#24782=ORIENTED_EDGE('',*,*,#16917,.T.);
#24783=ORIENTED_EDGE('',*,*,#17168,.F.);
#24784=ORIENTED_EDGE('',*,*,#17031,.T.);
#24785=ORIENTED_EDGE('',*,*,#17033,.T.);
#24786=ORIENTED_EDGE('',*,*,#17025,.T.);
#24787=ORIENTED_EDGE('',*,*,#17169,.F.);
#24788=ORIENTED_EDGE('',*,*,#16932,.T.);
#24789=ORIENTED_EDGE('',*,*,#16934,.T.);
#24790=ORIENTED_EDGE('',*,*,#16926,.T.);
#24791=ORIENTED_EDGE('',*,*,#17170,.F.);
#24792=ORIENTED_EDGE('',*,*,#17022,.T.);
#24793=ORIENTED_EDGE('',*,*,#17024,.T.);
#24794=ORIENTED_EDGE('',*,*,#17016,.T.);
#24795=ORIENTED_EDGE('',*,*,#17171,.F.);
#24796=ORIENTED_EDGE('',*,*,#16941,.T.);
#24797=ORIENTED_EDGE('',*,*,#16943,.T.);
#24798=ORIENTED_EDGE('',*,*,#16935,.T.);
#24799=ORIENTED_EDGE('',*,*,#17172,.F.);
#24800=ORIENTED_EDGE('',*,*,#17013,.T.);
#24801=ORIENTED_EDGE('',*,*,#17015,.T.);
#24802=ORIENTED_EDGE('',*,*,#17007,.T.);
#24803=ORIENTED_EDGE('',*,*,#17173,.F.);
#24804=ORIENTED_EDGE('',*,*,#16950,.T.);
#24805=ORIENTED_EDGE('',*,*,#16952,.T.);
#24806=ORIENTED_EDGE('',*,*,#16944,.T.);
#24807=ORIENTED_EDGE('',*,*,#17174,.F.);
#24808=ORIENTED_EDGE('',*,*,#17004,.T.);
#24809=ORIENTED_EDGE('',*,*,#17006,.T.);
#24810=ORIENTED_EDGE('',*,*,#16998,.T.);
#24811=ORIENTED_EDGE('',*,*,#17175,.F.);
#24812=ORIENTED_EDGE('',*,*,#16959,.T.);
#24813=ORIENTED_EDGE('',*,*,#16961,.T.);
#24814=ORIENTED_EDGE('',*,*,#16953,.T.);
#24815=ORIENTED_EDGE('',*,*,#17176,.F.);
#24816=ORIENTED_EDGE('',*,*,#16995,.T.);
#24817=ORIENTED_EDGE('',*,*,#16997,.T.);
#24818=ORIENTED_EDGE('',*,*,#16989,.T.);
#24819=ORIENTED_EDGE('',*,*,#17177,.F.);
#24820=ORIENTED_EDGE('',*,*,#16968,.T.);
#24821=ORIENTED_EDGE('',*,*,#16970,.T.);
#24822=ORIENTED_EDGE('',*,*,#16962,.T.);
#24823=ORIENTED_EDGE('',*,*,#17178,.F.);
#24824=ORIENTED_EDGE('',*,*,#16986,.T.);
#24825=ORIENTED_EDGE('',*,*,#16988,.T.);
#24826=ORIENTED_EDGE('',*,*,#16980,.T.);
#24827=ORIENTED_EDGE('',*,*,#17179,.F.);
#24828=ORIENTED_EDGE('',*,*,#16977,.T.);
#24829=ORIENTED_EDGE('',*,*,#16979,.T.);
#24830=ORIENTED_EDGE('',*,*,#16971,.T.);
#24831=ORIENTED_EDGE('',*,*,#17180,.F.);
#24832=ORIENTED_EDGE('',*,*,#17058,.T.);
#24833=ORIENTED_EDGE('',*,*,#17060,.T.);
#24834=ORIENTED_EDGE('',*,*,#17055,.T.);
#24835=ORIENTED_EDGE('',*,*,#17181,.F.);
#24836=ORIENTED_EDGE('',*,*,#17139,.T.);
#24837=ORIENTED_EDGE('',*,*,#17141,.T.);
#24838=ORIENTED_EDGE('',*,*,#17133,.T.);
#24839=ORIENTED_EDGE('',*,*,#17182,.F.);
#24840=ORIENTED_EDGE('',*,*,#16822,.T.);
#24841=ORIENTED_EDGE('',*,*,#16824,.T.);
#24842=ORIENTED_EDGE('',*,*,#17183,.F.);
#24843=ORIENTED_EDGE('',*,*,#17184,.T.);
#24844=ORIENTED_EDGE('',*,*,#16894,.T.);
#24845=ORIENTED_EDGE('',*,*,#17161,.T.);
#24846=ORIENTED_EDGE('',*,*,#17065,.T.);
#24847=ORIENTED_EDGE('',*,*,#17160,.T.);
#24848=ORIENTED_EDGE('',*,*,#16883,.T.);
#24849=ORIENTED_EDGE('',*,*,#17159,.T.);
#24850=ORIENTED_EDGE('',*,*,#17074,.T.);
#24851=ORIENTED_EDGE('',*,*,#17158,.T.);
#24852=ORIENTED_EDGE('',*,*,#16874,.T.);
#24853=ORIENTED_EDGE('',*,*,#17157,.T.);
#24854=ORIENTED_EDGE('',*,*,#17083,.T.);
#24855=ORIENTED_EDGE('',*,*,#17156,.T.);
#24856=ORIENTED_EDGE('',*,*,#16865,.T.);
#24857=ORIENTED_EDGE('',*,*,#17155,.T.);
#24858=ORIENTED_EDGE('',*,*,#17092,.T.);
#24859=ORIENTED_EDGE('',*,*,#17154,.T.);
#24860=ORIENTED_EDGE('',*,*,#16856,.T.);
#24861=ORIENTED_EDGE('',*,*,#17153,.T.);
#24862=ORIENTED_EDGE('',*,*,#17101,.T.);
#24863=ORIENTED_EDGE('',*,*,#17152,.T.);
#24864=ORIENTED_EDGE('',*,*,#16847,.T.);
#24865=ORIENTED_EDGE('',*,*,#17151,.T.);
#24866=ORIENTED_EDGE('',*,*,#17110,.T.);
#24867=ORIENTED_EDGE('',*,*,#17150,.T.);
#24868=ORIENTED_EDGE('',*,*,#16838,.T.);
#24869=ORIENTED_EDGE('',*,*,#17149,.T.);
#24870=ORIENTED_EDGE('',*,*,#17119,.T.);
#24871=ORIENTED_EDGE('',*,*,#17148,.T.);
#24872=ORIENTED_EDGE('',*,*,#16829,.T.);
#24873=ORIENTED_EDGE('',*,*,#17147,.T.);
#24874=ORIENTED_EDGE('',*,*,#17128,.T.);
#24875=ORIENTED_EDGE('',*,*,#17146,.T.);
#24876=ORIENTED_EDGE('',*,*,#16820,.T.);
#24877=ORIENTED_EDGE('',*,*,#17182,.T.);
#24878=ORIENTED_EDGE('',*,*,#17137,.T.);
#24879=ORIENTED_EDGE('',*,*,#17181,.T.);
#24880=ORIENTED_EDGE('',*,*,#17052,.T.);
#24881=ORIENTED_EDGE('',*,*,#17180,.T.);
#24882=ORIENTED_EDGE('',*,*,#16975,.T.);
#24883=ORIENTED_EDGE('',*,*,#17179,.T.);
#24884=ORIENTED_EDGE('',*,*,#16984,.T.);
#24885=ORIENTED_EDGE('',*,*,#17178,.T.);
#24886=ORIENTED_EDGE('',*,*,#16966,.T.);
#24887=ORIENTED_EDGE('',*,*,#17177,.T.);
#24888=ORIENTED_EDGE('',*,*,#16993,.T.);
#24889=ORIENTED_EDGE('',*,*,#17176,.T.);
#24890=ORIENTED_EDGE('',*,*,#16957,.T.);
#24891=ORIENTED_EDGE('',*,*,#17175,.T.);
#24892=ORIENTED_EDGE('',*,*,#17002,.T.);
#24893=ORIENTED_EDGE('',*,*,#17174,.T.);
#24894=ORIENTED_EDGE('',*,*,#16948,.T.);
#24895=ORIENTED_EDGE('',*,*,#17173,.T.);
#24896=ORIENTED_EDGE('',*,*,#17011,.T.);
#24897=ORIENTED_EDGE('',*,*,#17172,.T.);
#24898=ORIENTED_EDGE('',*,*,#16939,.T.);
#24899=ORIENTED_EDGE('',*,*,#17171,.T.);
#24900=ORIENTED_EDGE('',*,*,#17020,.T.);
#24901=ORIENTED_EDGE('',*,*,#17170,.T.);
#24902=ORIENTED_EDGE('',*,*,#16930,.T.);
#24903=ORIENTED_EDGE('',*,*,#17169,.T.);
#24904=ORIENTED_EDGE('',*,*,#17029,.T.);
#24905=ORIENTED_EDGE('',*,*,#17168,.T.);
#24906=ORIENTED_EDGE('',*,*,#16921,.T.);
#24907=ORIENTED_EDGE('',*,*,#17167,.T.);
#24908=ORIENTED_EDGE('',*,*,#17038,.T.);
#24909=ORIENTED_EDGE('',*,*,#17166,.T.);
#24910=ORIENTED_EDGE('',*,*,#16912,.T.);
#24911=ORIENTED_EDGE('',*,*,#17165,.T.);
#24912=ORIENTED_EDGE('',*,*,#17047,.T.);
#24913=ORIENTED_EDGE('',*,*,#17164,.T.);
#24914=ORIENTED_EDGE('',*,*,#16903,.T.);
#24915=ORIENTED_EDGE('',*,*,#17163,.T.);
#24916=ORIENTED_EDGE('',*,*,#16892,.T.);
#24917=ORIENTED_EDGE('',*,*,#17184,.F.);
#24918=ORIENTED_EDGE('',*,*,#17183,.T.);
#24919=ORIENTED_EDGE('',*,*,#16804,.T.);
#24920=ORIENTED_EDGE('',*,*,#16815,.T.);
#24921=ORIENTED_EDGE('',*,*,#16813,.T.);
#24922=ORIENTED_EDGE('',*,*,#16811,.T.);
#24923=ORIENTED_EDGE('',*,*,#16809,.T.);
#24924=ORIENTED_EDGE('',*,*,#16807,.T.);
#25108=CONICAL_SURFACE('',#29047,0.144337567297406,1.03037682652431);
#25109=CONICAL_SURFACE('',#29274,0.275,0.785398163397448);
#25110=CONICAL_SURFACE('',#29275,0.485,0.785398163397448);
#25111=CONICAL_SURFACE('',#29314,0.475,0.785398163397449);
#26454=ADVANCED_FACE('',(#3866),#1511,.T.);
#26455=ADVANCED_FACE('',(#3867),#1512,.T.);
#26456=ADVANCED_FACE('',(#3868),#1513,.T.);
#26457=ADVANCED_FACE('',(#3869),#1514,.T.);
#26458=ADVANCED_FACE('',(#3870),#1515,.T.);
#26459=ADVANCED_FACE('',(#3871),#1516,.T.);
#26460=ADVANCED_FACE('',(#3872),#1517,.T.);
#26461=ADVANCED_FACE('',(#3873),#1518,.T.);
#26462=ADVANCED_FACE('',(#3874),#1519,.T.);
#26463=ADVANCED_FACE('',(#3875),#1520,.T.);
#26464=ADVANCED_FACE('',(#3876),#1521,.T.);
#26465=ADVANCED_FACE('',(#3877),#1522,.T.);
#26466=ADVANCED_FACE('',(#3878),#1523,.T.);
#26467=ADVANCED_FACE('',(#3879),#1524,.T.);
#26468=ADVANCED_FACE('',(#3880),#1525,.T.);
#26469=ADVANCED_FACE('',(#3881),#1526,.T.);
#26470=ADVANCED_FACE('',(#3882),#1527,.T.);
#26471=ADVANCED_FACE('',(#3883),#1528,.T.);
#26472=ADVANCED_FACE('',(#3884),#1529,.T.);
#26473=ADVANCED_FACE('',(#3885),#1530,.T.);
#26474=ADVANCED_FACE('',(#3886),#1531,.T.);
#26475=ADVANCED_FACE('',(#3887),#1532,.T.);
#26476=ADVANCED_FACE('',(#3888),#1533,.T.);
#26477=ADVANCED_FACE('',(#3889),#1534,.T.);
#26478=ADVANCED_FACE('',(#3890),#1535,.T.);
#26479=ADVANCED_FACE('',(#3891),#1536,.T.);
#26480=ADVANCED_FACE('',(#3892),#1537,.T.);
#26481=ADVANCED_FACE('',(#3893),#1538,.T.);
#26482=ADVANCED_FACE('',(#3894),#1539,.T.);
#26483=ADVANCED_FACE('',(#3895),#1540,.T.);
#26484=ADVANCED_FACE('',(#3896),#1541,.T.);
#26485=ADVANCED_FACE('',(#3897),#1542,.T.);
#26486=ADVANCED_FACE('',(#3898),#1543,.T.);
#26487=ADVANCED_FACE('',(#3899),#1544,.T.);
#26488=ADVANCED_FACE('',(#3900),#1545,.T.);
#26489=ADVANCED_FACE('',(#3901),#1546,.T.);
#26490=ADVANCED_FACE('',(#3902),#1547,.T.);
#26491=ADVANCED_FACE('',(#3903),#1548,.T.);
#26492=ADVANCED_FACE('',(#3904),#1549,.T.);
#26493=ADVANCED_FACE('',(#3905),#2363,.F.);
#26494=ADVANCED_FACE('',(#3906),#172,.F.);
#26495=ADVANCED_FACE('',(#3907),#2364,.T.);
#26496=ADVANCED_FACE('',(#3908),#1550,.T.);
#26497=ADVANCED_FACE('',(#3909),#173,.F.);
#26498=ADVANCED_FACE('',(#3910),#1088,.F.);
#26499=ADVANCED_FACE('',(#3911),#1551,.T.);
#26500=ADVANCED_FACE('',(#3912,#1654),#2365,.T.);
#26501=ADVANCED_FACE('',(#3913),#2366,.F.);
#26502=ADVANCED_FACE('',(#3914),#2367,.F.);
#26503=ADVANCED_FACE('',(#3915),#2368,.F.);
#26504=ADVANCED_FACE('',(#3916),#2369,.F.);
#26505=ADVANCED_FACE('',(#3917),#2370,.F.);
#26506=ADVANCED_FACE('',(#3918),#2371,.F.);
#26507=ADVANCED_FACE('',(#3919),#25108,.F.);
#26508=ADVANCED_FACE('',(#3920),#2372,.F.);
#26509=ADVANCED_FACE('',(#3921),#2373,.F.);
#26510=ADVANCED_FACE('',(#3922),#2374,.F.);
#26511=ADVANCED_FACE('',(#3923),#2375,.F.);
#26512=ADVANCED_FACE('',(#3924),#2376,.F.);
#26513=ADVANCED_FACE('',(#3925),#2377,.F.);
#26514=ADVANCED_FACE('',(#3926),#2378,.F.);
#26515=ADVANCED_FACE('',(#3927),#2379,.F.);
#26516=ADVANCED_FACE('',(#3928),#2380,.F.);
#26517=ADVANCED_FACE('',(#3929),#2381,.F.);
#26518=ADVANCED_FACE('',(#3930),#2382,.F.);
#26519=ADVANCED_FACE('',(#3931),#2383,.F.);
#26520=ADVANCED_FACE('',(#3932),#2384,.F.);
#26521=ADVANCED_FACE('',(#3933),#2385,.F.);
#26522=ADVANCED_FACE('',(#3934),#2386,.F.);
#26523=ADVANCED_FACE('',(#3935),#2387,.F.);
#26524=ADVANCED_FACE('',(#3936),#2388,.F.);
#26525=ADVANCED_FACE('',(#3937),#2389,.F.);
#26526=ADVANCED_FACE('',(#3938),#2390,.F.);
#26527=ADVANCED_FACE('',(#3939),#2391,.F.);
#26528=ADVANCED_FACE('',(#3940),#2392,.F.);
#26529=ADVANCED_FACE('',(#3941),#2393,.F.);
#26530=ADVANCED_FACE('',(#3942),#2394,.F.);
#26531=ADVANCED_FACE('',(#3943),#2395,.F.);
#26532=ADVANCED_FACE('',(#3944),#2396,.F.);
#26533=ADVANCED_FACE('',(#3945),#2397,.F.);
#26534=ADVANCED_FACE('',(#3946),#2398,.F.);
#26535=ADVANCED_FACE('',(#3947),#2399,.F.);
#26536=ADVANCED_FACE('',(#3948),#2400,.F.);
#26537=ADVANCED_FACE('',(#3949),#2401,.F.);
#26538=ADVANCED_FACE('',(#3950),#2402,.F.);
#26539=ADVANCED_FACE('',(#3951),#2403,.F.);
#26540=ADVANCED_FACE('',(#3952),#2404,.F.);
#26541=ADVANCED_FACE('',(#3953),#2405,.F.);
#26542=ADVANCED_FACE('',(#3954),#2406,.F.);
#26543=ADVANCED_FACE('',(#3955),#2407,.F.);
#26544=ADVANCED_FACE('',(#3956),#2408,.F.);
#26545=ADVANCED_FACE('',(#3957),#2409,.F.);
#26546=ADVANCED_FACE('',(#3958),#2410,.F.);
#26547=ADVANCED_FACE('',(#3959),#2411,.F.);
#26548=ADVANCED_FACE('',(#3960),#2412,.F.);
#26549=ADVANCED_FACE('',(#3961),#2413,.F.);
#26550=ADVANCED_FACE('',(#3962),#2414,.F.);
#26551=ADVANCED_FACE('',(#3963),#2415,.F.);
#26552=ADVANCED_FACE('',(#3964),#2416,.F.);
#26553=ADVANCED_FACE('',(#3965),#2417,.F.);
#26554=ADVANCED_FACE('',(#3966),#2418,.F.);
#26555=ADVANCED_FACE('',(#3967),#2419,.F.);
#26556=ADVANCED_FACE('',(#3968),#2420,.F.);
#26557=ADVANCED_FACE('',(#3969),#2421,.F.);
#26558=ADVANCED_FACE('',(#3970),#2422,.F.);
#26559=ADVANCED_FACE('',(#3971),#2423,.F.);
#26560=ADVANCED_FACE('',(#3972),#2424,.F.);
#26561=ADVANCED_FACE('',(#3973),#2425,.F.);
#26562=ADVANCED_FACE('',(#3974),#2426,.F.);
#26563=ADVANCED_FACE('',(#3975),#2427,.F.);
#26564=ADVANCED_FACE('',(#3976),#2428,.F.);
#26565=ADVANCED_FACE('',(#3977),#2429,.F.);
#26566=ADVANCED_FACE('',(#3978),#2430,.F.);
#26567=ADVANCED_FACE('',(#3979),#2431,.F.);
#26568=ADVANCED_FACE('',(#3980),#2432,.F.);
#26569=ADVANCED_FACE('',(#3981),#2433,.F.);
#26570=ADVANCED_FACE('',(#3982),#2434,.F.);
#26571=ADVANCED_FACE('',(#3983),#2435,.F.);
#26572=ADVANCED_FACE('',(#3984),#2436,.F.);
#26573=ADVANCED_FACE('',(#3985),#2437,.F.);
#26574=ADVANCED_FACE('',(#3986),#2438,.F.);
#26575=ADVANCED_FACE('',(#3987),#2439,.F.);
#26576=ADVANCED_FACE('',(#3988),#2440,.F.);
#26577=ADVANCED_FACE('',(#3989),#2441,.F.);
#26578=ADVANCED_FACE('',(#3990),#2442,.F.);
#26579=ADVANCED_FACE('',(#3991),#2443,.F.);
#26580=ADVANCED_FACE('',(#3992),#2444,.F.);
#26581=ADVANCED_FACE('',(#3993),#2445,.F.);
#26582=ADVANCED_FACE('',(#3994),#2446,.F.);
#26583=ADVANCED_FACE('',(#3995),#2447,.F.);
#26584=ADVANCED_FACE('',(#3996),#2448,.F.);
#26585=ADVANCED_FACE('',(#3997),#2449,.F.);
#26586=ADVANCED_FACE('',(#3998),#2450,.F.);
#26587=ADVANCED_FACE('',(#3999),#2451,.F.);
#26588=ADVANCED_FACE('',(#4000),#2452,.F.);
#26589=ADVANCED_FACE('',(#4001),#2453,.F.);
#26590=ADVANCED_FACE('',(#4002),#2454,.F.);
#26591=ADVANCED_FACE('',(#4003),#2455,.F.);
#26592=ADVANCED_FACE('',(#4004),#2456,.F.);
#26593=ADVANCED_FACE('',(#4005),#2457,.F.);
#26594=ADVANCED_FACE('',(#4006),#2458,.F.);
#26595=ADVANCED_FACE('',(#4007),#2459,.F.);
#26596=ADVANCED_FACE('',(#4008),#2460,.F.);
#26597=ADVANCED_FACE('',(#4009),#2461,.F.);
#26598=ADVANCED_FACE('',(#4010),#2462,.F.);
#26599=ADVANCED_FACE('',(#4011),#2463,.F.);
#26600=ADVANCED_FACE('',(#4012),#2464,.F.);
#26601=ADVANCED_FACE('',(#4013),#2465,.F.);
#26602=ADVANCED_FACE('',(#4014),#2466,.F.);
#26603=ADVANCED_FACE('',(#4015),#2467,.F.);
#26604=ADVANCED_FACE('',(#4016),#2468,.F.);
#26605=ADVANCED_FACE('',(#4017),#2469,.F.);
#26606=ADVANCED_FACE('',(#4018),#2470,.F.);
#26607=ADVANCED_FACE('',(#4019),#2471,.F.);
#26608=ADVANCED_FACE('',(#4020),#2472,.F.);
#26609=ADVANCED_FACE('',(#4021),#2473,.F.);
#26610=ADVANCED_FACE('',(#4022),#2474,.F.);
#26611=ADVANCED_FACE('',(#4023),#2475,.F.);
#26612=ADVANCED_FACE('',(#4024),#2476,.F.);
#26613=ADVANCED_FACE('',(#4025),#2477,.F.);
#26614=ADVANCED_FACE('',(#4026),#2478,.F.);
#26615=ADVANCED_FACE('',(#4027),#2479,.F.);
#26616=ADVANCED_FACE('',(#4028),#2480,.F.);
#26617=ADVANCED_FACE('',(#4029),#2481,.F.);
#26618=ADVANCED_FACE('',(#4030),#2482,.F.);
#26619=ADVANCED_FACE('',(#4031),#2483,.F.);
#26620=ADVANCED_FACE('',(#4032),#2484,.F.);
#26621=ADVANCED_FACE('',(#4033),#2485,.F.);
#26622=ADVANCED_FACE('',(#4034),#2486,.F.);
#26623=ADVANCED_FACE('',(#4035),#2487,.F.);
#26624=ADVANCED_FACE('',(#4036),#2488,.F.);
#26625=ADVANCED_FACE('',(#4037),#2489,.F.);
#26626=ADVANCED_FACE('',(#4038),#2490,.F.);
#26627=ADVANCED_FACE('',(#4039),#2491,.F.);
#26628=ADVANCED_FACE('',(#4040),#2492,.F.);
#26629=ADVANCED_FACE('',(#4041),#2493,.F.);
#26630=ADVANCED_FACE('',(#4042),#2494,.F.);
#26631=ADVANCED_FACE('',(#4043),#2495,.F.);
#26632=ADVANCED_FACE('',(#4044),#2496,.F.);
#26633=ADVANCED_FACE('',(#4045),#2497,.F.);
#26634=ADVANCED_FACE('',(#4046),#2498,.F.);
#26635=ADVANCED_FACE('',(#4047),#2499,.F.);
#26636=ADVANCED_FACE('',(#4048),#2500,.F.);
#26637=ADVANCED_FACE('',(#4049),#2501,.F.);
#26638=ADVANCED_FACE('',(#4050),#2502,.F.);
#26639=ADVANCED_FACE('',(#4051),#2503,.F.);
#26640=ADVANCED_FACE('',(#4052),#2504,.F.);
#26641=ADVANCED_FACE('',(#4053),#2505,.F.);
#26642=ADVANCED_FACE('',(#4054),#2506,.F.);
#26643=ADVANCED_FACE('',(#4055),#2507,.F.);
#26644=ADVANCED_FACE('',(#4056),#2508,.F.);
#26645=ADVANCED_FACE('',(#4057),#2509,.F.);
#26646=ADVANCED_FACE('',(#4058),#2510,.F.);
#26647=ADVANCED_FACE('',(#4059),#2511,.F.);
#26648=ADVANCED_FACE('',(#4060),#2512,.F.);
#26649=ADVANCED_FACE('',(#4061),#2513,.F.);
#26650=ADVANCED_FACE('',(#4062),#2514,.F.);
#26651=ADVANCED_FACE('',(#4063),#2515,.F.);
#26652=ADVANCED_FACE('',(#4064),#2516,.F.);
#26653=ADVANCED_FACE('',(#4065),#2517,.F.);
#26654=ADVANCED_FACE('',(#4066),#2518,.F.);
#26655=ADVANCED_FACE('',(#4067),#2519,.F.);
#26656=ADVANCED_FACE('',(#4068),#2520,.F.);
#26657=ADVANCED_FACE('',(#4069),#2521,.F.);
#26658=ADVANCED_FACE('',(#4070),#2522,.T.);
#26659=ADVANCED_FACE('',(#4071),#25109,.T.);
#26660=ADVANCED_FACE('',(#4072),#25110,.T.);
#26661=ADVANCED_FACE('',(#4073),#1552,.T.);
#26662=ADVANCED_FACE('',(#4074),#25111,.T.);
#26663=ADVANCED_FACE('',(#4075,#1655),#2523,.T.);
#26683=CLOSED_SHELL('',(#26454,#26455,#26456,#26457,#26458,#26459,#26460,
#26461,#26462,#26463,#26464,#26465,#26466,#26467,#26468,#26469,#26470,#26471,
#26472,#26473,#26474,#26475,#26476,#26477,#26478,#26479,#26480,#26481,#26482,
#26483,#26484,#26485,#26486,#26487,#26488,#26489,#26490,#26491,#26492,#26493,
#26494,#26495,#26496,#26497,#26498,#26499,#26500,#26501,#26502,#26503,#26504,
#26505,#26506,#26507,#26508,#26509,#26510,#26511,#26512,#26513,#26514,#26515,
#26516,#26517,#26518,#26519,#26520,#26521,#26522,#26523,#26524,#26525,#26526,
#26527,#26528,#26529,#26530,#26531,#26532,#26533,#26534,#26535,#26536,#26537,
#26538,#26539,#26540,#26541,#26542,#26543,#26544,#26545,#26546,#26547,#26548,
#26549,#26550,#26551,#26552,#26553,#26554,#26555,#26556,#26557,#26558,#26559,
#26560,#26561,#26562,#26563,#26564,#26565,#26566,#26567,#26568,#26569,#26570,
#26571,#26572,#26573,#26574,#26575,#26576,#26577,#26578,#26579,#26580,#26581,
#26582,#26583,#26584,#26585,#26586,#26587,#26588,#26589,#26590,#26591,#26592,
#26593,#26594,#26595,#26596,#26597,#26598,#26599,#26600,#26601,#26602,#26603,
#26604,#26605,#26606,#26607,#26608,#26609,#26610,#26611,#26612,#26613,#26614,
#26615,#26616,#26617,#26618,#26619,#26620,#26621,#26622,#26623,#26624,#26625,
#26626,#26627,#26628,#26629,#26630,#26631,#26632,#26633,#26634,#26635,#26636,
#26637,#26638,#26639,#26640,#26641,#26642,#26643,#26644,#26645,#26646,#26647,
#26648,#26649,#26650,#26651,#26652,#26653,#26654,#26655,#26656,#26657,#26658,
#26659,#26660,#26661,#26662,#26663));
#28978=AXIS2_PLACEMENT_3D('',#73082,#35333,#35334);
#28979=AXIS2_PLACEMENT_3D('',#73083,#35335,#35336);
#28980=AXIS2_PLACEMENT_3D('',#73099,#35338,#35339);
#28981=AXIS2_PLACEMENT_3D('',#73107,#35340,#35341);
#28982=AXIS2_PLACEMENT_3D('',#73155,#35343,#35344);
#28983=AXIS2_PLACEMENT_3D('',#73203,#35346,#35347);
#28984=AXIS2_PLACEMENT_3D('',#73257,#35349,#35350);
#28985=AXIS2_PLACEMENT_3D('',#73305,#35352,#35353);
#28986=AXIS2_PLACEMENT_3D('',#73353,#35355,#35356);
#28987=AXIS2_PLACEMENT_3D('',#73404,#35358,#35359);
#28988=AXIS2_PLACEMENT_3D('',#73452,#35361,#35362);
#28989=AXIS2_PLACEMENT_3D('',#73500,#35364,#35365);
#28990=AXIS2_PLACEMENT_3D('',#73548,#35367,#35368);
#28991=AXIS2_PLACEMENT_3D('',#73602,#35370,#35371);
#28992=AXIS2_PLACEMENT_3D('',#73650,#35373,#35374);
#28993=AXIS2_PLACEMENT_3D('',#73698,#35376,#35377);
#28994=AXIS2_PLACEMENT_3D('',#73752,#35379,#35380);
#28995=AXIS2_PLACEMENT_3D('',#73800,#35382,#35383);
#28996=AXIS2_PLACEMENT_3D('',#73848,#35385,#35386);
#28997=AXIS2_PLACEMENT_3D('',#73902,#35388,#35389);
#28998=AXIS2_PLACEMENT_3D('',#73950,#35391,#35392);
#28999=AXIS2_PLACEMENT_3D('',#73998,#35394,#35395);
#29000=AXIS2_PLACEMENT_3D('',#74003,#35397,#35398);
#29001=AXIS2_PLACEMENT_3D('',#74051,#35399,#35400);
#29002=AXIS2_PLACEMENT_3D('',#74065,#35402,#35403);
#29003=AXIS2_PLACEMENT_3D('',#74072,#35404,#35405);
#29004=AXIS2_PLACEMENT_3D('',#74097,#35407,#35408);
#29005=AXIS2_PLACEMENT_3D('',#74121,#35410,#35411);
#29006=AXIS2_PLACEMENT_3D('',#74146,#35413,#35414);
#29007=AXIS2_PLACEMENT_3D('',#74171,#35416,#35417);
#29008=AXIS2_PLACEMENT_3D('',#74195,#35419,#35420);
#29009=AXIS2_PLACEMENT_3D('',#74220,#35422,#35423);
#29010=AXIS2_PLACEMENT_3D('',#74245,#35425,#35426);
#29011=AXIS2_PLACEMENT_3D('',#74269,#35428,#35429);
#29012=AXIS2_PLACEMENT_3D('',#74294,#35431,#35432);
#29013=AXIS2_PLACEMENT_3D('',#74319,#35434,#35435);
#29014=AXIS2_PLACEMENT_3D('',#74343,#35437,#35438);
#29015=AXIS2_PLACEMENT_3D('',#74367,#35440,#35441);
#29016=AXIS2_PLACEMENT_3D('',#74392,#35443,#35444);
#29017=AXIS2_PLACEMENT_3D('',#74417,#35446,#35447);
#29018=AXIS2_PLACEMENT_3D('',#74441,#35449,#35450);
#29019=AXIS2_PLACEMENT_3D('',#74466,#35452,#35453);
#29020=AXIS2_PLACEMENT_3D('',#74491,#35455,#35456);
#29021=AXIS2_PLACEMENT_3D('',#74515,#35458,#35459);
#29022=AXIS2_PLACEMENT_3D('',#74572,#35460,#35461);
#29023=AXIS2_PLACEMENT_3D('',#75208,#35462,#35463);
#29024=AXIS2_PLACEMENT_3D('',#75210,#35464,#35465);
#29025=AXIS2_PLACEMENT_3D('',#75211,#35466,#35467);
#29026=AXIS2_PLACEMENT_3D('',#75271,#35468,#35469);
#29027=AXIS2_PLACEMENT_3D('',#75272,#35470,#35471);
#29028=AXIS2_PLACEMENT_3D('',#75789,#35472,#35473);
#29029=AXIS2_PLACEMENT_3D('',#75791,#35474,#35475);
#29030=AXIS2_PLACEMENT_3D('',#75792,#35476,#35477);
#29031=AXIS2_PLACEMENT_3D('',#75793,#35478,#35479);
#29032=AXIS2_PLACEMENT_3D('',#75794,#35480,#35481);
#29033=AXIS2_PLACEMENT_3D('',#75795,#35482,#35483);
#29034=AXIS2_PLACEMENT_3D('',#75797,#35484,#35485);
#29035=AXIS2_PLACEMENT_3D('',#75798,#35486,#35487);
#29036=AXIS2_PLACEMENT_3D('',#75802,#35489,#35490);
#29037=AXIS2_PLACEMENT_3D('',#75803,#35491,#35492);
#29038=AXIS2_PLACEMENT_3D('',#75806,#35494,#35495);
#29039=AXIS2_PLACEMENT_3D('',#75807,#35496,#35497);
#29040=AXIS2_PLACEMENT_3D('',#75810,#35499,#35500);
#29041=AXIS2_PLACEMENT_3D('',#75811,#35501,#35502);
#29042=AXIS2_PLACEMENT_3D('',#75814,#35504,#35505);
#29043=AXIS2_PLACEMENT_3D('',#75815,#35506,#35507);
#29044=AXIS2_PLACEMENT_3D('',#75818,#35509,#35510);
#29045=AXIS2_PLACEMENT_3D('',#75819,#35511,#35512);
#29046=AXIS2_PLACEMENT_3D('',#75821,#35514,#35515);
#29047=AXIS2_PLACEMENT_3D('',#75822,#35516,#35517);
#29048=AXIS2_PLACEMENT_3D('',#75825,#35519,#35520);
#29049=AXIS2_PLACEMENT_3D('',#75831,#35524,#35525);
#29050=AXIS2_PLACEMENT_3D('',#75835,#35528,#35529);
#29051=AXIS2_PLACEMENT_3D('',#75839,#35532,#35533);
#29052=AXIS2_PLACEMENT_3D('',#75843,#35536,#35537);
#29053=AXIS2_PLACEMENT_3D('',#75847,#35540,#35541);
#29054=AXIS2_PLACEMENT_3D('',#75849,#35543,#35544);
#29055=AXIS2_PLACEMENT_3D('',#75858,#35549,#35550);
#29056=AXIS2_PLACEMENT_3D('',#75860,#35551,#35552);
#29057=AXIS2_PLACEMENT_3D('',#75862,#35554,#35555);
#29058=AXIS2_PLACEMENT_3D('',#75866,#35558,#35559);
#29059=AXIS2_PLACEMENT_3D('',#75867,#35560,#35561);
#29060=AXIS2_PLACEMENT_3D('',#75868,#35562,#35563);
#29061=AXIS2_PLACEMENT_3D('',#75877,#35568,#35569);
#29062=AXIS2_PLACEMENT_3D('',#75879,#35570,#35571);
#29063=AXIS2_PLACEMENT_3D('',#75881,#35573,#35574);
#29064=AXIS2_PLACEMENT_3D('',#75885,#35577,#35578);
#29065=AXIS2_PLACEMENT_3D('',#75886,#35579,#35580);
#29066=AXIS2_PLACEMENT_3D('',#75887,#35581,#35582);
#29067=AXIS2_PLACEMENT_3D('',#75896,#35587,#35588);
#29068=AXIS2_PLACEMENT_3D('',#75898,#35589,#35590);
#29069=AXIS2_PLACEMENT_3D('',#75900,#35592,#35593);
#29070=AXIS2_PLACEMENT_3D('',#75904,#35596,#35597);
#29071=AXIS2_PLACEMENT_3D('',#75905,#35598,#35599);
#29072=AXIS2_PLACEMENT_3D('',#75906,#35600,#35601);
#29073=AXIS2_PLACEMENT_3D('',#75915,#35606,#35607);
#29074=AXIS2_PLACEMENT_3D('',#75917,#35608,#35609);
#29075=AXIS2_PLACEMENT_3D('',#75919,#35611,#35612);
#29076=AXIS2_PLACEMENT_3D('',#75923,#35615,#35616);
#29077=AXIS2_PLACEMENT_3D('',#75924,#35617,#35618);
#29078=AXIS2_PLACEMENT_3D('',#75925,#35619,#35620);
#29079=AXIS2_PLACEMENT_3D('',#75934,#35625,#35626);
#29080=AXIS2_PLACEMENT_3D('',#75936,#35627,#35628);
#29081=AXIS2_PLACEMENT_3D('',#75938,#35630,#35631);
#29082=AXIS2_PLACEMENT_3D('',#75942,#35634,#35635);
#29083=AXIS2_PLACEMENT_3D('',#75943,#35636,#35637);
#29084=AXIS2_PLACEMENT_3D('',#75944,#35638,#35639);
#29085=AXIS2_PLACEMENT_3D('',#75953,#35644,#35645);
#29086=AXIS2_PLACEMENT_3D('',#75955,#35646,#35647);
#29087=AXIS2_PLACEMENT_3D('',#75957,#35649,#35650);
#29088=AXIS2_PLACEMENT_3D('',#75961,#35653,#35654);
#29089=AXIS2_PLACEMENT_3D('',#75962,#35655,#35656);
#29090=AXIS2_PLACEMENT_3D('',#75963,#35657,#35658);
#29091=AXIS2_PLACEMENT_3D('',#75972,#35663,#35664);
#29092=AXIS2_PLACEMENT_3D('',#75974,#35665,#35666);
#29093=AXIS2_PLACEMENT_3D('',#75976,#35668,#35669);
#29094=AXIS2_PLACEMENT_3D('',#75980,#35672,#35673);
#29095=AXIS2_PLACEMENT_3D('',#75981,#35674,#35675);
#29096=AXIS2_PLACEMENT_3D('',#75982,#35676,#35677);
#29097=AXIS2_PLACEMENT_3D('',#75991,#35682,#35683);
#29098=AXIS2_PLACEMENT_3D('',#75993,#35684,#35685);
#29099=AXIS2_PLACEMENT_3D('',#75995,#35687,#35688);
#29100=AXIS2_PLACEMENT_3D('',#75999,#35691,#35692);
#29101=AXIS2_PLACEMENT_3D('',#76000,#35693,#35694);
#29102=AXIS2_PLACEMENT_3D('',#76001,#35695,#35696);
#29103=AXIS2_PLACEMENT_3D('',#76010,#35701,#35702);
#29104=AXIS2_PLACEMENT_3D('',#76012,#35703,#35704);
#29105=AXIS2_PLACEMENT_3D('',#76015,#35706,#35707);
#29106=AXIS2_PLACEMENT_3D('',#76016,#35708,#35709);
#29107=AXIS2_PLACEMENT_3D('',#76020,#35712,#35713);
#29108=AXIS2_PLACEMENT_3D('',#76022,#35714,#35715);
#29109=AXIS2_PLACEMENT_3D('',#76023,#35716,#35717);
#29110=AXIS2_PLACEMENT_3D('',#76024,#35718,#35719);
#29111=AXIS2_PLACEMENT_3D('',#76033,#35724,#35725);
#29112=AXIS2_PLACEMENT_3D('',#76035,#35726,#35727);
#29113=AXIS2_PLACEMENT_3D('',#76037,#35729,#35730);
#29114=AXIS2_PLACEMENT_3D('',#76041,#35733,#35734);
#29115=AXIS2_PLACEMENT_3D('',#76042,#35735,#35736);
#29116=AXIS2_PLACEMENT_3D('',#76043,#35737,#35738);
#29117=AXIS2_PLACEMENT_3D('',#76052,#35743,#35744);
#29118=AXIS2_PLACEMENT_3D('',#76054,#35745,#35746);
#29119=AXIS2_PLACEMENT_3D('',#76056,#35748,#35749);
#29120=AXIS2_PLACEMENT_3D('',#76060,#35752,#35753);
#29121=AXIS2_PLACEMENT_3D('',#76061,#35754,#35755);
#29122=AXIS2_PLACEMENT_3D('',#76062,#35756,#35757);
#29123=AXIS2_PLACEMENT_3D('',#76071,#35762,#35763);
#29124=AXIS2_PLACEMENT_3D('',#76073,#35764,#35765);
#29125=AXIS2_PLACEMENT_3D('',#76075,#35767,#35768);
#29126=AXIS2_PLACEMENT_3D('',#76079,#35771,#35772);
#29127=AXIS2_PLACEMENT_3D('',#76080,#35773,#35774);
#29128=AXIS2_PLACEMENT_3D('',#76081,#35775,#35776);
#29129=AXIS2_PLACEMENT_3D('',#76090,#35781,#35782);
#29130=AXIS2_PLACEMENT_3D('',#76092,#35783,#35784);
#29131=AXIS2_PLACEMENT_3D('',#76094,#35786,#35787);
#29132=AXIS2_PLACEMENT_3D('',#76098,#35790,#35791);
#29133=AXIS2_PLACEMENT_3D('',#76099,#35792,#35793);
#29134=AXIS2_PLACEMENT_3D('',#76100,#35794,#35795);
#29135=AXIS2_PLACEMENT_3D('',#76109,#35800,#35801);
#29136=AXIS2_PLACEMENT_3D('',#76111,#35802,#35803);
#29137=AXIS2_PLACEMENT_3D('',#76113,#35805,#35806);
#29138=AXIS2_PLACEMENT_3D('',#76117,#35809,#35810);
#29139=AXIS2_PLACEMENT_3D('',#76118,#35811,#35812);
#29140=AXIS2_PLACEMENT_3D('',#76119,#35813,#35814);
#29141=AXIS2_PLACEMENT_3D('',#76128,#35819,#35820);
#29142=AXIS2_PLACEMENT_3D('',#76130,#35821,#35822);
#29143=AXIS2_PLACEMENT_3D('',#76132,#35824,#35825);
#29144=AXIS2_PLACEMENT_3D('',#76136,#35828,#35829);
#29145=AXIS2_PLACEMENT_3D('',#76137,#35830,#35831);
#29146=AXIS2_PLACEMENT_3D('',#76138,#35832,#35833);
#29147=AXIS2_PLACEMENT_3D('',#76147,#35838,#35839);
#29148=AXIS2_PLACEMENT_3D('',#76149,#35840,#35841);
#29149=AXIS2_PLACEMENT_3D('',#76151,#35843,#35844);
#29150=AXIS2_PLACEMENT_3D('',#76155,#35847,#35848);
#29151=AXIS2_PLACEMENT_3D('',#76156,#35849,#35850);
#29152=AXIS2_PLACEMENT_3D('',#76157,#35851,#35852);
#29153=AXIS2_PLACEMENT_3D('',#76166,#35857,#35858);
#29154=AXIS2_PLACEMENT_3D('',#76168,#35859,#35860);
#29155=AXIS2_PLACEMENT_3D('',#76170,#35862,#35863);
#29156=AXIS2_PLACEMENT_3D('',#76174,#35866,#35867);
#29157=AXIS2_PLACEMENT_3D('',#76175,#35868,#35869);
#29158=AXIS2_PLACEMENT_3D('',#76176,#35870,#35871);
#29159=AXIS2_PLACEMENT_3D('',#76185,#35876,#35877);
#29160=AXIS2_PLACEMENT_3D('',#76187,#35878,#35879);
#29161=AXIS2_PLACEMENT_3D('',#76189,#35881,#35882);
#29162=AXIS2_PLACEMENT_3D('',#76193,#35885,#35886);
#29163=AXIS2_PLACEMENT_3D('',#76194,#35887,#35888);
#29164=AXIS2_PLACEMENT_3D('',#76195,#35889,#35890);
#29165=AXIS2_PLACEMENT_3D('',#76204,#35895,#35896);
#29166=AXIS2_PLACEMENT_3D('',#76206,#35897,#35898);
#29167=AXIS2_PLACEMENT_3D('',#76208,#35900,#35901);
#29168=AXIS2_PLACEMENT_3D('',#76212,#35904,#35905);
#29169=AXIS2_PLACEMENT_3D('',#76213,#35906,#35907);
#29170=AXIS2_PLACEMENT_3D('',#76214,#35908,#35909);
#29171=AXIS2_PLACEMENT_3D('',#76223,#35914,#35915);
#29172=AXIS2_PLACEMENT_3D('',#76225,#35916,#35917);
#29173=AXIS2_PLACEMENT_3D('',#76227,#35919,#35920);
#29174=AXIS2_PLACEMENT_3D('',#76231,#35923,#35924);
#29175=AXIS2_PLACEMENT_3D('',#76232,#35925,#35926);
#29176=AXIS2_PLACEMENT_3D('',#76233,#35927,#35928);
#29177=AXIS2_PLACEMENT_3D('',#76242,#35933,#35934);
#29178=AXIS2_PLACEMENT_3D('',#76244,#35935,#35936);
#29179=AXIS2_PLACEMENT_3D('',#76246,#35938,#35939);
#29180=AXIS2_PLACEMENT_3D('',#76250,#35942,#35943);
#29181=AXIS2_PLACEMENT_3D('',#76251,#35944,#35945);
#29182=AXIS2_PLACEMENT_3D('',#76252,#35946,#35947);
#29183=AXIS2_PLACEMENT_3D('',#76261,#35952,#35953);
#29184=AXIS2_PLACEMENT_3D('',#76263,#35954,#35955);
#29185=AXIS2_PLACEMENT_3D('',#76265,#35957,#35958);
#29186=AXIS2_PLACEMENT_3D('',#76269,#35961,#35962);
#29187=AXIS2_PLACEMENT_3D('',#76270,#35963,#35964);
#29188=AXIS2_PLACEMENT_3D('',#76271,#35965,#35966);
#29189=AXIS2_PLACEMENT_3D('',#76280,#35971,#35972);
#29190=AXIS2_PLACEMENT_3D('',#76282,#35973,#35974);
#29191=AXIS2_PLACEMENT_3D('',#76284,#35976,#35977);
#29192=AXIS2_PLACEMENT_3D('',#76288,#35980,#35981);
#29193=AXIS2_PLACEMENT_3D('',#76289,#35982,#35983);
#29194=AXIS2_PLACEMENT_3D('',#76290,#35984,#35985);
#29195=AXIS2_PLACEMENT_3D('',#76299,#35990,#35991);
#29196=AXIS2_PLACEMENT_3D('',#76301,#35992,#35993);
#29197=AXIS2_PLACEMENT_3D('',#76303,#35995,#35996);
#29198=AXIS2_PLACEMENT_3D('',#76307,#35999,#36000);
#29199=AXIS2_PLACEMENT_3D('',#76308,#36001,#36002);
#29200=AXIS2_PLACEMENT_3D('',#76309,#36003,#36004);
#29201=AXIS2_PLACEMENT_3D('',#76318,#36009,#36010);
#29202=AXIS2_PLACEMENT_3D('',#76320,#36011,#36012);
#29203=AXIS2_PLACEMENT_3D('',#76322,#36014,#36015);
#29204=AXIS2_PLACEMENT_3D('',#76326,#36018,#36019);
#29205=AXIS2_PLACEMENT_3D('',#76327,#36020,#36021);
#29206=AXIS2_PLACEMENT_3D('',#76328,#36022,#36023);
#29207=AXIS2_PLACEMENT_3D('',#76337,#36028,#36029);
#29208=AXIS2_PLACEMENT_3D('',#76339,#36030,#36031);
#29209=AXIS2_PLACEMENT_3D('',#76341,#36033,#36034);
#29210=AXIS2_PLACEMENT_3D('',#76345,#36037,#36038);
#29211=AXIS2_PLACEMENT_3D('',#76346,#36039,#36040);
#29212=AXIS2_PLACEMENT_3D('',#76347,#36041,#36042);
#29213=AXIS2_PLACEMENT_3D('',#76350,#36043,#36044);
#29214=AXIS2_PLACEMENT_3D('',#76354,#36047,#36048);
#29215=AXIS2_PLACEMENT_3D('',#76360,#36052,#36053);
#29216=AXIS2_PLACEMENT_3D('',#76364,#36056,#36057);
#29217=AXIS2_PLACEMENT_3D('',#76365,#36058,#36059);
#29218=AXIS2_PLACEMENT_3D('',#76366,#36060,#36061);
#29219=AXIS2_PLACEMENT_3D('',#76375,#36066,#36067);
#29220=AXIS2_PLACEMENT_3D('',#76377,#36068,#36069);
#29221=AXIS2_PLACEMENT_3D('',#76379,#36071,#36072);
#29222=AXIS2_PLACEMENT_3D('',#76383,#36075,#36076);
#29223=AXIS2_PLACEMENT_3D('',#76384,#36077,#36078);
#29224=AXIS2_PLACEMENT_3D('',#76385,#36079,#36080);
#29225=AXIS2_PLACEMENT_3D('',#76394,#36085,#36086);
#29226=AXIS2_PLACEMENT_3D('',#76396,#36087,#36088);
#29227=AXIS2_PLACEMENT_3D('',#76398,#36090,#36091);
#29228=AXIS2_PLACEMENT_3D('',#76402,#36094,#36095);
#29229=AXIS2_PLACEMENT_3D('',#76403,#36096,#36097);
#29230=AXIS2_PLACEMENT_3D('',#76404,#36098,#36099);
#29231=AXIS2_PLACEMENT_3D('',#76413,#36104,#36105);
#29232=AXIS2_PLACEMENT_3D('',#76415,#36106,#36107);
#29233=AXIS2_PLACEMENT_3D('',#76417,#36109,#36110);
#29234=AXIS2_PLACEMENT_3D('',#76421,#36113,#36114);
#29235=AXIS2_PLACEMENT_3D('',#76422,#36115,#36116);
#29236=AXIS2_PLACEMENT_3D('',#76423,#36117,#36118);
#29237=AXIS2_PLACEMENT_3D('',#76432,#36123,#36124);
#29238=AXIS2_PLACEMENT_3D('',#76434,#36125,#36126);
#29239=AXIS2_PLACEMENT_3D('',#76436,#36128,#36129);
#29240=AXIS2_PLACEMENT_3D('',#76440,#36132,#36133);
#29241=AXIS2_PLACEMENT_3D('',#76441,#36134,#36135);
#29242=AXIS2_PLACEMENT_3D('',#76442,#36136,#36137);
#29243=AXIS2_PLACEMENT_3D('',#76451,#36142,#36143);
#29244=AXIS2_PLACEMENT_3D('',#76453,#36144,#36145);
#29245=AXIS2_PLACEMENT_3D('',#76455,#36147,#36148);
#29246=AXIS2_PLACEMENT_3D('',#76459,#36151,#36152);
#29247=AXIS2_PLACEMENT_3D('',#76460,#36153,#36154);
#29248=AXIS2_PLACEMENT_3D('',#76461,#36155,#36156);
#29249=AXIS2_PLACEMENT_3D('',#76470,#36161,#36162);
#29250=AXIS2_PLACEMENT_3D('',#76472,#36163,#36164);
#29251=AXIS2_PLACEMENT_3D('',#76474,#36166,#36167);
#29252=AXIS2_PLACEMENT_3D('',#76478,#36170,#36171);
#29253=AXIS2_PLACEMENT_3D('',#76479,#36172,#36173);
#29254=AXIS2_PLACEMENT_3D('',#76480,#36174,#36175);
#29255=AXIS2_PLACEMENT_3D('',#76489,#36180,#36181);
#29256=AXIS2_PLACEMENT_3D('',#76491,#36182,#36183);
#29257=AXIS2_PLACEMENT_3D('',#76493,#36185,#36186);
#29258=AXIS2_PLACEMENT_3D('',#76497,#36189,#36190);
#29259=AXIS2_PLACEMENT_3D('',#76498,#36191,#36192);
#29260=AXIS2_PLACEMENT_3D('',#76499,#36193,#36194);
#29261=AXIS2_PLACEMENT_3D('',#76508,#36199,#36200);
#29262=AXIS2_PLACEMENT_3D('',#76510,#36201,#36202);
#29263=AXIS2_PLACEMENT_3D('',#76512,#36204,#36205);
#29264=AXIS2_PLACEMENT_3D('',#76516,#36208,#36209);
#29265=AXIS2_PLACEMENT_3D('',#76517,#36210,#36211);
#29266=AXIS2_PLACEMENT_3D('',#76518,#36212,#36213);
#29267=AXIS2_PLACEMENT_3D('',#76527,#36218,#36219);
#29268=AXIS2_PLACEMENT_3D('',#76529,#36220,#36221);
#29269=AXIS2_PLACEMENT_3D('',#76531,#36223,#36224);
#29270=AXIS2_PLACEMENT_3D('',#76535,#36227,#36228);
#29271=AXIS2_PLACEMENT_3D('',#76536,#36229,#36230);
#29272=AXIS2_PLACEMENT_3D('',#76537,#36231,#36232);
#29273=AXIS2_PLACEMENT_3D('',#76539,#36233,#36234);
#29274=AXIS2_PLACEMENT_3D('',#76540,#36235,#36236);
#29275=AXIS2_PLACEMENT_3D('',#76542,#36238,#36239);
#29276=AXIS2_PLACEMENT_3D('',#76544,#36240,#36241);
#29277=AXIS2_PLACEMENT_3D('',#76546,#36243,#36244);
#29278=AXIS2_PLACEMENT_3D('',#76547,#36245,#36246);
#29279=AXIS2_PLACEMENT_3D('',#76548,#36247,#36248);
#29280=AXIS2_PLACEMENT_3D('',#76549,#36249,#36250);
#29281=AXIS2_PLACEMENT_3D('',#76550,#36251,#36252);
#29282=AXIS2_PLACEMENT_3D('',#76551,#36253,#36254);
#29283=AXIS2_PLACEMENT_3D('',#76552,#36255,#36256);
#29284=AXIS2_PLACEMENT_3D('',#76553,#36257,#36258);
#29285=AXIS2_PLACEMENT_3D('',#76554,#36259,#36260);
#29286=AXIS2_PLACEMENT_3D('',#76555,#36261,#36262);
#29287=AXIS2_PLACEMENT_3D('',#76556,#36263,#36264);
#29288=AXIS2_PLACEMENT_3D('',#76557,#36265,#36266);
#29289=AXIS2_PLACEMENT_3D('',#76558,#36267,#36268);
#29290=AXIS2_PLACEMENT_3D('',#76559,#36269,#36270);
#29291=AXIS2_PLACEMENT_3D('',#76560,#36271,#36272);
#29292=AXIS2_PLACEMENT_3D('',#76561,#36273,#36274);
#29293=AXIS2_PLACEMENT_3D('',#76562,#36275,#36276);
#29294=AXIS2_PLACEMENT_3D('',#76564,#36278,#36279);
#29295=AXIS2_PLACEMENT_3D('',#76565,#36280,#36281);
#29296=AXIS2_PLACEMENT_3D('',#76566,#36282,#36283);
#29297=AXIS2_PLACEMENT_3D('',#76567,#36284,#36285);
#29298=AXIS2_PLACEMENT_3D('',#76568,#36286,#36287);
#29299=AXIS2_PLACEMENT_3D('',#76569,#36288,#36289);
#29300=AXIS2_PLACEMENT_3D('',#76570,#36290,#36291);
#29301=AXIS2_PLACEMENT_3D('',#76571,#36292,#36293);
#29302=AXIS2_PLACEMENT_3D('',#76572,#36294,#36295);
#29303=AXIS2_PLACEMENT_3D('',#76573,#36296,#36297);
#29304=AXIS2_PLACEMENT_3D('',#76574,#36298,#36299);
#29305=AXIS2_PLACEMENT_3D('',#76575,#36300,#36301);
#29306=AXIS2_PLACEMENT_3D('',#76576,#36302,#36303);
#29307=AXIS2_PLACEMENT_3D('',#76577,#36304,#36305);
#29308=AXIS2_PLACEMENT_3D('',#76578,#36306,#36307);
#29309=AXIS2_PLACEMENT_3D('',#76579,#36308,#36309);
#29310=AXIS2_PLACEMENT_3D('',#76580,#36310,#36311);
#29311=AXIS2_PLACEMENT_3D('',#76581,#36312,#36313);
#29312=AXIS2_PLACEMENT_3D('',#76582,#36314,#36315);
#29313=AXIS2_PLACEMENT_3D('',#76583,#36316,#36317);
#29314=AXIS2_PLACEMENT_3D('',#76584,#36318,#36319);
#29315=AXIS2_PLACEMENT_3D('',#76586,#36320,#36321);
#29316=AXIS2_PLACEMENT_3D('',#76588,#36323,#36324);
#35333=DIRECTION('axis',(0.,0.,1.));
#35334=DIRECTION('refdir',(1.,0.,0.));
#35335=DIRECTION('center_axis',(0.,0.,1.));
#35336=DIRECTION('ref_axis',(1.,0.,0.));
#35337=DIRECTION('',(0.,0.,-1.));
#35338=DIRECTION('center_axis',(0.,0.,1.));
#35339=DIRECTION('ref_axis',(1.,0.,0.));
#35340=DIRECTION('center_axis',(0.,0.,1.));
#35341=DIRECTION('ref_axis',(1.,0.,0.));
#35342=DIRECTION('',(0.,0.,-1.));
#35343=DIRECTION('center_axis',(0.,0.,1.));
#35344=DIRECTION('ref_axis',(1.,0.,0.));
#35345=DIRECTION('',(0.,0.,-1.));
#35346=DIRECTION('center_axis',(0.,0.,1.));
#35347=DIRECTION('ref_axis',(1.,0.,0.));
#35348=DIRECTION('',(0.,0.,-1.));
#35349=DIRECTION('center_axis',(0.,0.,1.));
#35350=DIRECTION('ref_axis',(1.,0.,0.));
#35351=DIRECTION('',(0.,0.,-1.));
#35352=DIRECTION('center_axis',(0.,0.,1.));
#35353=DIRECTION('ref_axis',(1.,0.,0.));
#35354=DIRECTION('',(0.,0.,-1.));
#35355=DIRECTION('center_axis',(0.,0.,1.));
#35356=DIRECTION('ref_axis',(1.,0.,0.));
#35357=DIRECTION('',(0.,0.,-1.));
#35358=DIRECTION('center_axis',(0.,0.,1.));
#35359=DIRECTION('ref_axis',(1.,0.,0.));
#35360=DIRECTION('',(0.,0.,-1.));
#35361=DIRECTION('center_axis',(0.,0.,1.));
#35362=DIRECTION('ref_axis',(1.,0.,0.));
#35363=DIRECTION('',(0.,0.,-1.));
#35364=DIRECTION('center_axis',(0.,0.,1.));
#35365=DIRECTION('ref_axis',(1.,0.,0.));
#35366=DIRECTION('',(0.,0.,-1.));
#35367=DIRECTION('center_axis',(0.,0.,1.));
#35368=DIRECTION('ref_axis',(1.,0.,0.));
#35369=DIRECTION('',(0.,0.,-1.));
#35370=DIRECTION('center_axis',(0.,0.,1.));
#35371=DIRECTION('ref_axis',(1.,0.,0.));
#35372=DIRECTION('',(0.,0.,-1.));
#35373=DIRECTION('center_axis',(0.,0.,1.));
#35374=DIRECTION('ref_axis',(1.,0.,0.));
#35375=DIRECTION('',(0.,0.,-1.));
#35376=DIRECTION('center_axis',(0.,0.,1.));
#35377=DIRECTION('ref_axis',(1.,0.,0.));
#35378=DIRECTION('',(0.,0.,-1.));
#35379=DIRECTION('center_axis',(0.,0.,1.));
#35380=DIRECTION('ref_axis',(1.,0.,0.));
#35381=DIRECTION('',(0.,0.,-1.));
#35382=DIRECTION('center_axis',(0.,0.,1.));
#35383=DIRECTION('ref_axis',(1.,0.,0.));
#35384=DIRECTION('',(0.,0.,-1.));
#35385=DIRECTION('center_axis',(0.,0.,1.));
#35386=DIRECTION('ref_axis',(1.,0.,0.));
#35387=DIRECTION('',(0.,0.,-1.));
#35388=DIRECTION('center_axis',(0.,0.,1.));
#35389=DIRECTION('ref_axis',(1.,0.,0.));
#35390=DIRECTION('',(0.,0.,-1.));
#35391=DIRECTION('center_axis',(0.,0.,1.));
#35392=DIRECTION('ref_axis',(1.,0.,0.));
#35393=DIRECTION('',(0.,0.,-1.));
#35394=DIRECTION('center_axis',(0.,0.,1.));
#35395=DIRECTION('ref_axis',(1.,0.,0.));
#35396=DIRECTION('',(0.,0.,-1.));
#35397=DIRECTION('center_axis',(0.,0.,1.));
#35398=DIRECTION('ref_axis',(1.,0.,0.));
#35399=DIRECTION('center_axis',(0.,0.,1.));
#35400=DIRECTION('ref_axis',(0.472251364843622,-0.881463923483733,0.));
#35401=DIRECTION('',(0.,0.,1.));
#35402=DIRECTION('center_axis',(0.,0.,1.));
#35403=DIRECTION('ref_axis',(1.,9.72557910080329E-14,0.));
#35404=DIRECTION('center_axis',(0.,0.,1.));
#35405=DIRECTION('ref_axis',(1.,9.72557910080329E-14,0.));
#35406=DIRECTION('',(0.,0.,1.));
#35407=DIRECTION('center_axis',(0.,0.,1.));
#35408=DIRECTION('ref_axis',(1.,9.72557910080329E-14,0.));
#35409=DIRECTION('',(0.,0.,1.));
#35410=DIRECTION('center_axis',(0.,0.,1.));
#35411=DIRECTION('ref_axis',(1.,9.72557910080329E-14,0.));
#35412=DIRECTION('',(0.,0.,1.));
#35413=DIRECTION('center_axis',(0.,0.,1.));
#35414=DIRECTION('ref_axis',(1.,9.72557910080329E-14,0.));
#35415=DIRECTION('',(0.,0.,1.));
#35416=DIRECTION('center_axis',(0.,0.,1.));
#35417=DIRECTION('ref_axis',(1.,9.72557910080329E-14,0.));
#35418=DIRECTION('',(0.,0.,1.));
#35419=DIRECTION('center_axis',(0.,0.,1.));
#35420=DIRECTION('ref_axis',(1.,9.72557910080329E-14,0.));
#35421=DIRECTION('',(0.,0.,1.));
#35422=DIRECTION('center_axis',(0.,0.,1.));
#35423=DIRECTION('ref_axis',(1.,9.72557910080329E-14,0.));
#35424=DIRECTION('',(0.,0.,1.));
#35425=DIRECTION('center_axis',(0.,0.,1.));
#35426=DIRECTION('ref_axis',(1.,9.72557910080329E-14,0.));
#35427=DIRECTION('',(0.,0.,1.));
#35428=DIRECTION('center_axis',(0.,0.,1.));
#35429=DIRECTION('ref_axis',(1.,9.72557910080329E-14,0.));
#35430=DIRECTION('',(0.,0.,1.));
#35431=DIRECTION('center_axis',(0.,0.,1.));
#35432=DIRECTION('ref_axis',(1.,9.72557910080329E-14,0.));
#35433=DIRECTION('',(0.,0.,1.));
#35434=DIRECTION('center_axis',(0.,0.,1.));
#35435=DIRECTION('ref_axis',(1.,9.72557910080329E-14,0.));
#35436=DIRECTION('',(0.,0.,1.));
#35437=DIRECTION('center_axis',(0.,0.,1.));
#35438=DIRECTION('ref_axis',(1.,9.72557910080329E-14,0.));
#35439=DIRECTION('',(0.,0.,1.));
#35440=DIRECTION('center_axis',(0.,0.,1.));
#35441=DIRECTION('ref_axis',(1.,9.72557910080329E-14,0.));
#35442=DIRECTION('',(0.,0.,1.));
#35443=DIRECTION('center_axis',(0.,0.,1.));
#35444=DIRECTION('ref_axis',(1.,9.72557910080329E-14,0.));
#35445=DIRECTION('',(0.,0.,1.));
#35446=DIRECTION('center_axis',(0.,0.,1.));
#35447=DIRECTION('ref_axis',(1.,9.72557910080329E-14,0.));
#35448=DIRECTION('',(0.,0.,1.));
#35449=DIRECTION('center_axis',(0.,0.,1.));
#35450=DIRECTION('ref_axis',(1.,9.72557910080329E-14,0.));
#35451=DIRECTION('',(0.,0.,1.));
#35452=DIRECTION('center_axis',(0.,0.,1.));
#35453=DIRECTION('ref_axis',(1.,9.72557910080329E-14,0.));
#35454=DIRECTION('',(0.,0.,1.));
#35455=DIRECTION('center_axis',(0.,0.,1.));
#35456=DIRECTION('ref_axis',(1.,9.72557910080329E-14,0.));
#35457=DIRECTION('',(0.,0.,1.));
#35458=DIRECTION('center_axis',(0.,0.,1.));
#35459=DIRECTION('ref_axis',(1.,0.,0.));
#35460=DIRECTION('center_axis',(0.,0.,1.));
#35461=DIRECTION('ref_axis',(1.,0.,0.));
#35462=DIRECTION('center_axis',(0.,0.,1.));
#35463=DIRECTION('ref_axis',(1.,0.,0.));
#35464=DIRECTION('center_axis',(0.,0.,1.));
#35465=DIRECTION('ref_axis',(1.,0.,0.));
#35466=DIRECTION('center_axis',(0.,0.,1.));
#35467=DIRECTION('ref_axis',(1.,0.,0.));
#35468=DIRECTION('center_axis',(0.,0.,-1.));
#35469=DIRECTION('ref_axis',(1.,9.72557910080329E-14,0.));
#35470=DIRECTION('center_axis',(0.,0.,1.));
#35471=DIRECTION('ref_axis',(1.,9.72557910080329E-14,0.));
#35472=DIRECTION('center_axis',(0.,0.,1.));
#35473=DIRECTION('ref_axis',(1.,0.,0.));
#35474=DIRECTION('center_axis',(1.22464679914735E-16,-1.,0.));
#35475=DIRECTION('ref_axis',(-1.,-1.22464679914735E-16,0.));
#35476=DIRECTION('center_axis',(0.,0.,-1.));
#35477=DIRECTION('ref_axis',(1.,0.,0.));
#35478=DIRECTION('center_axis',(0.,0.,1.));
#35479=DIRECTION('ref_axis',(1.,0.,0.));
#35480=DIRECTION('center_axis',(0.,0.,1.));
#35481=DIRECTION('ref_axis',(-0.917573945891785,-0.397565156698344,0.));
#35482=DIRECTION('center_axis',(0.,0.,-1.));
#35483=DIRECTION('ref_axis',(-1.,0.,0.));
#35484=DIRECTION('center_axis',(0.,0.,1.));
#35485=DIRECTION('ref_axis',(1.,0.,0.));
#35486=DIRECTION('center_axis',(0.,0.,1.));
#35487=DIRECTION('ref_axis',(1.,0.,0.));
#35488=DIRECTION('',(0.5,-0.866025403784439,0.));
#35489=DIRECTION('center_axis',(0.,0.,1.));
#35490=DIRECTION('ref_axis',(1.,0.,0.));
#35491=DIRECTION('center_axis',(0.,0.,1.));
#35492=DIRECTION('ref_axis',(1.,0.,0.));
#35493=DIRECTION('',(-0.5,-0.866025403784439,0.));
#35494=DIRECTION('center_axis',(0.,0.,1.));
#35495=DIRECTION('ref_axis',(1.,0.,0.));
#35496=DIRECTION('center_axis',(0.,0.,1.));
#35497=DIRECTION('ref_axis',(1.,0.,0.));
#35498=DIRECTION('',(-1.,1.92296268638356E-16,0.));
#35499=DIRECTION('center_axis',(0.,0.,1.));
#35500=DIRECTION('ref_axis',(1.,0.,0.));
#35501=DIRECTION('center_axis',(0.,0.,1.));
#35502=DIRECTION('ref_axis',(1.,0.,0.));
#35503=DIRECTION('',(-0.5,0.866025403784439,0.));
#35504=DIRECTION('center_axis',(0.,0.,1.));
#35505=DIRECTION('ref_axis',(1.,0.,0.));
#35506=DIRECTION('center_axis',(0.,0.,1.));
#35507=DIRECTION('ref_axis',(1.,0.,0.));
#35508=DIRECTION('',(0.5,0.866025403784438,0.));
#35509=DIRECTION('center_axis',(0.,0.,1.));
#35510=DIRECTION('ref_axis',(1.,0.,0.));
#35511=DIRECTION('center_axis',(0.,0.,1.));
#35512=DIRECTION('ref_axis',(1.,0.,0.));
#35513=DIRECTION('',(1.,-1.92296268638356E-16,0.));
#35514=DIRECTION('center_axis',(0.,0.,1.));
#35515=DIRECTION('ref_axis',(1.,0.,0.));
#35516=DIRECTION('center_axis',(0.,0.,1.));
#35517=DIRECTION('ref_axis',(1.,0.,0.));
#35518=DIRECTION('',(-0.857492925712544,-1.05012596676537E-16,0.514495755427527));
#35519=DIRECTION('center_axis',(0.866025403784439,0.5,0.));
#35520=DIRECTION('ref_axis',(0.5,-0.866025403784439,0.));
#35521=DIRECTION('',(0.5,-0.866025403784439,0.));
#35522=DIRECTION('',(0.,0.,-1.));
#35523=DIRECTION('',(0.,0.,-1.));
#35524=DIRECTION('center_axis',(1.92296268638356E-16,1.,0.));
#35525=DIRECTION('ref_axis',(1.,-1.92296268638356E-16,0.));
#35526=DIRECTION('',(1.,-1.92296268638356E-16,0.));
#35527=DIRECTION('',(0.,0.,-1.));
#35528=DIRECTION('center_axis',(-0.866025403784438,0.5,0.));
#35529=DIRECTION('ref_axis',(0.5,0.866025403784438,0.));
#35530=DIRECTION('',(0.5,0.866025403784438,0.));
#35531=DIRECTION('',(0.,0.,-1.));
#35532=DIRECTION('center_axis',(-0.866025403784439,-0.5,0.));
#35533=DIRECTION('ref_axis',(-0.5,0.866025403784439,0.));
#35534=DIRECTION('',(-0.5,0.866025403784439,0.));
#35535=DIRECTION('',(0.,0.,-1.));
#35536=DIRECTION('center_axis',(-1.92296268638356E-16,-1.,0.));
#35537=DIRECTION('ref_axis',(-1.,1.92296268638356E-16,0.));
#35538=DIRECTION('',(-1.,1.92296268638356E-16,0.));
#35539=DIRECTION('',(0.,0.,-1.));
#35540=DIRECTION('center_axis',(0.866025403784439,-0.5,0.));
#35541=DIRECTION('ref_axis',(-0.5,-0.866025403784439,0.));
#35542=DIRECTION('',(-0.5,-0.866025403784439,0.));
#35543=DIRECTION('center_axis',(-0.713210659190727,-0.700949752561999,0.));
#35544=DIRECTION('ref_axis',(-0.700949752561999,0.713210659190727,0.));
#35545=DIRECTION('',(0.,0.,1.));
#35546=DIRECTION('',(-0.700949752561999,0.713210659190727,0.));
#35547=DIRECTION('',(0.,0.,-1.));
#35548=DIRECTION('',(-0.700949752561999,0.713210659190727,0.));
#35549=DIRECTION('center_axis',(0.,0.,1.));
#35550=DIRECTION('ref_axis',(1.,0.,0.));
#35551=DIRECTION('center_axis',(0.,0.,1.));
#35552=DIRECTION('ref_axis',(1.,0.,0.));
#35553=DIRECTION('',(0.995401637679912,0.0957892462865752,0.));
#35554=DIRECTION('center_axis',(-0.0957892462865752,0.995401637679912,0.));
#35555=DIRECTION('ref_axis',(0.995401637679912,0.0957892462865752,0.));
#35556=DIRECTION('',(0.,0.,-1.));
#35557=DIRECTION('',(0.995401637679912,0.0957892462865752,0.));
#35558=DIRECTION('center_axis',(0.,0.,-1.));
#35559=DIRECTION('ref_axis',(-1.,0.,0.));
#35560=DIRECTION('center_axis',(0.,0.,-1.));
#35561=DIRECTION('ref_axis',(1.,0.,0.));
#35562=DIRECTION('center_axis',(-0.909937728342724,-0.414744898146418,0.));
#35563=DIRECTION('ref_axis',(-0.414744898146418,0.909937728342724,0.));
#35564=DIRECTION('',(0.,0.,1.));
#35565=DIRECTION('',(-0.414744898146418,0.909937728342724,0.));
#35566=DIRECTION('',(0.,0.,-1.));
#35567=DIRECTION('',(-0.414744898146418,0.909937728342724,0.));
#35568=DIRECTION('center_axis',(0.,0.,1.));
#35569=DIRECTION('ref_axis',(1.,0.,0.));
#35570=DIRECTION('center_axis',(0.,0.,1.));
#35571=DIRECTION('ref_axis',(1.,0.,0.));
#35572=DIRECTION('',(0.968133425390015,-0.250434962899744,0.));
#35573=DIRECTION('center_axis',(0.250434962899744,0.968133425390015,0.));
#35574=DIRECTION('ref_axis',(0.968133425390015,-0.250434962899744,0.));
#35575=DIRECTION('',(0.,0.,-1.));
#35576=DIRECTION('',(0.968133425390015,-0.250434962899744,0.));
#35577=DIRECTION('center_axis',(0.,0.,-1.));
#35578=DIRECTION('ref_axis',(-1.,0.,0.));
#35579=DIRECTION('center_axis',(0.,0.,-1.));
#35580=DIRECTION('ref_axis',(1.,0.,0.));
#35581=DIRECTION('center_axis',(-0.996912878205979,-0.0785156880315736,
0.));
#35582=DIRECTION('ref_axis',(-0.0785156880315736,0.996912878205979,0.));
#35583=DIRECTION('',(0.,0.,1.));
#35584=DIRECTION('',(-0.0785156880315736,0.996912878205979,0.));
#35585=DIRECTION('',(0.,0.,-1.));
#35586=DIRECTION('',(-0.0785156880315736,0.996912878205979,0.));
#35587=DIRECTION('center_axis',(0.,0.,1.));
#35588=DIRECTION('ref_axis',(1.,0.,0.));
#35589=DIRECTION('center_axis',(0.,0.,1.));
#35590=DIRECTION('ref_axis',(1.,0.,0.));
#35591=DIRECTION('',(0.824094033870449,-0.566453019533952,0.));
#35592=DIRECTION('center_axis',(0.566453019533952,0.824094033870449,0.));
#35593=DIRECTION('ref_axis',(0.824094033870449,-0.566453019533952,0.));
#35594=DIRECTION('',(0.,0.,-1.));
#35595=DIRECTION('',(0.824094033870449,-0.566453019533952,0.));
#35596=DIRECTION('center_axis',(0.,0.,-1.));
#35597=DIRECTION('ref_axis',(-1.,0.,0.));
#35598=DIRECTION('center_axis',(0.,0.,-1.));
#35599=DIRECTION('ref_axis',(1.,0.,0.));
#35600=DIRECTION('center_axis',(-0.963645622090473,0.26718367282801,0.));
#35601=DIRECTION('ref_axis',(0.26718367282801,0.963645622090473,0.));
#35602=DIRECTION('',(0.,0.,1.));
#35603=DIRECTION('',(0.26718367282801,0.963645622090473,0.));
#35604=DIRECTION('',(0.,0.,-1.));
#35605=DIRECTION('',(0.26718367282801,0.963645622090473,0.));
#35606=DIRECTION('center_axis',(0.,0.,1.));
#35607=DIRECTION('ref_axis',(1.,0.,0.));
#35608=DIRECTION('center_axis',(0.,0.,1.));
#35609=DIRECTION('ref_axis',(1.,0.,0.));
#35610=DIRECTION('',(0.580656739533499,-0.814148482056146,0.));
#35611=DIRECTION('center_axis',(0.814148482056146,0.580656739533499,0.));
#35612=DIRECTION('ref_axis',(0.580656739533499,-0.814148482056146,0.));
#35613=DIRECTION('',(0.,0.,-1.));
#35614=DIRECTION('',(0.580656739533499,-0.814148482056146,0.));
#35615=DIRECTION('center_axis',(0.,0.,-1.));
#35616=DIRECTION('ref_axis',(-1.,0.,0.));
#35617=DIRECTION('center_axis',(0.,0.,-1.));
#35618=DIRECTION('ref_axis',(1.,0.,0.));
#35619=DIRECTION('center_axis',(-0.814148482056146,0.580656739533499,0.));
#35620=DIRECTION('ref_axis',(0.580656739533499,0.814148482056146,0.));
#35621=DIRECTION('',(0.,0.,1.));
#35622=DIRECTION('',(0.580656739533499,0.814148482056146,0.));
#35623=DIRECTION('',(0.,0.,-1.));
#35624=DIRECTION('',(0.580656739533499,0.814148482056146,0.));
#35625=DIRECTION('center_axis',(0.,0.,1.));
#35626=DIRECTION('ref_axis',(1.,0.,0.));
#35627=DIRECTION('center_axis',(0.,0.,1.));
#35628=DIRECTION('ref_axis',(1.,0.,0.));
#35629=DIRECTION('',(0.267183672828016,-0.963645622090472,0.));
#35630=DIRECTION('center_axis',(0.963645622090472,0.267183672828016,0.));
#35631=DIRECTION('ref_axis',(0.267183672828016,-0.963645622090472,0.));
#35632=DIRECTION('',(0.,0.,-1.));
#35633=DIRECTION('',(0.267183672828016,-0.963645622090472,0.));
#35634=DIRECTION('center_axis',(0.,0.,-1.));
#35635=DIRECTION('ref_axis',(-1.,0.,0.));
#35636=DIRECTION('center_axis',(0.,0.,-1.));
#35637=DIRECTION('ref_axis',(1.,0.,0.));
#35638=DIRECTION('center_axis',(-0.56645301953395,0.82409403387045,0.));
#35639=DIRECTION('ref_axis',(0.82409403387045,0.56645301953395,0.));
#35640=DIRECTION('',(0.,0.,1.));
#35641=DIRECTION('',(0.82409403387045,0.56645301953395,0.));
#35642=DIRECTION('',(0.,0.,-1.));
#35643=DIRECTION('',(0.82409403387045,0.56645301953395,0.));
#35644=DIRECTION('center_axis',(0.,0.,1.));
#35645=DIRECTION('ref_axis',(1.,0.,0.));
#35646=DIRECTION('center_axis',(0.,0.,1.));
#35647=DIRECTION('ref_axis',(1.,0.,0.));
#35648=DIRECTION('',(-0.0785156880315734,-0.996912878205979,0.));
#35649=DIRECTION('center_axis',(0.996912878205979,-0.0785156880315734,0.));
#35650=DIRECTION('ref_axis',(-0.0785156880315734,-0.996912878205979,0.));
#35651=DIRECTION('',(0.,0.,-1.));
#35652=DIRECTION('',(-0.0785156880315734,-0.996912878205979,0.));
#35653=DIRECTION('center_axis',(0.,0.,-1.));
#35654=DIRECTION('ref_axis',(-1.,0.,0.));
#35655=DIRECTION('center_axis',(0.,0.,-1.));
#35656=DIRECTION('ref_axis',(1.,0.,0.));
#35657=DIRECTION('center_axis',(-0.250434962899748,0.968133425390014,0.));
#35658=DIRECTION('ref_axis',(0.968133425390014,0.250434962899748,0.));
#35659=DIRECTION('',(0.,0.,1.));
#35660=DIRECTION('',(0.968133425390014,0.250434962899748,0.));
#35661=DIRECTION('',(0.,0.,-1.));
#35662=DIRECTION('',(0.968133425390014,0.250434962899748,0.));
#35663=DIRECTION('center_axis',(0.,0.,1.));
#35664=DIRECTION('ref_axis',(1.,0.,0.));
#35665=DIRECTION('center_axis',(0.,0.,1.));
#35666=DIRECTION('ref_axis',(1.,0.,0.));
#35667=DIRECTION('',(-0.414744898146415,-0.909937728342726,0.));
#35668=DIRECTION('center_axis',(0.909937728342726,-0.414744898146415,0.));
#35669=DIRECTION('ref_axis',(-0.414744898146415,-0.909937728342726,0.));
#35670=DIRECTION('',(0.,0.,-1.));
#35671=DIRECTION('',(-0.414744898146415,-0.909937728342726,0.));
#35672=DIRECTION('center_axis',(0.,0.,-1.));
#35673=DIRECTION('ref_axis',(-1.,0.,0.));
#35674=DIRECTION('center_axis',(0.,0.,-1.));
#35675=DIRECTION('ref_axis',(1.,0.,0.));
#35676=DIRECTION('center_axis',(0.0957892462865784,0.995401637679911,0.));
#35677=DIRECTION('ref_axis',(0.995401637679911,-0.0957892462865784,0.));
#35678=DIRECTION('',(0.,0.,1.));
#35679=DIRECTION('',(0.995401637679911,-0.0957892462865784,0.));
#35680=DIRECTION('',(0.,0.,-1.));
#35681=DIRECTION('',(0.995401637679911,-0.0957892462865784,0.));
#35682=DIRECTION('center_axis',(0.,0.,1.));
#35683=DIRECTION('ref_axis',(1.,0.,0.));
#35684=DIRECTION('center_axis',(0.,0.,1.));
#35685=DIRECTION('ref_axis',(1.,0.,0.));
#35686=DIRECTION('',(-0.700949752562001,-0.713210659190726,0.));
#35687=DIRECTION('center_axis',(0.713210659190726,-0.700949752562001,0.));
#35688=DIRECTION('ref_axis',(-0.700949752562001,-0.713210659190726,0.));
#35689=DIRECTION('',(0.,0.,-1.));
#35690=DIRECTION('',(-0.700949752562001,-0.713210659190726,0.));
#35691=DIRECTION('center_axis',(0.,0.,-1.));
#35692=DIRECTION('ref_axis',(-1.,0.,0.));
#35693=DIRECTION('center_axis',(0.,0.,-1.));
#35694=DIRECTION('ref_axis',(1.,0.,0.));
#35695=DIRECTION('center_axis',(0.43045985867203,0.902609721902028,0.));
#35696=DIRECTION('ref_axis',(0.902609721902028,-0.43045985867203,0.));
#35697=DIRECTION('',(0.,0.,1.));
#35698=DIRECTION('',(0.902609721902028,-0.43045985867203,0.));
#35699=DIRECTION('',(0.,0.,-1.));
#35700=DIRECTION('',(0.902609721902028,-0.43045985867203,0.));
#35701=DIRECTION('center_axis',(0.,0.,1.));
#35702=DIRECTION('ref_axis',(1.,0.,0.));
#35703=DIRECTION('center_axis',(0.,0.,1.));
#35704=DIRECTION('ref_axis',(1.,0.,0.));
#35705=DIRECTION('',(-0.902609721902028,-0.43045985867203,0.));
#35706=DIRECTION('center_axis',(0.,0.,1.));
#35707=DIRECTION('ref_axis',(1.,0.,0.));
#35708=DIRECTION('center_axis',(0.43045985867203,-0.902609721902028,0.));
#35709=DIRECTION('ref_axis',(-0.902609721902028,-0.43045985867203,0.));
#35710=DIRECTION('',(0.,0.,-1.));
#35711=DIRECTION('',(-0.902609721902028,-0.43045985867203,0.));
#35712=DIRECTION('center_axis',(0.,0.,-1.));
#35713=DIRECTION('ref_axis',(-1.,0.,0.));
#35714=DIRECTION('center_axis',(0.,0.,-1.));
#35715=DIRECTION('ref_axis',(1.,0.,0.));
#35716=DIRECTION('center_axis',(0.,0.,-1.));
#35717=DIRECTION('ref_axis',(1.,0.,0.));
#35718=DIRECTION('center_axis',(0.580656739533499,0.814148482056146,0.));
#35719=DIRECTION('ref_axis',(0.814148482056146,-0.580656739533499,0.));
#35720=DIRECTION('',(0.,0.,1.));
#35721=DIRECTION('',(0.814148482056146,-0.580656739533499,0.));
#35722=DIRECTION('',(0.,0.,-1.));
#35723=DIRECTION('',(0.814148482056146,-0.580656739533499,0.));
#35724=DIRECTION('center_axis',(0.,0.,1.));
#35725=DIRECTION('ref_axis',(1.,0.,0.));
#35726=DIRECTION('center_axis',(0.,0.,1.));
#35727=DIRECTION('ref_axis',(1.,0.,0.));
#35728=DIRECTION('',(-0.963645622090472,-0.267183672828013,0.));
#35729=DIRECTION('center_axis',(0.267183672828013,-0.963645622090472,0.));
#35730=DIRECTION('ref_axis',(-0.963645622090472,-0.267183672828013,0.));
#35731=DIRECTION('',(0.,0.,-1.));
#35732=DIRECTION('',(-0.963645622090472,-0.267183672828013,0.));
#35733=DIRECTION('center_axis',(0.,0.,-1.));
#35734=DIRECTION('ref_axis',(-1.,0.,0.));
#35735=DIRECTION('center_axis',(0.,0.,-1.));
#35736=DIRECTION('ref_axis',(1.,0.,0.));
#35737=DIRECTION('center_axis',(0.824094033870453,0.566453019533945,0.));
#35738=DIRECTION('ref_axis',(0.566453019533945,-0.824094033870453,0.));
#35739=DIRECTION('',(0.,0.,1.));
#35740=DIRECTION('',(0.566453019533945,-0.824094033870453,0.));
#35741=DIRECTION('',(0.,0.,-1.));
#35742=DIRECTION('',(0.566453019533945,-0.824094033870453,0.));
#35743=DIRECTION('center_axis',(0.,0.,1.));
#35744=DIRECTION('ref_axis',(1.,0.,0.));
#35745=DIRECTION('center_axis',(0.,0.,1.));
#35746=DIRECTION('ref_axis',(1.,0.,0.));
#35747=DIRECTION('',(-0.996912878205979,0.078515688031577,0.));
#35748=DIRECTION('center_axis',(-0.078515688031577,-0.996912878205979,0.));
#35749=DIRECTION('ref_axis',(-0.996912878205979,0.078515688031577,0.));
#35750=DIRECTION('',(0.,0.,-1.));
#35751=DIRECTION('',(-0.996912878205979,0.078515688031577,0.));
#35752=DIRECTION('center_axis',(0.,0.,-1.));
#35753=DIRECTION('ref_axis',(-1.,0.,0.));
#35754=DIRECTION('center_axis',(0.,0.,-1.));
#35755=DIRECTION('ref_axis',(1.,0.,0.));
#35756=DIRECTION('center_axis',(0.968133425390014,0.250434962899747,0.));
#35757=DIRECTION('ref_axis',(0.250434962899747,-0.968133425390014,0.));
#35758=DIRECTION('',(0.,0.,1.));
#35759=DIRECTION('',(0.250434962899747,-0.968133425390014,0.));
#35760=DIRECTION('',(0.,0.,-1.));
#35761=DIRECTION('',(0.250434962899747,-0.968133425390014,0.));
#35762=DIRECTION('center_axis',(0.,0.,1.));
#35763=DIRECTION('ref_axis',(1.,0.,0.));
#35764=DIRECTION('center_axis',(0.,0.,1.));
#35765=DIRECTION('ref_axis',(1.,0.,0.));
#35766=DIRECTION('',(-0.909937728342725,0.414744898146415,0.));
#35767=DIRECTION('center_axis',(-0.414744898146415,-0.909937728342725,0.));
#35768=DIRECTION('ref_axis',(-0.909937728342725,0.414744898146415,0.));
#35769=DIRECTION('',(0.,0.,-1.));
#35770=DIRECTION('',(-0.909937728342725,0.414744898146415,0.));
#35771=DIRECTION('center_axis',(0.,0.,-1.));
#35772=DIRECTION('ref_axis',(-1.,0.,0.));
#35773=DIRECTION('center_axis',(0.,0.,-1.));
#35774=DIRECTION('ref_axis',(1.,0.,0.));
#35775=DIRECTION('center_axis',(0.995401637679911,-0.0957892462865797,0.));
#35776=DIRECTION('ref_axis',(-0.0957892462865797,-0.995401637679911,0.));
#35777=DIRECTION('',(0.,0.,1.));
#35778=DIRECTION('',(-0.0957892462865797,-0.995401637679911,0.));
#35779=DIRECTION('',(0.,0.,-1.));
#35780=DIRECTION('',(-0.0957892462865797,-0.995401637679911,0.));
#35781=DIRECTION('center_axis',(0.,0.,1.));
#35782=DIRECTION('ref_axis',(1.,0.,0.));
#35783=DIRECTION('center_axis',(0.,0.,1.));
#35784=DIRECTION('ref_axis',(1.,0.,0.));
#35785=DIRECTION('',(-0.713210659190727,0.700949752562,0.));
#35786=DIRECTION('center_axis',(-0.700949752562,-0.713210659190727,0.));
#35787=DIRECTION('ref_axis',(-0.713210659190727,0.700949752562,0.));
#35788=DIRECTION('',(0.,0.,-1.));
#35789=DIRECTION('',(-0.713210659190727,0.700949752562,0.));
#35790=DIRECTION('center_axis',(0.,0.,-1.));
#35791=DIRECTION('ref_axis',(-1.,0.,0.));
#35792=DIRECTION('center_axis',(0.,0.,-1.));
#35793=DIRECTION('ref_axis',(1.,0.,0.));
#35794=DIRECTION('center_axis',(0.902609721902027,-0.430459858672031,0.));
#35795=DIRECTION('ref_axis',(-0.430459858672031,-0.902609721902027,0.));
#35796=DIRECTION('',(0.,0.,1.));
#35797=DIRECTION('',(-0.430459858672031,-0.902609721902027,0.));
#35798=DIRECTION('',(0.,0.,-1.));
#35799=DIRECTION('',(-0.430459858672031,-0.902609721902027,0.));
#35800=DIRECTION('center_axis',(0.,0.,1.));
#35801=DIRECTION('ref_axis',(1.,0.,0.));
#35802=DIRECTION('center_axis',(0.,0.,1.));
#35803=DIRECTION('ref_axis',(1.,0.,0.));
#35804=DIRECTION('',(-0.430459858672031,0.902609721902027,0.));
#35805=DIRECTION('center_axis',(-0.902609721902027,-0.430459858672031,0.));
#35806=DIRECTION('ref_axis',(-0.430459858672031,0.902609721902027,0.));
#35807=DIRECTION('',(0.,0.,-1.));
#35808=DIRECTION('',(-0.430459858672031,0.902609721902027,0.));
#35809=DIRECTION('center_axis',(0.,0.,-1.));
#35810=DIRECTION('ref_axis',(-1.,0.,0.));
#35811=DIRECTION('center_axis',(0.,0.,-1.));
#35812=DIRECTION('ref_axis',(1.,0.,0.));
#35813=DIRECTION('center_axis',(0.700949752562001,-0.713210659190726,0.));
#35814=DIRECTION('ref_axis',(-0.713210659190726,-0.700949752562001,0.));
#35815=DIRECTION('',(0.,0.,1.));
#35816=DIRECTION('',(-0.713210659190726,-0.700949752562001,0.));
#35817=DIRECTION('',(0.,0.,-1.));
#35818=DIRECTION('',(-0.713210659190726,-0.700949752562001,0.));
#35819=DIRECTION('center_axis',(0.,0.,1.));
#35820=DIRECTION('ref_axis',(1.,0.,0.));
#35821=DIRECTION('center_axis',(0.,0.,1.));
#35822=DIRECTION('ref_axis',(1.,0.,0.));
#35823=DIRECTION('',(-0.0957892462865797,0.995401637679911,0.));
#35824=DIRECTION('center_axis',(-0.995401637679911,-0.0957892462865797,
0.));
#35825=DIRECTION('ref_axis',(-0.0957892462865797,0.995401637679911,0.));
#35826=DIRECTION('',(0.,0.,-1.));
#35827=DIRECTION('',(-0.0957892462865797,0.995401637679911,0.));
#35828=DIRECTION('center_axis',(0.,0.,-1.));
#35829=DIRECTION('ref_axis',(-1.,0.,0.));
#35830=DIRECTION('center_axis',(0.,0.,-1.));
#35831=DIRECTION('ref_axis',(1.,0.,0.));
#35832=DIRECTION('center_axis',(0.414744898146414,-0.909937728342726,0.));
#35833=DIRECTION('ref_axis',(-0.909937728342726,-0.414744898146414,0.));
#35834=DIRECTION('',(0.,0.,1.));
#35835=DIRECTION('',(-0.909937728342726,-0.414744898146414,0.));
#35836=DIRECTION('',(0.,0.,-1.));
#35837=DIRECTION('',(-0.909937728342726,-0.414744898146414,0.));
#35838=DIRECTION('center_axis',(0.,0.,1.));
#35839=DIRECTION('ref_axis',(1.,0.,0.));
#35840=DIRECTION('center_axis',(0.,0.,1.));
#35841=DIRECTION('ref_axis',(1.,0.,0.));
#35842=DIRECTION('',(0.250434962899747,0.968133425390014,0.));
#35843=DIRECTION('center_axis',(-0.968133425390014,0.250434962899747,0.));
#35844=DIRECTION('ref_axis',(0.250434962899747,0.968133425390014,0.));
#35845=DIRECTION('',(0.,0.,-1.));
#35846=DIRECTION('',(0.250434962899747,0.968133425390014,0.));
#35847=DIRECTION('center_axis',(0.,0.,-1.));
#35848=DIRECTION('ref_axis',(-1.,0.,0.));
#35849=DIRECTION('center_axis',(0.,0.,-1.));
#35850=DIRECTION('ref_axis',(1.,0.,0.));
#35851=DIRECTION('center_axis',(0.078515688031576,-0.996912878205979,0.));
#35852=DIRECTION('ref_axis',(-0.996912878205979,-0.078515688031576,0.));
#35853=DIRECTION('',(0.,0.,1.));
#35854=DIRECTION('',(-0.996912878205979,-0.078515688031576,0.));
#35855=DIRECTION('',(0.,0.,-1.));
#35856=DIRECTION('',(-0.996912878205979,-0.078515688031576,0.));
#35857=DIRECTION('center_axis',(0.,0.,1.));
#35858=DIRECTION('ref_axis',(1.,0.,0.));
#35859=DIRECTION('center_axis',(0.,0.,1.));
#35860=DIRECTION('ref_axis',(1.,0.,0.));
#35861=DIRECTION('',(0.566453019533946,0.824094033870453,0.));
#35862=DIRECTION('center_axis',(-0.824094033870453,0.566453019533946,0.));
#35863=DIRECTION('ref_axis',(0.566453019533946,0.824094033870453,0.));
#35864=DIRECTION('',(0.,0.,-1.));
#35865=DIRECTION('',(0.566453019533946,0.824094033870453,0.));
#35866=DIRECTION('center_axis',(0.,0.,-1.));
#35867=DIRECTION('ref_axis',(-1.,0.,0.));
#35868=DIRECTION('center_axis',(0.,0.,-1.));
#35869=DIRECTION('ref_axis',(1.,0.,0.));
#35870=DIRECTION('center_axis',(-0.267183672828014,-0.963645622090472,0.));
#35871=DIRECTION('ref_axis',(-0.963645622090472,0.267183672828014,0.));
#35872=DIRECTION('',(0.,0.,1.));
#35873=DIRECTION('',(-0.963645622090472,0.267183672828014,0.));
#35874=DIRECTION('',(0.,0.,-1.));
#35875=DIRECTION('',(-0.963645622090472,0.267183672828014,0.));
#35876=DIRECTION('center_axis',(0.,0.,1.));
#35877=DIRECTION('ref_axis',(1.,0.,0.));
#35878=DIRECTION('center_axis',(0.,0.,1.));
#35879=DIRECTION('ref_axis',(1.,0.,0.));
#35880=DIRECTION('',(0.814148482056147,0.580656739533497,0.));
#35881=DIRECTION('center_axis',(-0.580656739533497,0.814148482056147,0.));
#35882=DIRECTION('ref_axis',(0.814148482056147,0.580656739533497,0.));
#35883=DIRECTION('',(0.,0.,-1.));
#35884=DIRECTION('',(0.814148482056147,0.580656739533497,0.));
#35885=DIRECTION('center_axis',(0.,0.,-1.));
#35886=DIRECTION('ref_axis',(-1.,0.,0.));
#35887=DIRECTION('center_axis',(0.,0.,-1.));
#35888=DIRECTION('ref_axis',(1.,0.,0.));
#35889=DIRECTION('center_axis',(-0.0957892462865788,-0.995401637679911,
0.));
#35890=DIRECTION('ref_axis',(-0.995401637679911,0.0957892462865788,0.));
#35891=DIRECTION('',(0.,0.,1.));
#35892=DIRECTION('',(-0.995401637679911,0.0957892462865788,0.));
#35893=DIRECTION('',(0.,0.,-1.));
#35894=DIRECTION('',(-0.995401637679911,0.0957892462865788,0.));
#35895=DIRECTION('center_axis',(0.,0.,1.));
#35896=DIRECTION('ref_axis',(1.,0.,0.));
#35897=DIRECTION('center_axis',(0.,0.,1.));
#35898=DIRECTION('ref_axis',(1.,0.,0.));
#35899=DIRECTION('',(0.700949752562,0.713210659190726,0.));
#35900=DIRECTION('center_axis',(-0.713210659190726,0.700949752562,0.));
#35901=DIRECTION('ref_axis',(0.700949752562,0.713210659190726,0.));
#35902=DIRECTION('',(0.,0.,-1.));
#35903=DIRECTION('',(0.700949752562,0.713210659190726,0.));
#35904=DIRECTION('center_axis',(0.,0.,-1.));
#35905=DIRECTION('ref_axis',(-1.,0.,0.));
#35906=DIRECTION('center_axis',(0.,0.,-1.));
#35907=DIRECTION('ref_axis',(1.,0.,0.));
#35908=DIRECTION('center_axis',(0.250434962899746,-0.968133425390014,0.));
#35909=DIRECTION('ref_axis',(-0.968133425390014,-0.250434962899746,0.));
#35910=DIRECTION('',(0.,0.,1.));
#35911=DIRECTION('',(-0.968133425390014,-0.250434962899746,0.));
#35912=DIRECTION('',(0.,0.,-1.));
#35913=DIRECTION('',(-0.968133425390014,-0.250434962899746,0.));
#35914=DIRECTION('center_axis',(0.,0.,1.));
#35915=DIRECTION('ref_axis',(1.,0.,0.));
#35916=DIRECTION('center_axis',(0.,0.,1.));
#35917=DIRECTION('ref_axis',(1.,0.,0.));
#35918=DIRECTION('',(0.414744898146414,0.909937728342726,0.));
#35919=DIRECTION('center_axis',(-0.909937728342726,0.414744898146414,0.));
#35920=DIRECTION('ref_axis',(0.414744898146414,0.909937728342726,0.));
#35921=DIRECTION('',(0.,0.,-1.));
#35922=DIRECTION('',(0.414744898146414,0.909937728342726,0.));
#35923=DIRECTION('center_axis',(0.,0.,-1.));
#35924=DIRECTION('ref_axis',(-1.,0.,0.));
#35925=DIRECTION('center_axis',(0.,0.,-1.));
#35926=DIRECTION('ref_axis',(1.,0.,0.));
#35927=DIRECTION('center_axis',(0.566453019533948,-0.824094033870452,0.));
#35928=DIRECTION('ref_axis',(-0.824094033870452,-0.566453019533948,0.));
#35929=DIRECTION('',(0.,0.,1.));
#35930=DIRECTION('',(-0.824094033870452,-0.566453019533948,0.));
#35931=DIRECTION('',(0.,0.,-1.));
#35932=DIRECTION('',(-0.824094033870452,-0.566453019533948,0.));
#35933=DIRECTION('center_axis',(0.,0.,1.));
#35934=DIRECTION('ref_axis',(1.,0.,0.));
#35935=DIRECTION('center_axis',(0.,0.,1.));
#35936=DIRECTION('ref_axis',(1.,0.,0.));
#35937=DIRECTION('',(0.0785156880315752,0.996912878205979,0.));
#35938=DIRECTION('center_axis',(-0.996912878205979,0.0785156880315752,0.));
#35939=DIRECTION('ref_axis',(0.0785156880315752,0.996912878205979,0.));
#35940=DIRECTION('',(0.,0.,-1.));
#35941=DIRECTION('',(0.0785156880315752,0.996912878205979,0.));
#35942=DIRECTION('center_axis',(0.,0.,-1.));
#35943=DIRECTION('ref_axis',(-1.,0.,0.));
#35944=DIRECTION('center_axis',(0.,0.,-1.));
#35945=DIRECTION('ref_axis',(1.,0.,0.));
#35946=DIRECTION('center_axis',(0.814148482056148,-0.580656739533496,0.));
#35947=DIRECTION('ref_axis',(-0.580656739533496,-0.814148482056148,0.));
#35948=DIRECTION('',(0.,0.,1.));
#35949=DIRECTION('',(-0.580656739533496,-0.814148482056148,0.));
#35950=DIRECTION('',(0.,0.,-1.));
#35951=DIRECTION('',(-0.580656739533496,-0.814148482056148,0.));
#35952=DIRECTION('center_axis',(0.,0.,1.));
#35953=DIRECTION('ref_axis',(1.,0.,0.));
#35954=DIRECTION('center_axis',(0.,0.,1.));
#35955=DIRECTION('ref_axis',(1.,0.,0.));
#35956=DIRECTION('',(-0.267183672828014,0.963645622090472,0.));
#35957=DIRECTION('center_axis',(-0.963645622090472,-0.267183672828014,0.));
#35958=DIRECTION('ref_axis',(-0.267183672828014,0.963645622090472,0.));
#35959=DIRECTION('',(0.,0.,-1.));
#35960=DIRECTION('',(-0.267183672828014,0.963645622090472,0.));
#35961=DIRECTION('center_axis',(0.,0.,-1.));
#35962=DIRECTION('ref_axis',(-1.,0.,0.));
#35963=DIRECTION('center_axis',(0.,0.,-1.));
#35964=DIRECTION('ref_axis',(1.,0.,0.));
#35965=DIRECTION('center_axis',(0.963645622090472,-0.267183672828014,0.));
#35966=DIRECTION('ref_axis',(-0.267183672828014,-0.963645622090472,0.));
#35967=DIRECTION('',(0.,0.,1.));
#35968=DIRECTION('',(-0.267183672828014,-0.963645622090472,0.));
#35969=DIRECTION('',(0.,0.,-1.));
#35970=DIRECTION('',(-0.267183672828014,-0.963645622090472,0.));
#35971=DIRECTION('center_axis',(0.,0.,1.));
#35972=DIRECTION('ref_axis',(1.,0.,0.));
#35973=DIRECTION('center_axis',(0.,0.,1.));
#35974=DIRECTION('ref_axis',(1.,0.,0.));
#35975=DIRECTION('',(-0.580656739533497,0.814148482056147,0.));
#35976=DIRECTION('center_axis',(-0.814148482056147,-0.580656739533497,0.));
#35977=DIRECTION('ref_axis',(-0.580656739533497,0.814148482056147,0.));
#35978=DIRECTION('',(0.,0.,-1.));
#35979=DIRECTION('',(-0.580656739533497,0.814148482056147,0.));
#35980=DIRECTION('center_axis',(0.,0.,-1.));
#35981=DIRECTION('ref_axis',(-1.,0.,0.));
#35982=DIRECTION('center_axis',(0.,0.,-1.));
#35983=DIRECTION('ref_axis',(1.,0.,0.));
#35984=DIRECTION('center_axis',(0.996912878205979,0.078515688031576,0.));
#35985=DIRECTION('ref_axis',(0.078515688031576,-0.996912878205979,0.));
#35986=DIRECTION('',(0.,0.,1.));
#35987=DIRECTION('',(0.078515688031576,-0.996912878205979,0.));
#35988=DIRECTION('',(0.,0.,-1.));
#35989=DIRECTION('',(0.078515688031576,-0.996912878205979,0.));
#35990=DIRECTION('center_axis',(0.,0.,1.));
#35991=DIRECTION('ref_axis',(1.,0.,0.));
#35992=DIRECTION('center_axis',(0.,0.,1.));
#35993=DIRECTION('ref_axis',(1.,0.,0.));
#35994=DIRECTION('',(-0.824094033870453,0.566453019533946,0.));
#35995=DIRECTION('center_axis',(-0.566453019533946,-0.824094033870453,0.));
#35996=DIRECTION('ref_axis',(-0.824094033870453,0.566453019533946,0.));
#35997=DIRECTION('',(0.,0.,-1.));
#35998=DIRECTION('',(-0.824094033870453,0.566453019533946,0.));
#35999=DIRECTION('center_axis',(0.,0.,-1.));
#36000=DIRECTION('ref_axis',(-1.,0.,0.));
#36001=DIRECTION('center_axis',(0.,0.,-1.));
#36002=DIRECTION('ref_axis',(1.,0.,0.));
#36003=DIRECTION('center_axis',(0.909937728342726,0.414744898146415,0.));
#36004=DIRECTION('ref_axis',(0.414744898146415,-0.909937728342726,0.));
#36005=DIRECTION('',(0.,0.,1.));
#36006=DIRECTION('',(0.414744898146415,-0.909937728342726,0.));
#36007=DIRECTION('',(0.,0.,-1.));
#36008=DIRECTION('',(0.414744898146415,-0.909937728342726,0.));
#36009=DIRECTION('center_axis',(0.,0.,1.));
#36010=DIRECTION('ref_axis',(1.,0.,0.));
#36011=DIRECTION('center_axis',(0.,0.,1.));
#36012=DIRECTION('ref_axis',(1.,0.,0.));
#36013=DIRECTION('',(-0.968133425390015,0.250434962899744,0.));
#36014=DIRECTION('center_axis',(-0.250434962899744,-0.968133425390015,0.));
#36015=DIRECTION('ref_axis',(-0.968133425390015,0.250434962899744,0.));
#36016=DIRECTION('',(0.,0.,-1.));
#36017=DIRECTION('',(-0.968133425390015,0.250434962899744,0.));
#36018=DIRECTION('center_axis',(0.,0.,-1.));
#36019=DIRECTION('ref_axis',(-1.,0.,0.));
#36020=DIRECTION('center_axis',(0.,0.,-1.));
#36021=DIRECTION('ref_axis',(1.,0.,0.));
#36022=DIRECTION('center_axis',(0.713210659190726,0.700949752562001,0.));
#36023=DIRECTION('ref_axis',(0.700949752562001,-0.713210659190726,0.));
#36024=DIRECTION('',(0.,0.,1.));
#36025=DIRECTION('',(0.700949752562001,-0.713210659190726,0.));
#36026=DIRECTION('',(0.,0.,-1.));
#36027=DIRECTION('',(0.700949752562001,-0.713210659190726,0.));
#36028=DIRECTION('center_axis',(0.,0.,1.));
#36029=DIRECTION('ref_axis',(1.,0.,0.));
#36030=DIRECTION('center_axis',(0.,0.,1.));
#36031=DIRECTION('ref_axis',(1.,0.,0.));
#36032=DIRECTION('',(-0.995401637679911,-0.0957892462865814,0.));
#36033=DIRECTION('center_axis',(0.0957892462865814,-0.995401637679911,0.));
#36034=DIRECTION('ref_axis',(-0.995401637679911,-0.0957892462865814,0.));
#36035=DIRECTION('',(0.,0.,-1.));
#36036=DIRECTION('',(-0.995401637679911,-0.0957892462865814,0.));
#36037=DIRECTION('center_axis',(0.,0.,-1.));
#36038=DIRECTION('ref_axis',(-1.,0.,0.));
#36039=DIRECTION('center_axis',(0.,0.,-1.));
#36040=DIRECTION('ref_axis',(1.,0.,0.));
#36041=DIRECTION('center_axis',(0.,0.,1.));
#36042=DIRECTION('ref_axis',(1.,0.,0.));
#36043=DIRECTION('center_axis',(0.,0.,1.));
#36044=DIRECTION('ref_axis',(1.,0.,0.));
#36045=DIRECTION('',(-0.902609721902027,0.430459858672031,0.));
#36046=DIRECTION('',(0.902609721902027,0.430459858672031,0.));
#36047=DIRECTION('center_axis',(-0.430459858672031,-0.902609721902027,0.));
#36048=DIRECTION('ref_axis',(-0.902609721902027,0.430459858672031,0.));
#36049=DIRECTION('',(0.,0.,1.));
#36050=DIRECTION('',(-0.902609721902027,0.430459858672031,0.));
#36051=DIRECTION('',(0.,0.,-1.));
#36052=DIRECTION('center_axis',(-0.430459858672031,0.902609721902027,0.));
#36053=DIRECTION('ref_axis',(0.902609721902027,0.430459858672031,0.));
#36054=DIRECTION('',(0.,0.,-1.));
#36055=DIRECTION('',(0.902609721902027,0.430459858672031,0.));
#36056=DIRECTION('center_axis',(0.,0.,-1.));
#36057=DIRECTION('ref_axis',(-1.,0.,0.));
#36058=DIRECTION('center_axis',(0.,0.,-1.));
#36059=DIRECTION('ref_axis',(1.,0.,0.));
#36060=DIRECTION('center_axis',(0.267183672828015,0.963645622090472,0.));
#36061=DIRECTION('ref_axis',(0.963645622090472,-0.267183672828015,0.));
#36062=DIRECTION('',(0.,0.,1.));
#36063=DIRECTION('',(0.963645622090472,-0.267183672828015,0.));
#36064=DIRECTION('',(0.,0.,-1.));
#36065=DIRECTION('',(0.963645622090472,-0.267183672828015,0.));
#36066=DIRECTION('center_axis',(0.,0.,1.));
#36067=DIRECTION('ref_axis',(1.,0.,0.));
#36068=DIRECTION('center_axis',(0.,0.,1.));
#36069=DIRECTION('ref_axis',(1.,0.,0.));
#36070=DIRECTION('',(-0.814148482056148,-0.580656739533496,0.));
#36071=DIRECTION('center_axis',(0.580656739533496,-0.814148482056148,0.));
#36072=DIRECTION('ref_axis',(-0.814148482056148,-0.580656739533496,0.));
#36073=DIRECTION('',(0.,0.,-1.));
#36074=DIRECTION('',(-0.814148482056148,-0.580656739533496,0.));
#36075=DIRECTION('center_axis',(0.,0.,-1.));
#36076=DIRECTION('ref_axis',(-1.,0.,0.));
#36077=DIRECTION('center_axis',(0.,0.,-1.));
#36078=DIRECTION('ref_axis',(1.,0.,0.));
#36079=DIRECTION('center_axis',(-0.0785156880315738,0.996912878205979,0.));
#36080=DIRECTION('ref_axis',(0.996912878205979,0.0785156880315738,0.));
#36081=DIRECTION('',(0.,0.,1.));
#36082=DIRECTION('',(0.996912878205979,0.0785156880315738,0.));
#36083=DIRECTION('',(0.,0.,-1.));
#36084=DIRECTION('',(0.996912878205979,0.0785156880315738,0.));
#36085=DIRECTION('center_axis',(0.,0.,1.));
#36086=DIRECTION('ref_axis',(1.,0.,0.));
#36087=DIRECTION('center_axis',(0.,0.,1.));
#36088=DIRECTION('ref_axis',(1.,0.,0.));
#36089=DIRECTION('',(-0.566453019533948,-0.824094033870452,0.));
#36090=DIRECTION('center_axis',(0.824094033870452,-0.566453019533948,0.));
#36091=DIRECTION('ref_axis',(-0.566453019533948,-0.824094033870452,0.));
#36092=DIRECTION('',(0.,0.,-1.));
#36093=DIRECTION('',(-0.566453019533948,-0.824094033870452,0.));
#36094=DIRECTION('center_axis',(0.,0.,-1.));
#36095=DIRECTION('ref_axis',(-1.,0.,0.));
#36096=DIRECTION('center_axis',(0.,0.,-1.));
#36097=DIRECTION('ref_axis',(1.,0.,0.));
#36098=DIRECTION('center_axis',(-0.414744898146415,0.909937728342726,0.));
#36099=DIRECTION('ref_axis',(0.909937728342726,0.414744898146415,0.));
#36100=DIRECTION('',(0.,0.,1.));
#36101=DIRECTION('',(0.909937728342726,0.414744898146415,0.));
#36102=DIRECTION('',(0.,0.,-1.));
#36103=DIRECTION('',(0.909937728342726,0.414744898146415,0.));
#36104=DIRECTION('center_axis',(0.,0.,1.));
#36105=DIRECTION('ref_axis',(1.,0.,0.));
#36106=DIRECTION('center_axis',(0.,0.,1.));
#36107=DIRECTION('ref_axis',(1.,0.,0.));
#36108=DIRECTION('',(-0.250434962899745,-0.968133425390015,0.));
#36109=DIRECTION('center_axis',(0.968133425390015,-0.250434962899745,0.));
#36110=DIRECTION('ref_axis',(-0.250434962899745,-0.968133425390015,0.));
#36111=DIRECTION('',(0.,0.,-1.));
#36112=DIRECTION('',(-0.250434962899745,-0.968133425390015,0.));
#36113=DIRECTION('center_axis',(0.,0.,-1.));
#36114=DIRECTION('ref_axis',(-1.,0.,0.));
#36115=DIRECTION('center_axis',(0.,0.,-1.));
#36116=DIRECTION('ref_axis',(1.,0.,0.));
#36117=DIRECTION('center_axis',(-0.700949752561999,0.713210659190727,0.));
#36118=DIRECTION('ref_axis',(0.713210659190727,0.700949752561999,0.));
#36119=DIRECTION('',(0.,0.,1.));
#36120=DIRECTION('',(0.713210659190727,0.700949752561999,0.));
#36121=DIRECTION('',(0.,0.,-1.));
#36122=DIRECTION('',(0.713210659190727,0.700949752561999,0.));
#36123=DIRECTION('center_axis',(0.,0.,1.));
#36124=DIRECTION('ref_axis',(1.,0.,0.));
#36125=DIRECTION('center_axis',(0.,0.,1.));
#36126=DIRECTION('ref_axis',(1.,0.,0.));
#36127=DIRECTION('',(0.0957892462865748,-0.995401637679912,0.));
#36128=DIRECTION('center_axis',(0.995401637679912,0.0957892462865748,0.));
#36129=DIRECTION('ref_axis',(0.0957892462865748,-0.995401637679912,0.));
#36130=DIRECTION('',(0.,0.,-1.));
#36131=DIRECTION('',(0.0957892462865748,-0.995401637679912,0.));
#36132=DIRECTION('center_axis',(0.,0.,-1.));
#36133=DIRECTION('ref_axis',(-1.,0.,0.));
#36134=DIRECTION('center_axis',(0.,0.,-1.));
#36135=DIRECTION('ref_axis',(1.,0.,0.));
#36136=DIRECTION('center_axis',(-0.902609721902026,0.430459858672033,0.));
#36137=DIRECTION('ref_axis',(0.430459858672033,0.902609721902026,0.));
#36138=DIRECTION('',(0.,0.,1.));
#36139=DIRECTION('',(0.430459858672033,0.902609721902026,0.));
#36140=DIRECTION('',(0.,0.,-1.));
#36141=DIRECTION('',(0.430459858672033,0.902609721902026,0.));
#36142=DIRECTION('center_axis',(0.,0.,1.));
#36143=DIRECTION('ref_axis',(1.,0.,0.));
#36144=DIRECTION('center_axis',(0.,0.,1.));
#36145=DIRECTION('ref_axis',(1.,0.,0.));
#36146=DIRECTION('',(0.430459858672033,-0.902609721902027,0.));
#36147=DIRECTION('center_axis',(0.902609721902027,0.430459858672033,0.));
#36148=DIRECTION('ref_axis',(0.430459858672033,-0.902609721902027,0.));
#36149=DIRECTION('',(0.,0.,-1.));
#36150=DIRECTION('',(0.430459858672033,-0.902609721902027,0.));
#36151=DIRECTION('center_axis',(0.,0.,-1.));
#36152=DIRECTION('ref_axis',(-1.,0.,0.));
#36153=DIRECTION('center_axis',(0.,0.,-1.));
#36154=DIRECTION('ref_axis',(1.,0.,0.));
#36155=DIRECTION('center_axis',(-0.995401637679911,0.0957892462865809,0.));
#36156=DIRECTION('ref_axis',(0.0957892462865809,0.995401637679911,0.));
#36157=DIRECTION('',(0.,0.,1.));
#36158=DIRECTION('',(0.0957892462865809,0.995401637679911,0.));
#36159=DIRECTION('',(0.,0.,-1.));
#36160=DIRECTION('',(0.0957892462865809,0.995401637679911,0.));
#36161=DIRECTION('center_axis',(0.,0.,1.));
#36162=DIRECTION('ref_axis',(1.,0.,0.));
#36163=DIRECTION('center_axis',(0.,0.,1.));
#36164=DIRECTION('ref_axis',(1.,0.,0.));
#36165=DIRECTION('',(0.713210659190723,-0.700949752562004,0.));
#36166=DIRECTION('center_axis',(0.700949752562004,0.713210659190723,0.));
#36167=DIRECTION('ref_axis',(0.713210659190723,-0.700949752562004,0.));
#36168=DIRECTION('',(0.,0.,-1.));
#36169=DIRECTION('',(0.713210659190723,-0.700949752562004,0.));
#36170=DIRECTION('center_axis',(0.,0.,-1.));
#36171=DIRECTION('ref_axis',(-1.,0.,0.));
#36172=DIRECTION('center_axis',(0.,0.,-1.));
#36173=DIRECTION('ref_axis',(1.,0.,0.));
#36174=DIRECTION('center_axis',(-0.968133425390015,-0.250434962899744,0.));
#36175=DIRECTION('ref_axis',(-0.250434962899744,0.968133425390015,0.));
#36176=DIRECTION('',(0.,0.,1.));
#36177=DIRECTION('',(-0.250434962899744,0.968133425390015,0.));
#36178=DIRECTION('',(0.,0.,-1.));
#36179=DIRECTION('',(-0.250434962899744,0.968133425390015,0.));
#36180=DIRECTION('center_axis',(0.,0.,1.));
#36181=DIRECTION('ref_axis',(1.,0.,0.));
#36182=DIRECTION('center_axis',(0.,0.,1.));
#36183=DIRECTION('ref_axis',(1.,0.,0.));
#36184=DIRECTION('',(0.909937728342727,-0.414744898146412,0.));
#36185=DIRECTION('center_axis',(0.414744898146412,0.909937728342727,0.));
#36186=DIRECTION('ref_axis',(0.909937728342727,-0.414744898146412,0.));
#36187=DIRECTION('',(0.,0.,-1.));
#36188=DIRECTION('',(0.909937728342727,-0.414744898146412,0.));
#36189=DIRECTION('center_axis',(0.,0.,-1.));
#36190=DIRECTION('ref_axis',(-1.,0.,0.));
#36191=DIRECTION('center_axis',(0.,0.,-1.));
#36192=DIRECTION('ref_axis',(1.,0.,0.));
#36193=DIRECTION('center_axis',(-0.82409403387045,-0.56645301953395,0.));
#36194=DIRECTION('ref_axis',(-0.56645301953395,0.82409403387045,0.));
#36195=DIRECTION('',(0.,0.,1.));
#36196=DIRECTION('',(-0.56645301953395,0.82409403387045,0.));
#36197=DIRECTION('',(0.,0.,-1.));
#36198=DIRECTION('',(-0.56645301953395,0.82409403387045,0.));
#36199=DIRECTION('center_axis',(0.,0.,1.));
#36200=DIRECTION('ref_axis',(1.,0.,0.));
#36201=DIRECTION('center_axis',(0.,0.,1.));
#36202=DIRECTION('ref_axis',(1.,0.,0.));
#36203=DIRECTION('',(0.996912878205979,-0.0785156880315738,0.));
#36204=DIRECTION('center_axis',(0.0785156880315738,0.996912878205979,0.));
#36205=DIRECTION('ref_axis',(0.996912878205979,-0.0785156880315738,0.));
#36206=DIRECTION('',(0.,0.,-1.));
#36207=DIRECTION('',(0.996912878205979,-0.0785156880315738,0.));
#36208=DIRECTION('center_axis',(0.,0.,-1.));
#36209=DIRECTION('ref_axis',(-1.,0.,0.));
#36210=DIRECTION('center_axis',(0.,0.,-1.));
#36211=DIRECTION('ref_axis',(1.,0.,0.));
#36212=DIRECTION('center_axis',(-0.580656739533499,-0.814148482056146,0.));
#36213=DIRECTION('ref_axis',(-0.814148482056146,0.580656739533499,0.));
#36214=DIRECTION('',(0.,0.,1.));
#36215=DIRECTION('',(-0.814148482056146,0.580656739533499,0.));
#36216=DIRECTION('',(0.,0.,-1.));
#36217=DIRECTION('',(-0.814148482056146,0.580656739533499,0.));
#36218=DIRECTION('center_axis',(0.,0.,1.));
#36219=DIRECTION('ref_axis',(1.,0.,0.));
#36220=DIRECTION('center_axis',(0.,0.,1.));
#36221=DIRECTION('ref_axis',(1.,0.,0.));
#36222=DIRECTION('',(0.963645622090472,0.267183672828016,0.));
#36223=DIRECTION('center_axis',(-0.267183672828016,0.963645622090472,0.));
#36224=DIRECTION('ref_axis',(0.963645622090472,0.267183672828016,0.));
#36225=DIRECTION('',(0.,0.,-1.));
#36226=DIRECTION('',(0.963645622090472,0.267183672828016,0.));
#36227=DIRECTION('center_axis',(0.,0.,-1.));
#36228=DIRECTION('ref_axis',(-1.,0.,0.));
#36229=DIRECTION('center_axis',(0.,0.,-1.));
#36230=DIRECTION('ref_axis',(1.,0.,0.));
#36231=DIRECTION('center_axis',(0.,0.,-1.));
#36232=DIRECTION('ref_axis',(-1.,0.,0.));
#36233=DIRECTION('center_axis',(0.,0.,1.));
#36234=DIRECTION('ref_axis',(1.,0.,0.));
#36235=DIRECTION('center_axis',(0.,0.,1.));
#36236=DIRECTION('ref_axis',(1.,0.,0.));
#36237=DIRECTION('',(0.707106781186547,8.65956056235493E-17,-0.707106781186548));
#36238=DIRECTION('center_axis',(0.,0.,1.));
#36239=DIRECTION('ref_axis',(1.,0.,0.));
#36240=DIRECTION('center_axis',(0.,0.,1.));
#36241=DIRECTION('ref_axis',(1.,0.,0.));
#36242=DIRECTION('',(0.707106781186547,8.65956056235493E-17,-0.707106781186548));
#36243=DIRECTION('center_axis',(0.,0.,1.));
#36244=DIRECTION('ref_axis',(1.,0.,0.));
#36245=DIRECTION('center_axis',(0.,0.,1.));
#36246=DIRECTION('ref_axis',(1.,0.,0.));
#36247=DIRECTION('center_axis',(0.,0.,1.));
#36248=DIRECTION('ref_axis',(1.,0.,0.));
#36249=DIRECTION('center_axis',(0.,0.,1.));
#36250=DIRECTION('ref_axis',(1.,0.,0.));
#36251=DIRECTION('center_axis',(0.,0.,1.));
#36252=DIRECTION('ref_axis',(1.,0.,0.));
#36253=DIRECTION('center_axis',(0.,0.,1.));
#36254=DIRECTION('ref_axis',(1.,0.,0.));
#36255=DIRECTION('center_axis',(0.,0.,1.));
#36256=DIRECTION('ref_axis',(1.,0.,0.));
#36257=DIRECTION('center_axis',(0.,0.,1.));
#36258=DIRECTION('ref_axis',(1.,0.,0.));
#36259=DIRECTION('center_axis',(0.,0.,1.));
#36260=DIRECTION('ref_axis',(1.,0.,0.));
#36261=DIRECTION('center_axis',(0.,0.,1.));
#36262=DIRECTION('ref_axis',(1.,0.,0.));
#36263=DIRECTION('center_axis',(0.,0.,1.));
#36264=DIRECTION('ref_axis',(1.,0.,0.));
#36265=DIRECTION('center_axis',(0.,0.,1.));
#36266=DIRECTION('ref_axis',(1.,0.,0.));
#36267=DIRECTION('center_axis',(0.,0.,1.));
#36268=DIRECTION('ref_axis',(1.,0.,0.));
#36269=DIRECTION('center_axis',(0.,0.,1.));
#36270=DIRECTION('ref_axis',(1.,0.,0.));
#36271=DIRECTION('center_axis',(0.,0.,1.));
#36272=DIRECTION('ref_axis',(1.,0.,0.));
#36273=DIRECTION('center_axis',(0.,0.,1.));
#36274=DIRECTION('ref_axis',(1.,0.,0.));
#36275=DIRECTION('center_axis',(0.,0.,1.));
#36276=DIRECTION('ref_axis',(1.,0.,0.));
#36277=DIRECTION('',(0.,0.,-1.));
#36278=DIRECTION('center_axis',(0.,0.,1.));
#36279=DIRECTION('ref_axis',(1.,0.,0.));
#36280=DIRECTION('center_axis',(0.,0.,1.));
#36281=DIRECTION('ref_axis',(1.,0.,0.));
#36282=DIRECTION('center_axis',(0.,0.,1.));
#36283=DIRECTION('ref_axis',(1.,0.,0.));
#36284=DIRECTION('center_axis',(0.,0.,1.));
#36285=DIRECTION('ref_axis',(1.,0.,0.));
#36286=DIRECTION('center_axis',(0.,0.,1.));
#36287=DIRECTION('ref_axis',(1.,0.,0.));
#36288=DIRECTION('center_axis',(0.,0.,1.));
#36289=DIRECTION('ref_axis',(1.,0.,0.));
#36290=DIRECTION('center_axis',(0.,0.,1.));
#36291=DIRECTION('ref_axis',(1.,0.,0.));
#36292=DIRECTION('center_axis',(0.,0.,1.));
#36293=DIRECTION('ref_axis',(1.,0.,0.));
#36294=DIRECTION('center_axis',(0.,0.,1.));
#36295=DIRECTION('ref_axis',(1.,0.,0.));
#36296=DIRECTION('center_axis',(0.,0.,1.));
#36297=DIRECTION('ref_axis',(1.,0.,0.));
#36298=DIRECTION('center_axis',(0.,0.,1.));
#36299=DIRECTION('ref_axis',(1.,0.,0.));
#36300=DIRECTION('center_axis',(0.,0.,1.));
#36301=DIRECTION('ref_axis',(1.,0.,0.));
#36302=DIRECTION('center_axis',(0.,0.,1.));
#36303=DIRECTION('ref_axis',(1.,0.,0.));
#36304=DIRECTION('center_axis',(0.,0.,1.));
#36305=DIRECTION('ref_axis',(1.,0.,0.));
#36306=DIRECTION('center_axis',(0.,0.,1.));
#36307=DIRECTION('ref_axis',(1.,0.,0.));
#36308=DIRECTION('center_axis',(0.,0.,1.));
#36309=DIRECTION('ref_axis',(1.,0.,0.));
#36310=DIRECTION('center_axis',(0.,0.,1.));
#36311=DIRECTION('ref_axis',(1.,0.,0.));
#36312=DIRECTION('center_axis',(0.,0.,1.));
#36313=DIRECTION('ref_axis',(1.,0.,0.));
#36314=DIRECTION('center_axis',(0.,0.,1.));
#36315=DIRECTION('ref_axis',(1.,0.,0.));
#36316=DIRECTION('center_axis',(0.,0.,1.));
#36317=DIRECTION('ref_axis',(1.,0.,0.));
#36318=DIRECTION('center_axis',(0.,0.,-1.));
#36319=DIRECTION('ref_axis',(1.,0.,0.));
#36320=DIRECTION('center_axis',(0.,0.,1.));
#36321=DIRECTION('ref_axis',(1.,0.,0.));
#36322=DIRECTION('',(-0.707106781186548,-8.65956056235494E-17,-0.707106781186547));
#36323=DIRECTION('center_axis',(0.,0.,1.));
#36324=DIRECTION('ref_axis',(1.,0.,0.));
#73082=CARTESIAN_POINT('',(0.,0.,0.));
#73083=CARTESIAN_POINT('Origin',(0.,0.,-0.975));
#73084=CARTESIAN_POINT('',(-0.294526041752932,0.000202016893245491,-1.92358238829104));
#73085=CARTESIAN_POINT('',(-0.294462282070766,0.000314061004039186,-1.93801761170896));
#73086=CARTESIAN_POINT('',(-0.2942,-3.60291088309151E-17,-0.975));
#73087=CARTESIAN_POINT('',(0.129046731032871,0.264647125805703,-1.9558));
#73088=CARTESIAN_POINT('Ctrl Pts',(-0.294526041752932,0.000202016893245491,
-1.92358238829104));
#73089=CARTESIAN_POINT('Ctrl Pts',(-0.294606382001833,0.0112270322590358,
-1.9241807531942));
#73090=CARTESIAN_POINT('Ctrl Pts',(-0.294040815978278,0.0222432322455178,
-1.92477911809736));
#73091=CARTESIAN_POINT('Ctrl Pts',(-0.292801839103187,0.0331825365608063,
-1.92537748300052));
#73092=CARTESIAN_POINT('Ctrl Pts',(-0.281871479166624,0.129690014646629,
-1.93065630934219));
#73093=CARTESIAN_POINT('Ctrl Pts',(-0.218530096272678,0.220212764718254,
-1.93593513568386));
#73094=CARTESIAN_POINT('Ctrl Pts',(-0.131611395378181,0.263625056394311,
-1.94121396202553));
#73095=CARTESIAN_POINT('Ctrl Pts',(-0.0515557548574951,0.303609533622244,
-1.94607597468368));
#73096=CARTESIAN_POINT('Ctrl Pts',(0.0485008907872385,0.303629477151138,
-1.95093798734184));
#73097=CARTESIAN_POINT('Ctrl Pts',(0.129201276660417,0.264831693691691,
-1.9558));
#73098=CARTESIAN_POINT('',(-0.128892185405329,0.264462557919714,-1.9558));
#73099=CARTESIAN_POINT('Origin',(0.,0.,-1.9558));
#73100=CARTESIAN_POINT('Ctrl Pts',(-0.128892185405329,0.264462557919714,
-1.9558));
#73101=CARTESIAN_POINT('Ctrl Pts',(-0.216608714343133,0.221711798795636,
-1.95052117365833));
#73102=CARTESIAN_POINT('Ctrl Pts',(-0.280643579713015,0.13227595083354,
-1.94524234731666));
#73103=CARTESIAN_POINT('Ctrl Pts',(-0.292444290812177,0.0360181640441311,
-1.93996352097499));
#73104=CARTESIAN_POINT('Ctrl Pts',(-0.29389430460864,0.0241904769082657,
-1.93931488455298));
#73105=CARTESIAN_POINT('Ctrl Pts',(-0.294555671724416,0.0122597901261511,
-1.93866624813097));
#73106=CARTESIAN_POINT('Ctrl Pts',(-0.294462282070766,0.000314061004039186,
-1.93801761170896));
#73107=CARTESIAN_POINT('Origin',(0.,0.,-0.975));
#73108=CARTESIAN_POINT('',(-0.29376368569052,0.000111582411140523,-1.82358238829104));
#73109=CARTESIAN_POINT('',(-0.293753041170369,9.93547412011704E-5,-1.83801761170896));
#73110=CARTESIAN_POINT('',(-0.2942,-3.60291088309151E-17,-0.975));
#73111=CARTESIAN_POINT('Ctrl Pts',(-0.29376368569052,0.000111582411140523,
-1.82358238829104));
#73112=CARTESIAN_POINT('Ctrl Pts',(-0.293906879889716,0.0420094747863047,
-1.82584112847753));
#73113=CARTESIAN_POINT('Ctrl Pts',(-0.285536454078649,0.0838527133558878,
-1.82809986866401));
#73114=CARTESIAN_POINT('Ctrl Pts',(-0.268369615014717,0.121706567466693,
-1.8303586088505));
#73115=CARTESIAN_POINT('Ctrl Pts',(-0.22824956809826,0.210173547161576,
-1.83563743519216));
#73116=CARTESIAN_POINT('Ctrl Pts',(-0.140084563281704,0.276850985726518,
-1.84091626153383));
#73117=CARTESIAN_POINT('Ctrl Pts',(-0.0440357056638973,0.291367766871805,
-1.8461950878755));
#73118=CARTESIAN_POINT('Ctrl Pts',(0.0520131519539096,0.305884548017093,
-1.85147391421717));
#73119=CARTESIAN_POINT('Ctrl Pts',(0.155945862372967,0.268240671742726,
-1.85675274055884));
#73120=CARTESIAN_POINT('Ctrl Pts',(0.220417510035407,0.195579651961848,
-1.8620315669005));
#73121=CARTESIAN_POINT('Ctrl Pts',(0.284889157697847,0.122918632180969,
-1.86731039324217));
#73122=CARTESIAN_POINT('Ctrl Pts',(0.30989974260367,0.0152404688935781,
-1.87258921958384));
#73123=CARTESIAN_POINT('Ctrl Pts',(0.284057777716934,-0.0783963834015649,
-1.87786804592551));
#73124=CARTESIAN_POINT('Ctrl Pts',(0.258215812830198,-0.172033235696708,
-1.88314687226718));
#73125=CARTESIAN_POINT('Ctrl Pts',(0.181521298150903,-0.251628776999603,
-1.88842569860885));
#73126=CARTESIAN_POINT('Ctrl Pts',(0.0889077647329698,-0.280940720221476,
-1.89370452495051));
#73127=CARTESIAN_POINT('Ctrl Pts',(-0.00370576868496414,-0.31025266344335,
-1.89898335129218));
#73128=CARTESIAN_POINT('Ctrl Pts',(-0.112238320841537,-0.289281008584203,
-1.90426217763385));
#73129=CARTESIAN_POINT('Ctrl Pts',(-0.187244928430233,-0.227549078104619,
-1.90954100397552));
#73130=CARTESIAN_POINT('Ctrl Pts',(-0.253749395849641,-0.172814578154573,
-1.91422146541402));
#73131=CARTESIAN_POINT('Ctrl Pts',(-0.293897613456161,-0.086036596043438,
-1.91890192685253));
#73132=CARTESIAN_POINT('Ctrl Pts',(-0.294526041752932,0.000202016893245491,
-1.92358238829104));
#73133=CARTESIAN_POINT('Ctrl Pts',(-0.294462282070766,0.000314061004039186,
-1.93801761170896));
#73134=CARTESIAN_POINT('Ctrl Pts',(-0.293795634595768,-0.084958662955309,
-1.9333874217893));
#73135=CARTESIAN_POINT('Ctrl Pts',(-0.254669634955265,-0.170997883718377,
-1.92875723186965));
#73136=CARTESIAN_POINT('Ctrl Pts',(-0.189411438041069,-0.225809910607879,
-1.92412704194999));
#73137=CARTESIAN_POINT('Ctrl Pts',(-0.115011317342356,-0.288300472853751,
-1.91884821560832));
#73138=CARTESIAN_POINT('Ctrl Pts',(-0.00664451911648993,-0.310201871728771,
-1.91356938926666));
#73139=CARTESIAN_POINT('Ctrl Pts',(0.0862516754582108,-0.281745185228748,
-1.90829056292499));
#73140=CARTESIAN_POINT('Ctrl Pts',(0.179147870032911,-0.253288498728725,
-1.90301173658332));
#73141=CARTESIAN_POINT('Ctrl Pts',(0.256573460956447,-0.17447372685366,
-1.89773291024165));
#73142=CARTESIAN_POINT('Ctrl Pts',(0.283296849325839,-0.081098014509368,
-1.89245408389998));
#73143=CARTESIAN_POINT('Ctrl Pts',(0.310020237695232,0.0122776978349239,
-1.88717525755831));
#73144=CARTESIAN_POINT('Ctrl Pts',(0.286041423510481,0.120214350648442,
-1.88189643121665));
#73145=CARTESIAN_POINT('Ctrl Pts',(0.222263652174004,0.193489302525945,
-1.87661760487498));
#73146=CARTESIAN_POINT('Ctrl Pts',(0.158485880837528,0.266764254403448,
-1.87133877853331));
#73147=CARTESIAN_POINT('Ctrl Pts',(0.0549091523493268,0.305377505344936,
-1.86605995219164));
#73148=CARTESIAN_POINT('Ctrl Pts',(-0.0412742315316208,0.291768235340026,
-1.86078112584997));
#73149=CARTESIAN_POINT('Ctrl Pts',(-0.137457615412569,0.278158965335116,
-1.85550229950831));
#73150=CARTESIAN_POINT('Ctrl Pts',(-0.226247654686263,0.212327174383808,
-1.85022347316664));
#73151=CARTESIAN_POINT('Ctrl Pts',(-0.267203521977581,0.124246060006099,
-1.84494464682497));
#73152=CARTESIAN_POINT('Ctrl Pts',(-0.285118030024829,0.0857184951737815,
-1.84263563511963));
#73153=CARTESIAN_POINT('Ctrl Pts',(-0.293880542962884,0.0429340217185596,
-1.8403266234143));
#73154=CARTESIAN_POINT('Ctrl Pts',(-0.293753041170369,9.93547412011704E-5,
-1.83801761170896));
#73155=CARTESIAN_POINT('Origin',(0.,0.,-0.975));
#73156=CARTESIAN_POINT('',(-0.294128475609455,-0.000264102212364226,-1.72358238829104));
#73157=CARTESIAN_POINT('',(-0.294155870929176,-0.000265231913958952,-1.73801761170896));
#73158=CARTESIAN_POINT('',(-0.2942,-3.60291088309151E-17,-0.975));
#73159=CARTESIAN_POINT('Ctrl Pts',(-0.294128475609455,-0.000264102212364226,
-1.72358238829104));
#73160=CARTESIAN_POINT('Ctrl Pts',(-0.293485479046885,0.0722049969462197,
-1.72750150376085));
#73161=CARTESIAN_POINT('Ctrl Pts',(-0.266422153164402,0.1451034209213,-1.73142061923066));
#73162=CARTESIAN_POINT('Ctrl Pts',(-0.217860899240002,0.198422075695203,
-1.73533973470047));
#73163=CARTESIAN_POINT('Ctrl Pts',(-0.15245164340784,0.270239280748482,
-1.74061856104214));
#73164=CARTESIAN_POINT('Ctrl Pts',(-0.0480396369288832,0.306533766850134,
-1.74589738738381));
#73165=CARTESIAN_POINT('Ctrl Pts',(0.0478126679033099,0.290772471240934,
-1.75117621372547));
#73166=CARTESIAN_POINT('Ctrl Pts',(0.143664972735503,0.275011175631734,
-1.75645504006714));
#73167=CARTESIAN_POINT('Ctrl Pts',(0.230957575920933,0.207194098311682,
-1.76173386640881));
#73168=CARTESIAN_POINT('Ctrl Pts',(0.269926346425774,0.118213643233769,
-1.76701269275048));
#73169=CARTESIAN_POINT('Ctrl Pts',(0.308895116930614,0.0292331881558552,
-1.77229151909215));
#73170=CARTESIAN_POINT('Ctrl Pts',(0.299540054754865,-0.0809106446799193,
-1.77757034543381));
#73171=CARTESIAN_POINT('Ctrl Pts',(0.246122671812768,-0.162044226057869,
-1.78284917177548));
#73172=CARTESIAN_POINT('Ctrl Pts',(0.192705288870672,-0.243177807435819,
-1.78812799811715));
#73173=CARTESIAN_POINT('Ctrl Pts',(0.0952255851622282,-0.295301137355943,
-1.79340682445882));
#73174=CARTESIAN_POINT('Ctrl Pts',(-0.00191188692827236,-0.294670966749634,
-1.79868565080049));
#73175=CARTESIAN_POINT('Ctrl Pts',(-0.0990493590187724,-0.294040796143324,
-1.80396447714215));
#73176=CARTESIAN_POINT('Ctrl Pts',(-0.195844599491329,-0.24065712501058,
-1.80924330348382));
#73177=CARTESIAN_POINT('Ctrl Pts',(-0.248204675219429,-0.158837029031797,
-1.81452212982549));
#73178=CARTESIAN_POINT('Ctrl Pts',(-0.278160564948661,-0.112026673265633,
-1.81754221598067));
#73179=CARTESIAN_POINT('Ctrl Pts',(-0.293572225503517,-0.055908691833193,
-1.82056230213586));
#73180=CARTESIAN_POINT('Ctrl Pts',(-0.29376368569052,0.000111582411140523,
-1.82358238829104));
#73181=CARTESIAN_POINT('Ctrl Pts',(-0.293753041170369,9.93547412011704E-5,
-1.83801761170896));
#73182=CARTESIAN_POINT('Ctrl Pts',(-0.293589050364825,-0.0549939220220992,
-1.83504779707263));
#73183=CARTESIAN_POINT('Ctrl Pts',(-0.278718574093716,-0.110170232427766,
-1.8320779824363));
#73184=CARTESIAN_POINT('Ctrl Pts',(-0.249699027023729,-0.156478964570943,
-1.82910816779997));
#73185=CARTESIAN_POINT('Ctrl Pts',(-0.198116969469617,-0.238792436966167,
-1.8238293414583));
#73186=CARTESIAN_POINT('Ctrl Pts',(-0.101831159052452,-0.293088943952504,
-1.81855051511663));
#73187=CARTESIAN_POINT('Ctrl Pts',(-0.00470384019102898,-0.294639071818577,
-1.81327168877496));
#73188=CARTESIAN_POINT('Ctrl Pts',(0.092423478670394,-0.29618919968465,
-1.80799286243329));
#73189=CARTESIAN_POINT('Ctrl Pts',(0.190392305976075,-0.244992948430459,
-1.80271403609162));
#73190=CARTESIAN_POINT('Ctrl Pts',(0.244575998013883,-0.164369434073953,
-1.79743520974996));
#73191=CARTESIAN_POINT('Ctrl Pts',(0.29875969005169,-0.0837459197174479,
-1.79215638340829));
#73192=CARTESIAN_POINT('Ctrl Pts',(0.309158246821627,0.0263048577413711,
-1.78687755706662));
#73193=CARTESIAN_POINT('Ctrl Pts',(0.271034440980663,0.115650703195309,
-1.78159873072495));
#73194=CARTESIAN_POINT('Ctrl Pts',(0.2329106351397,0.204996548649246,-1.77631990438328));
#73195=CARTESIAN_POINT('Ctrl Pts',(0.146264466687836,0.273637462098302,
-1.77104107804162));
#73196=CARTESIAN_POINT('Ctrl Pts',(0.0505657951064905,0.29030626034669,
-1.76576225169995));
#73197=CARTESIAN_POINT('Ctrl Pts',(-0.0451328764748552,0.306975058595079,
-1.76048342535828));
#73198=CARTESIAN_POINT('Ctrl Pts',(-0.149884051185683,0.2716717416428,-1.75520459901661));
#73199=CARTESIAN_POINT('Ctrl Pts',(-0.215970879562555,0.200477606298579,
-1.74992577267494));
#73200=CARTESIAN_POINT('Ctrl Pts',(-0.265664538664458,0.146943533341182,
-1.74595638568628));
#73201=CARTESIAN_POINT('Ctrl Pts',(-0.293496554389252,0.0731160286671296,
-1.74198699869762));
#73202=CARTESIAN_POINT('Ctrl Pts',(-0.294155870929176,-0.000265231913958952,
-1.73801761170896));
#73203=CARTESIAN_POINT('Origin',(0.,0.,-0.975));
#73204=CARTESIAN_POINT('',(-0.294635704950153,9.93244666355822E-5,-1.62358238829104));
#73205=CARTESIAN_POINT('',(-0.294621628357173,0.000114745350509935,-1.63801761170896));
#73206=CARTESIAN_POINT('',(-0.2942,-3.60291088309151E-17,-0.975));
#73207=CARTESIAN_POINT('Ctrl Pts',(-0.294635704950153,9.93244666355822E-5,
-1.62358238829104));
#73208=CARTESIAN_POINT('Ctrl Pts',(-0.29466007133164,0.00563415828093715,
-1.62388305270251));
#73209=CARTESIAN_POINT('Ctrl Pts',(-0.294517542364744,0.0111677125456974,
-1.62418371711397));
#73210=CARTESIAN_POINT('Ctrl Pts',(-0.294204148018538,0.016691572821619,
-1.62448438152544));
#73211=CARTESIAN_POINT('Ctrl Pts',(-0.288701819618525,0.113675113341228,
-1.62976320786711));
#73212=CARTESIAN_POINT('Ctrl Pts',(-0.230529314588497,0.207670429409272,
-1.63504203420877));
#73213=CARTESIAN_POINT('Ctrl Pts',(-0.146185764509842,0.255860140760567,
-1.64032086055044));
#73214=CARTESIAN_POINT('Ctrl Pts',(-0.0618422144311871,0.304049852111862,
-1.64559968689211));
#73215=CARTESIAN_POINT('Ctrl Pts',(0.0486723806960958,0.306433958746409,
-1.65087851323378));
#73216=CARTESIAN_POINT('Ctrl Pts',(0.135015667965605,0.261926437294344,
-1.65615733957545));
#73217=CARTESIAN_POINT('Ctrl Pts',(0.221358955235115,0.217418915842279,
-1.66143616591712));
#73218=CARTESIAN_POINT('Ctrl Pts',(0.283530934646851,0.126019766303602,
-1.66671499225878));
#73219=CARTESIAN_POINT('Ctrl Pts',(0.293210606856168,0.0293637433603259,
-1.67199381860045));
#73220=CARTESIAN_POINT('Ctrl Pts',(0.302890279065485,-0.0672922795829509,
-1.67727264494212));
#73221=CARTESIAN_POINT('Ctrl Pts',(0.260077644072382,-0.169205175930827,
-1.68255147128379));
#73222=CARTESIAN_POINT('Ctrl Pts',(0.184275002501595,-0.229950892928197,
-1.68783029762546));
#73223=CARTESIAN_POINT('Ctrl Pts',(0.108472360930808,-0.290696609925567,
-1.69310912396712));
#73224=CARTESIAN_POINT('Ctrl Pts',(-0.000320287217663959,-0.310275147572431,
-1.69838795030879));
#73225=CARTESIAN_POINT('Ctrl Pts',(-0.0925449829713599,-0.279767965087295,
-1.70366677665046));
#73226=CARTESIAN_POINT('Ctrl Pts',(-0.184769678725056,-0.249260782602159,
-1.70894560299213));
#73227=CARTESIAN_POINT('Ctrl Pts',(-0.260426422083976,-0.168667879985022,
-1.7142244293338));
#73228=CARTESIAN_POINT('Ctrl Pts',(-0.285051541170753,-0.0747014666740018,
-1.71950325567546));
#73229=CARTESIAN_POINT('Ctrl Pts',(-0.291394436347813,-0.0504977620057828,
-1.72086296654732));
#73230=CARTESIAN_POINT('Ctrl Pts',(-0.294351558961662,-0.0254067709494276,
-1.72222267741918));
#73231=CARTESIAN_POINT('Ctrl Pts',(-0.294128475609455,-0.000264102212364226,
-1.72358238829104));
#73232=CARTESIAN_POINT('Ctrl Pts',(-0.294155870929176,-0.000265231913958952,
-1.73801761170896));
#73233=CARTESIAN_POINT('Ctrl Pts',(-0.294373369254718,-0.0244725744211715,
-1.73670817235595));
#73234=CARTESIAN_POINT('Ctrl Pts',(-0.291633831150307,-0.0486313549496652,
-1.73539873300295));
#73235=CARTESIAN_POINT('Ctrl Pts',(-0.285746593491363,-0.0719970338945612,
-1.73408929364994));
#73236=CARTESIAN_POINT('Ctrl Pts',(-0.262012997000382,-0.166192585007317,
-1.72881046730827));
#73237=CARTESIAN_POINT('Ctrl Pts',(-0.187123321975502,-0.247498733496666,
-1.7235316409666));
#73238=CARTESIAN_POINT('Ctrl Pts',(-0.0951918484083055,-0.278878439174703,
-1.71825281462494));
#73239=CARTESIAN_POINT('Ctrl Pts',(-0.00326037484110897,-0.310258144852741,
-1.71297398828327));
#73240=CARTESIAN_POINT('Ctrl Pts',(0.105712897268404,-0.291711407719467,
-1.7076951619416));
#73241=CARTESIAN_POINT('Ctrl Pts',(0.182087744697166,-0.231686718226887,
-1.70241633559993));
#73242=CARTESIAN_POINT('Ctrl Pts',(0.258462592125928,-0.171662028734307,
-1.69713750925826));
#73243=CARTESIAN_POINT('Ctrl Pts',(0.302239014873937,-0.0701593868824198,
-1.6918586829166));
#73244=CARTESIAN_POINT('Ctrl Pts',(0.293475673477413,0.0265840167733769,
-1.68657985657493));
#73245=CARTESIAN_POINT('Ctrl Pts',(0.284712332080889,0.123327420429173,
-1.68130103023326));
#73246=CARTESIAN_POINT('Ctrl Pts',(0.223409226539831,0.215311585888878,
-1.67602220389159));
#73247=CARTESIAN_POINT('Ctrl Pts',(0.137491564974706,0.260635278388163,
-1.67074337754992));
#73248=CARTESIAN_POINT('Ctrl Pts',(0.0515739034095804,0.305958970887449,
-1.66546455120825));
#73249=CARTESIAN_POINT('Ctrl Pts',(-0.058958314179612,0.304622190426314,
-1.66018572486659));
#73250=CARTESIAN_POINT('Ctrl Pts',(-0.14375470950795,0.257233869898643,
-1.65490689852492));
#73251=CARTESIAN_POINT('Ctrl Pts',(-0.228551104836288,0.209845549370971,
-1.64962807218325));
#73252=CARTESIAN_POINT('Ctrl Pts',(-0.28761167790377,0.116405688776762,
-1.64434924584158));
#73253=CARTESIAN_POINT('Ctrl Pts',(-0.294032757280035,0.019478646388514,
-1.63907041949991));
#73254=CARTESIAN_POINT('Ctrl Pts',(-0.294459630095828,0.0130349447791417,
-1.6387194835696));
#73255=CARTESIAN_POINT('Ctrl Pts',(-0.294653858500483,0.0065758312936643,
-1.63836854763928));
#73256=CARTESIAN_POINT('Ctrl Pts',(-0.294621628357173,0.000114745350509935,
-1.63801761170896));
#73257=CARTESIAN_POINT('Origin',(0.,0.,-0.975));
#73258=CARTESIAN_POINT('',(-0.293848972356552,0.000185260601430967,-1.52358238829104));
#73259=CARTESIAN_POINT('',(-0.293831567852127,0.000174014199626464,-1.53801761170896));
#73260=CARTESIAN_POINT('',(-0.2942,-3.60291088309151E-17,-0.975));
#73261=CARTESIAN_POINT('Ctrl Pts',(-0.293848972356552,0.000185260601430967,
-1.52358238829104));
#73262=CARTESIAN_POINT('Ctrl Pts',(-0.294059652757306,0.0365345081610124,
-1.52554342798583));
#73263=CARTESIAN_POINT('Ctrl Pts',(-0.287810810463736,0.0728138920437894,
-1.52750446768062));
#73264=CARTESIAN_POINT('Ctrl Pts',(-0.274773239737348,0.106462932671202,
-1.52946550737541));
#73265=CARTESIAN_POINT('Ctrl Pts',(-0.23967804407933,0.197041130811557,
-1.53474433371708));
#73266=CARTESIAN_POINT('Ctrl Pts',(-0.155391308608968,0.268559701475745,
-1.54002316005875));
#73267=CARTESIAN_POINT('Ctrl Pts',(-0.0603078950404424,0.288440023412727,
-1.54530198640042));
#73268=CARTESIAN_POINT('Ctrl Pts',(0.034775518528081,0.308320345349709,
-1.55058081274209));
#73269=CARTESIAN_POINT('Ctrl Pts',(0.140655610194769,0.276562418559487,
-1.55585963908375));
#73270=CARTESIAN_POINT('Ctrl Pts',(0.209101167128348,0.20763282787565,-1.56113846542542));
#73271=CARTESIAN_POINT('Ctrl Pts',(0.277546724061928,0.138703237191812,
-1.56641729176709));
#73272=CARTESIAN_POINT('Ctrl Pts',(0.308557746262399,0.032601982614358,
-1.57169611810876));
#73273=CARTESIAN_POINT('Ctrl Pts',(0.288007883920642,-0.0623389774397669,
-1.57697494445043));
#73274=CARTESIAN_POINT('Ctrl Pts',(0.267458021578885,-0.157279937493893,
-1.58225377079209));
#73275=CARTESIAN_POINT('Ctrl Pts',(0.195347274694897,-0.241060603024691,
-1.58753259713376));
#73276=CARTESIAN_POINT('Ctrl Pts',(0.104524016624659,-0.275516640637564,
-1.59281142347543));
#73277=CARTESIAN_POINT('Ctrl Pts',(0.0137007585544223,-0.309972678250436,
-1.5980902498171));
#73278=CARTESIAN_POINT('Ctrl Pts',(-0.0958350107020636,-0.295104087945385,
-1.60336907615877));
#73279=CARTESIAN_POINT('Ctrl Pts',(-0.174186819445307,-0.237683910307274,
-1.60864790250043));
#73280=CARTESIAN_POINT('Ctrl Pts',(-0.248075969457547,-0.183534195230047,
-1.61362606443064));
#73281=CARTESIAN_POINT('Ctrl Pts',(-0.294232265806487,-0.0915420468882019,
-1.61860422636084));
#73282=CARTESIAN_POINT('Ctrl Pts',(-0.294635704950153,9.93244666355822E-5,
-1.62358238829104));
#73283=CARTESIAN_POINT('Ctrl Pts',(-0.294621628357173,0.000114745350509935,
-1.63801761170896));
#73284=CARTESIAN_POINT('Ctrl Pts',(-0.294169048269317,-0.0906127086249664,
-1.63308972129761));
#73285=CARTESIAN_POINT('Ctrl Pts',(-0.249063006756553,-0.18172909498379,
-1.62816183088626));
#73286=CARTESIAN_POINT('Ctrl Pts',(-0.176431238499582,-0.236022663853079,
-1.62323394047491));
#73287=CARTESIAN_POINT('Ctrl Pts',(-0.0986270546578152,-0.294182707524139,
-1.61795511413324));
#73288=CARTESIAN_POINT('Ctrl Pts',(0.0107628987107675,-0.310088570683974,
-1.61267628779157));
#73289=CARTESIAN_POINT('Ctrl Pts',(0.101908573247503,-0.276494706451795,
-1.6073974614499));
#73290=CARTESIAN_POINT('Ctrl Pts',(0.19305424778424,-0.242900842219616,
-1.60211863510824));
#73291=CARTESIAN_POINT('Ctrl Pts',(0.26595564348913,-0.159807250595422,
-1.59683980876657));
#73292=CARTESIAN_POINT('Ctrl Pts',(0.287404225167761,-0.0650652848440229,
-1.5915609824249));
#73293=CARTESIAN_POINT('Ctrl Pts',(0.308852806846392,0.0296766809073748,
-1.58628215608323));
#73294=CARTESIAN_POINT('Ctrl Pts',(0.278848574498767,0.136067020785977,
-1.58100332974156));
#73295=CARTESIAN_POINT('Ctrl Pts',(0.211059258319554,0.205642090503064,
-1.5757245033999));
#73296=CARTESIAN_POINT('Ctrl Pts',(0.143269942140342,0.275217160220151,
-1.57044567705823));
#73297=CARTESIAN_POINT('Ctrl Pts',(0.0376955421295423,0.307976959775722,
-1.56516685071656));
#73298=CARTESIAN_POINT('Ctrl Pts',(-0.0575719796483724,0.288998524391603,
-1.55988802437489));
#73299=CARTESIAN_POINT('Ctrl Pts',(-0.152839501426288,0.270020089007484,
-1.55460919803322));
#73300=CARTESIAN_POINT('Ctrl Pts',(-0.237800144971318,0.199303418683675,
-1.54933037169156));
#73301=CARTESIAN_POINT('Ctrl Pts',(-0.273752065399016,0.109061847682818,
-1.54405154534989));
#73302=CARTESIAN_POINT('Ctrl Pts',(-0.287450280878734,0.074678469268191,
-1.54204023413625));
#73303=CARTESIAN_POINT('Ctrl Pts',(-0.294033786615915,0.0374606158410958,
-1.5400289229226));
#73304=CARTESIAN_POINT('Ctrl Pts',(-0.293831567852127,0.000174014199626464,
-1.53801761170896));
#73305=CARTESIAN_POINT('Origin',(0.,0.,-0.975));
#73306=CARTESIAN_POINT('',(-0.293976078480642,-0.000239187850661487,-1.42358238829104));
#73307=CARTESIAN_POINT('',(-0.294000243181898,-0.000245490063885288,-1.43801761170896));
#73308=CARTESIAN_POINT('',(-0.2942,-3.60291088309151E-17,-0.975));
#73309=CARTESIAN_POINT('Ctrl Pts',(-0.293976078480642,-0.000239187850661488,
-1.42358238829104));
#73310=CARTESIAN_POINT('Ctrl Pts',(-0.293459100644232,0.0668131948144753,
-1.42720380326916));
#73311=CARTESIAN_POINT('Ctrl Pts',(-0.270685225221847,0.13418317542563,
-1.43082521824727));
#73312=CARTESIAN_POINT('Ctrl Pts',(-0.228646632964908,0.185890845774307,
-1.43444663322539));
#73313=CARTESIAN_POINT('Ctrl Pts',(-0.1673682571053,0.261263542345228,-1.43972545956705));
#73314=CARTESIAN_POINT('Ctrl Pts',(-0.0651562009534198,0.30335695397111,
-1.44500428590872));
#73315=CARTESIAN_POINT('Ctrl Pts',(0.0314292109107904,0.292996406139133,
-1.45028311225039));
#73316=CARTESIAN_POINT('Ctrl Pts',(0.128014622775002,0.282635858307157,
-1.45556193859206));
#73317=CARTESIAN_POINT('Ctrl Pts',(0.218973390351543,0.219821351017321,
-1.46084076493373));
#73318=CARTESIAN_POINT('Ctrl Pts',(0.262871362903329,0.133166571909731,
-1.46611959127539));
#73319=CARTESIAN_POINT('Ctrl Pts',(0.306769335455115,0.0465117928021422,
-1.47139841761706));
#73320=CARTESIAN_POINT('Ctrl Pts',(0.303606512982146,-0.0639832581232009,
-1.47667724395873));
#73321=CARTESIAN_POINT('Ctrl Pts',(0.254823645690022,-0.147985130692535,
-1.4819560703004));
#73322=CARTESIAN_POINT('Ctrl Pts',(0.206040778397898,-0.231987003261871,
-1.48723489664207));
#73323=CARTESIAN_POINT('Ctrl Pts',(0.111637866286618,-0.289495697475197,
-1.49251372298374));
#73324=CARTESIAN_POINT('Ctrl Pts',(0.0146179600206351,-0.29431446541747,
-1.4977925493254));
#73325=CARTESIAN_POINT('Ctrl Pts',(-0.0824019462453475,-0.299133233359743,
-1.50307137566707));
#73326=CARTESIAN_POINT('Ctrl Pts',(-0.182038846666034,-0.251262075030964,
-1.50835020200874));
#73327=CARTESIAN_POINT('Ctrl Pts',(-0.238905468953538,-0.172507583058315,
-1.51362902835041));
#73328=CARTESIAN_POINT('Ctrl Pts',(-0.274646618191435,-0.123009724076673,
-1.51694681499729));
#73329=CARTESIAN_POINT('Ctrl Pts',(-0.293492532544428,-0.0613122442668173,
-1.52026460164416));
#73330=CARTESIAN_POINT('Ctrl Pts',(-0.293848972356552,0.000185260601430967,
-1.52358238829104));
#73331=CARTESIAN_POINT('Ctrl Pts',(-0.293831567852127,0.000174014199626464,
-1.53801761170896));
#73332=CARTESIAN_POINT('Ctrl Pts',(-0.293503049388466,-0.0604006666900559,
-1.53475009658094));
#73333=CARTESIAN_POINT('Ctrl Pts',(-0.275265466965423,-0.121156789689294,
-1.53148258145291));
#73334=CARTESIAN_POINT('Ctrl Pts',(-0.240529380088274,-0.170236004540617,
-1.52821506632488));
#73335=CARTESIAN_POINT('Ctrl Pts',(-0.18441157703947,-0.249525814085292,
-1.52293623998321));
#73336=CARTESIAN_POINT('Ctrl Pts',(-0.0852327736314988,-0.298338961496739,
-1.51765741364155));
#73337=CARTESIAN_POINT('Ctrl Pts',(0.0118284332921869,-0.294439752917206,
-1.51237858729988));
#73338=CARTESIAN_POINT('Ctrl Pts',(0.108889640215873,-0.290540544337672,
-1.50709976095821));
#73339=CARTESIAN_POINT('Ctrl Pts',(0.203833250655272,-0.233928979767156,
-1.50182093461654));
#73340=CARTESIAN_POINT('Ctrl Pts',(0.253409911396691,-0.150393140588825,
-1.49654210827487));
#73341=CARTESIAN_POINT('Ctrl Pts',(0.302986572138111,-0.0668573014104933,
-1.49126328193321));
#73342=CARTESIAN_POINT('Ctrl Pts',(0.307196283181549,0.0436028123756558,
-1.48598445559154));
#73343=CARTESIAN_POINT('Ctrl Pts',(0.264121408586994,0.130669665401313,
-1.48070562924987));
#73344=CARTESIAN_POINT('Ctrl Pts',(0.221046533992439,0.217736518426971,
-1.4754268029082));
#73345=CARTESIAN_POINT('Ctrl Pts',(0.130687073759891,0.281410110692138,
-1.47014797656653));
#73346=CARTESIAN_POINT('Ctrl Pts',(0.0342041781057301,0.29268541837746,
-1.46486915022487));
#73347=CARTESIAN_POINT('Ctrl Pts',(-0.0622787175484317,0.303960726062782,
-1.4595903238832));
#73348=CARTESIAN_POINT('Ctrl Pts',(-0.164885048624206,0.262837749168258,
-1.45431149754153));
#73349=CARTESIAN_POINT('Ctrl Pts',(-0.226874887771002,0.188049103239753,
-1.44903267119986));
#73350=CARTESIAN_POINT('Ctrl Pts',(-0.269991906709058,0.136029877069238,
-1.44536098470289));
#73351=CARTESIAN_POINT('Ctrl Pts',(-0.29345909350785,0.0677235538611339,
-1.44168929820593));
#73352=CARTESIAN_POINT('Ctrl Pts',(-0.294000243181898,-0.000245490063885288,
-1.43801761170896));
#73353=CARTESIAN_POINT('Origin',(0.,0.,-0.975));
#73354=CARTESIAN_POINT('',(-0.294677260201263,1.00828370830571E-6,-1.32358238829104));
#73355=CARTESIAN_POINT('',(-0.29467583034949,1.80923891189878E-5,-1.33801761170896));
#73356=CARTESIAN_POINT('',(-0.2942,-3.60291088309151E-17,-0.975));
#73357=CARTESIAN_POINT('Ctrl Pts',(-0.294677258502014,1.00828011838765E-6,
-1.32358238829104));
#73358=CARTESIAN_POINT('Ctrl Pts',(-0.294682224165865,0.0971950549178843,
-1.32886417855248));
#73359=CARTESIAN_POINT('Ctrl Pts',(-0.241859572446614,0.194384460417949,
-1.33414596881392));
#73360=CARTESIAN_POINT('Ctrl Pts',(-0.160305775694497,0.24725846312689,
-1.33942775907536));
#73361=CARTESIAN_POINT('Ctrl Pts',(-0.0787977435219472,0.300102795157083,
-1.34470658541703));
#73362=CARTESIAN_POINT('Ctrl Pts',(0.0314091821623557,0.308681446350664,
-1.3499854117587));
#73363=CARTESIAN_POINT('Ctrl Pts',(0.120112799935227,0.269086611708214,
-1.35526423810036));
#73364=CARTESIAN_POINT('Ctrl Pts',(0.2088164177081,0.229491777065762,-1.36054306444203));
#73365=CARTESIAN_POINT('Ctrl Pts',(0.27601672756954,0.141723456587276,-1.3658218907837));
#73366=CARTESIAN_POINT('Ctrl Pts',(0.291102191538456,0.045762467048812,
-1.37110071712537));
#73367=CARTESIAN_POINT('Ctrl Pts',(0.306187655507372,-0.0501985224896504,
-1.37637954346704));
#73368=CARTESIAN_POINT('Ctrl Pts',(0.269158273583764,-0.15435218108809,
-1.38165836980871));
#73369=CARTESIAN_POINT('Ctrl Pts',(0.196881919346013,-0.219253732336566,
-1.38693719615037));
#73370=CARTESIAN_POINT('Ctrl Pts',(0.124605565108262,-0.284155283585041,
-1.39221602249204));
#73371=CARTESIAN_POINT('Ctrl Pts',(0.0170822385563674,-0.309804727483553,
-1.39749484883371));
#73372=CARTESIAN_POINT('Ctrl Pts',(-0.0767083100468562,-0.284518056507222,
-1.40277367517538));
#73373=CARTESIAN_POINT('Ctrl Pts',(-0.17049885865008,-0.259231385530891,
-1.40805250151705));
#73374=CARTESIAN_POINT('Ctrl Pts',(-0.250556629304634,-0.183008599679717,
-1.41333132785871));
#73375=CARTESIAN_POINT('Ctrl Pts',(-0.280413166848243,-0.0905712159961477,
-1.41861015420038));
#73376=CARTESIAN_POINT('Ctrl Pts',(-0.289787327200992,-0.0615483309421544,
-1.42026756556394));
#73377=CARTESIAN_POINT('Ctrl Pts',(-0.294212683494414,-0.0309270216543183,
-1.42192497692749));
#73378=CARTESIAN_POINT('Ctrl Pts',(-0.293976078480642,-0.000239187850661488,
-1.42358238829104));
#73379=CARTESIAN_POINT('Ctrl Pts',(-0.294000243181898,-0.000245490063885288,
-1.43801761170896));
#73380=CARTESIAN_POINT('Ctrl Pts',(-0.294237110682385,-0.0299963303898278,
-1.43641047186426));
#73381=CARTESIAN_POINT('Ctrl Pts',(-0.290081545205885,-0.0596825508847279,
-1.43480333201956));
#73382=CARTESIAN_POINT('Ctrl Pts',(-0.281258798274574,-0.0879100012713292,
-1.43319619217486));
#73383=CARTESIAN_POINT('Ctrl Pts',(-0.252279522413535,-0.180626144891419,
-1.42791736583319));
#73384=CARTESIAN_POINT('Ctrl Pts',(-0.172947623473641,-0.257604117169112,
-1.42263853949152));
#73385=CARTESIAN_POINT('Ctrl Pts',(-0.0794009026422469,-0.283778393451755,
-1.41735971314985));
#73386=CARTESIAN_POINT('Ctrl Pts',(0.0141458181891462,-0.309952669734398,
-1.41208088680818));
#73387=CARTESIAN_POINT('Ctrl Pts',(0.12190736091204,-0.285323250021994,
-1.40680206046652));
#73388=CARTESIAN_POINT('Ctrl Pts',(0.194795461428105,-0.221109493548848,
-1.40152323412485));
#73389=CARTESIAN_POINT('Ctrl Pts',(0.267683561944172,-0.156895737075701,
-1.39624440778318));
#73390=CARTESIAN_POINT('Ctrl Pts',(0.305698220253408,-0.0530976438418118,
-1.39096558144151));
#73391=CARTESIAN_POINT('Ctrl Pts',(0.291522743038951,0.0430019792738263,
-1.38568675509984));
#73392=CARTESIAN_POINT('Ctrl Pts',(0.277347265824494,0.139101602389462,
-1.38040792875818));
#73393=CARTESIAN_POINT('Ctrl Pts',(0.210981653086343,0.227502755386847,
-1.37512910241651));
#73394=CARTESIAN_POINT('Ctrl Pts',(0.122657215947318,0.267936349356492,
-1.36985027607484));
#73395=CARTESIAN_POINT('Ctrl Pts',(0.0343327788082925,0.308369943326136,
-1.36457144973317));
#73396=CARTESIAN_POINT('Ctrl Pts',(-0.0759504827316088,0.30083597826804,
-1.3592926233915));
#73397=CARTESIAN_POINT('Ctrl Pts',(-0.157955594225854,0.248766376713537,
-1.35401379704983));
#73398=CARTESIAN_POINT('Ctrl Pts',(-0.2399607057201,0.196696775159033,-1.34873497070817));
#73399=CARTESIAN_POINT('Ctrl Pts',(-0.29368766716869,0.10009153710812,-1.3434561443665));
#73400=CARTESIAN_POINT('Ctrl Pts',(-0.294662411050462,0.00295693157748309,
-1.33817731802483));
#73401=CARTESIAN_POINT('Ctrl Pts',(-0.29467224106091,0.00197735714252186,
-1.33812408258621));
#73402=CARTESIAN_POINT('Ctrl Pts',(-0.294676706097081,0.000997728870147867,
-1.33807084714758));
#73403=CARTESIAN_POINT('Ctrl Pts',(-0.29467583034949,1.80923891189878E-5,
-1.33801761170896));
#73404=CARTESIAN_POINT('Origin',(0.,0.,-0.975));
#73405=CARTESIAN_POINT('',(-0.293973278032798,0.000238391689448475,-1.22358238829104));
#73406=CARTESIAN_POINT('',(-0.293949969260341,0.000231200790277284,-1.23801761170896));
#73407=CARTESIAN_POINT('',(-0.2942,-3.60291088309151E-17,-0.975));
#73408=CARTESIAN_POINT('Ctrl Pts',(-0.293973278032798,0.000238391689448475,
-1.22358238829104));
#73409=CARTESIAN_POINT('Ctrl Pts',(-0.294209779461322,0.0310367239073477,
-1.22524572749414));
#73410=CARTESIAN_POINT('Ctrl Pts',(-0.28975201722522,0.0617683278239009,
-1.22690906669723));
#73411=CARTESIAN_POINT('Ctrl Pts',(-0.280311790129639,0.0908844850521986,
-1.22857240590033));
#73412=CARTESIAN_POINT('Ctrl Pts',(-0.250351984354179,0.183288450195776,
-1.233851232242));
#73413=CARTESIAN_POINT('Ctrl Pts',(-0.17020909453095,0.259421734217083,
-1.23913005858367));
#73414=CARTESIAN_POINT('Ctrl Pts',(-0.0763903498795328,0.28460359055038,
-1.24440888492533));
#73415=CARTESIAN_POINT('Ctrl Pts',(0.0174283947718846,0.309785446883678,
-1.249687711267));
#73416=CARTESIAN_POINT('Ctrl Pts',(0.124922994251492,0.284015875528968,
-1.25496653760867));
#73417=CARTESIAN_POINT('Ctrl Pts',(0.197126784246028,0.219033605279432,
-1.26024536395034));
#73418=CARTESIAN_POINT('Ctrl Pts',(0.269330574240564,0.154051335029895,
-1.26552419029201));
#73419=CARTESIAN_POINT('Ctrl Pts',(0.306243554750027,0.0498563658855321,
-1.27080301663368));
#73420=CARTESIAN_POINT('Ctrl Pts',(0.291050876152584,-0.0460877076854485,
-1.27608184297534));
#73421=CARTESIAN_POINT('Ctrl Pts',(0.275858197555141,-0.142031781256427,
-1.28136066931701));
#73422=CARTESIAN_POINT('Ctrl Pts',(0.208559859850791,-0.229724959254024,
-1.28663949565868));
#73423=CARTESIAN_POINT('Ctrl Pts',(0.119812055324197,-0.269220654311436,
-1.29191832200035));
#73424=CARTESIAN_POINT('Ctrl Pts',(0.0310642507976013,-0.308716349368848,
-1.29719714834201));
#73425=CARTESIAN_POINT('Ctrl Pts',(-0.0791330205512378,-0.300014561486076,
-1.30247597468368));
#73426=CARTESIAN_POINT('Ctrl Pts',(-0.160581955107085,-0.247079187716959,
-1.30775480102535));
#73427=CARTESIAN_POINT('Ctrl Pts',(-0.241985158265097,-0.194173535744089,
-1.31303066344725));
#73428=CARTESIAN_POINT('Ctrl Pts',(-0.294672298411209,-0.0970839558904198,
-1.31830652586914));
#73429=CARTESIAN_POINT('Ctrl Pts',(-0.294677258502014,1.00828011838765E-6,
-1.32358238829104));
#73430=CARTESIAN_POINT('Ctrl Pts',(-0.29467583034949,1.80923891189878E-5,
-1.33801761170896));
#73431=CARTESIAN_POINT('Ctrl Pts',(-0.294589866961943,-0.0961430291488454,
-1.33279202080592));
#73432=CARTESIAN_POINT('Ctrl Pts',(-0.243043387744428,-0.192383244249407,
-1.32756642990287));
#73433=CARTESIAN_POINT('Ctrl Pts',(-0.162916013713709,-0.245546436353821,
-1.32234083899983));
#73434=CARTESIAN_POINT('Ctrl Pts',(-0.0819723461802288,-0.299251225744129,
-1.31706201265816));
#73435=CARTESIAN_POINT('Ctrl Pts',(0.0281375152016859,-0.308996831514383,
-1.31178318631649));
#73436=CARTESIAN_POINT('Ctrl Pts',(0.117255584393945,-0.270343869652818,
-1.30650435997482));
#73437=CARTESIAN_POINT('Ctrl Pts',(0.206373653586204,-0.231690907791252,
-1.30122553363315));
#73438=CARTESIAN_POINT('Ctrl Pts',(0.274499930588806,-0.144639378297869,
-1.29594670729149));
#73439=CARTESIAN_POINT('Ctrl Pts',(0.290601074628839,-0.0488435804890409,
-1.29066788094982));
#73440=CARTESIAN_POINT('Ctrl Pts',(0.306702218668872,0.0469522173197857,
-1.28538905460815));
#73441=CARTESIAN_POINT('Ctrl Pts',(0.270778229746334,0.151492283444057,
-1.28011022826648));
#73442=CARTESIAN_POINT('Ctrl Pts',(0.19919344537101,0.217155822513817,-1.27483140192481));
#73443=CARTESIAN_POINT('Ctrl Pts',(0.127608660995684,0.282819361583577,
-1.26955257558315));
#73444=CARTESIAN_POINT('Ctrl Pts',(0.0203630811675721,0.309606373598827,
-1.26427374924148));
#73445=CARTESIAN_POINT('Ctrl Pts',(-0.0736900649097486,0.285314658340616,
-1.25899492289981));
#73446=CARTESIAN_POINT('Ctrl Pts',(-0.167743210987069,0.261022943082406,
-1.25371609655814));
#73447=CARTESIAN_POINT('Ctrl Pts',(-0.248603923313597,0.185652500550734,
-1.24843727021647));
#73448=CARTESIAN_POINT('Ctrl Pts',(-0.279437985325964,0.0935365826155301,
-1.2431584438748));
#73449=CARTESIAN_POINT('Ctrl Pts',(-0.289447327525483,0.0636339462302733,
-1.24144483315286));
#73450=CARTESIAN_POINT('Ctrl Pts',(-0.294184965742798,0.0319667066022578,
-1.23973122243091));
#73451=CARTESIAN_POINT('Ctrl Pts',(-0.293949969260341,0.000231200790277284,
-1.23801761170896));
#73452=CARTESIAN_POINT('Origin',(0.,0.,-0.975));
#73453=CARTESIAN_POINT('',(-0.293851097698083,-0.000186547984213553,-1.12358238829104));
#73454=CARTESIAN_POINT('',(-0.29386972337181,-0.000197122199406605,-1.13801761170896));
#73455=CARTESIAN_POINT('',(-0.2942,-3.60291088309151E-17,-0.975));
#73456=CARTESIAN_POINT('Ctrl Pts',(-0.293851097698083,-0.000186547984213553,
-1.12358238829104));
#73457=CARTESIAN_POINT('Ctrl Pts',(-0.293491376629239,0.0614197145543361,
-1.12690610277746));
#73458=CARTESIAN_POINT('Ctrl Pts',(-0.274572956169531,0.12322816383533,
-1.13022981726388));
#73459=CARTESIAN_POINT('Ctrl Pts',(-0.238712564810087,0.172774421459531,
-1.1335535317503));
#73460=CARTESIAN_POINT('Ctrl Pts',(-0.181757980021253,0.251465323143845,
-1.13883235809197));
#73461=CARTESIAN_POINT('Ctrl Pts',(-0.0820676519460495,0.299225120184297,
-1.14411118443364));
#73462=CARTESIAN_POINT('Ctrl Pts',(0.0149468094019105,0.294297948000982,
-1.14939001077531));
#73463=CARTESIAN_POINT('Ctrl Pts',(0.111961270749869,0.289370775817668,
-1.15466883711698));
#73464=CARTESIAN_POINT('Ctrl Pts',(0.206299865370584,0.231756634410589,
-1.15994766345864));
#73465=CARTESIAN_POINT('Ctrl Pts',(0.254988840936584,0.14770030570958,-1.16522648980031));
#73466=CARTESIAN_POINT('Ctrl Pts',(0.303677816502585,0.0636439770085698,
-1.17050531614198));
#73467=CARTESIAN_POINT('Ctrl Pts',(0.306717173013869,-0.0468545389863712,
-1.17578414248365));
#73468=CARTESIAN_POINT('Ctrl Pts',(0.262722402311544,-0.133460213668858,
-1.18106296882532));
#73469=CARTESIAN_POINT('Ctrl Pts',(0.218727631609219,-0.220065888351345,
-1.18634179516699));
#73470=CARTESIAN_POINT('Ctrl Pts',(0.127698733693286,-0.282778721721378,
-1.19162062150865));
#73471=CARTESIAN_POINT('Ctrl Pts',(0.0311018055456793,-0.293031341328338,
-1.19689944785032));
#73472=CARTESIAN_POINT('Ctrl Pts',(-0.0654951226019258,-0.303283960935298,
-1.20217827419199));
#73473=CARTESIAN_POINT('Ctrl Pts',(-0.167660080981204,-0.261076366779188,
-1.20745710053366));
#73474=CARTESIAN_POINT('Ctrl Pts',(-0.228854199306997,-0.185635246568208,
-1.21273592687533));
#73475=CARTESIAN_POINT('Ctrl Pts',(-0.270766270938664,-0.133965352127992,
-1.2163514140139));
#73476=CARTESIAN_POINT('Ctrl Pts',(-0.293459210985325,-0.0667058454306556,
-1.21996690115247));
#73477=CARTESIAN_POINT('Ctrl Pts',(-0.293973278032798,0.000238391689448475,
-1.22358238829104));
#73478=CARTESIAN_POINT('Ctrl Pts',(-0.293949969260341,0.000231200790277284,
-1.23801761170896));
#73479=CARTESIAN_POINT('Ctrl Pts',(-0.293461052425786,-0.0657954174909175,
-1.23445239608924));
#73480=CARTESIAN_POINT('Ctrl Pts',(-0.271447598728151,-0.132117532642881,
-1.23088718046952));
#73481=CARTESIAN_POINT('Ctrl Pts',(-0.230602957574135,-0.183458321938491,
-1.2273219648498));
#73482=CARTESIAN_POINT('Ctrl Pts',(-0.170126456111733,-0.259475915218572,
-1.22204313850813));
#73483=CARTESIAN_POINT('Ctrl Pts',(-0.0683660414887238,-0.302649708439997,
-1.21676431216646));
#73484=CARTESIAN_POINT('Ctrl Pts',(0.028323696507632,-0.293312884385547,
-1.2114854858248));
#73485=CARTESIAN_POINT('Ctrl Pts',(0.125013434503989,-0.283976060331096,
-1.20620665948313));
#73486=CARTESIAN_POINT('Ctrl Pts',(0.216632495873691,-0.222128619000769,
-1.20092783314146));
#73487=CARTESIAN_POINT('Ctrl Pts',(0.261445948401493,-0.135943723631765,
-1.19564900679979));
#73488=CARTESIAN_POINT('Ctrl Pts',(0.306259400929294,-0.0497588282627614,
-1.19037018045812));
#73489=CARTESIAN_POINT('Ctrl Pts',(0.304267244615197,0.0607635211449203,
-1.18509135411646));
#73490=CARTESIAN_POINT('Ctrl Pts',(0.256376959927654,0.145277439228119,
-1.17981252777479));
#73491=CARTESIAN_POINT('Ctrl Pts',(0.20848667524011,0.229791357311319,-1.17453370143312));
#73492=CARTESIAN_POINT('Ctrl Pts',(0.114698262179123,0.288296844070036,
-1.16925487509145));
#73493=CARTESIAN_POINT('Ctrl Pts',(0.0177348506606446,0.294143085933479,
-1.16397604874978));
#73494=CARTESIAN_POINT('Ctrl Pts',(-0.0792285608578346,0.299989327796923,
-1.15869722240811));
#73495=CARTESIAN_POINT('Ctrl Pts',(-0.179366970833807,0.253176324765089,
-1.15341839606645));
#73496=CARTESIAN_POINT('Ctrl Pts',(-0.23706465596679,0.175028651431054,
-1.14813956972478));
#73497=CARTESIAN_POINT('Ctrl Pts',(-0.273942395368571,0.12508020851821,
-1.14476558371951));
#73498=CARTESIAN_POINT('Ctrl Pts',(-0.293482310532986,0.0623309708912046,
-1.14139159771423));
#73499=CARTESIAN_POINT('Ctrl Pts',(-0.29386972337181,-0.000197122199406605,
-1.13801761170896));
#73500=CARTESIAN_POINT('Origin',(0.,0.,-0.975));
#73501=CARTESIAN_POINT('',(-0.294637244334855,-9.74749229996352E-5,-1.02358238829104));
#73502=CARTESIAN_POINT('',(-0.294649229866944,-8.15492747527925E-5,-1.03801761170896));
#73503=CARTESIAN_POINT('',(-0.2942,-3.60291088309151E-17,-0.975));
#73504=CARTESIAN_POINT('Ctrl Pts',(-0.294637244334855,-9.74749229996352E-5,
-1.02358238829104));
#73505=CARTESIAN_POINT('Ctrl Pts',(-0.294239924072814,0.0916517427871641,
-1.02856647806079));
#73506=CARTESIAN_POINT('Ctrl Pts',(-0.247958795653551,0.183746892171388,
-1.03355056783053));
#73507=CARTESIAN_POINT('Ctrl Pts',(-0.173921129559392,0.237878393305636,
-1.03853465760028));
#73508=CARTESIAN_POINT('Ctrl Pts',(-0.0955052100818042,0.295210987079538,
-1.04381348394195));
#73509=CARTESIAN_POINT('Ctrl Pts',(0.0140471045446477,0.3099571759117,-1.04909231028361));
#73510=CARTESIAN_POINT('Ctrl Pts',(0.104831805736983,0.275399676497285,
-1.05437113662528));
#73511=CARTESIAN_POINT('Ctrl Pts',(0.195616506929317,0.240842177082871,
-1.05964996296695));
#73512=CARTESIAN_POINT('Ctrl Pts',(0.267633594687535,0.156980989421882,
-1.06492878930862));
#73513=CARTESIAN_POINT('Ctrl Pts',(0.288077359904879,0.0620171268209079,
-1.07020761565029));
#73514=CARTESIAN_POINT('Ctrl Pts',(0.308521125122224,-0.0329467357800676,
-1.07548644199195));
#73515=CARTESIAN_POINT('Ctrl Pts',(0.277391567798695,-0.139013273321028,
-1.08076526833362));
#73516=CARTESIAN_POINT('Ctrl Pts',(0.208869033654551,-0.207866341886078,
-1.08604409467529));
#73517=CARTESIAN_POINT('Ctrl Pts',(0.140346499510407,-0.276719410451129,
-1.09132292101696));
#73518=CARTESIAN_POINT('Ctrl Pts',(0.034430988545649,-0.308359010040268,
-1.09660174735863));
#73519=CARTESIAN_POINT('Ctrl Pts',(-0.0606301519675207,-0.288372457043458,
-1.10188057370029));
#73520=CARTESIAN_POINT('Ctrl Pts',(-0.155691292480689,-0.268385904046649,
-1.10715940004196));
#73521=CARTESIAN_POINT('Ctrl Pts',(-0.239898062542269,-0.196773198463892,
-1.11243822638363));
#73522=CARTESIAN_POINT('Ctrl Pts',(-0.274892026821827,-0.106155842508426,
-1.1177170527253));
#73523=CARTESIAN_POINT('Ctrl Pts',(-0.287852694590911,-0.0725940135236007,
-1.11967216458055));
#73524=CARTESIAN_POINT('Ctrl Pts',(-0.294062696777712,-0.0364252606470018,
-1.12162727643579));
#73525=CARTESIAN_POINT('Ctrl Pts',(-0.293851097698083,-0.000186547984213553,
-1.12358238829104));
#73526=CARTESIAN_POINT('Ctrl Pts',(-0.29386972337181,-0.000197122199406605,
-1.13801761170896));
#73527=CARTESIAN_POINT('Ctrl Pts',(-0.294088443781758,-0.0354984049228036,
-1.13611277137257));
#73528=CARTESIAN_POINT('Ctrl Pts',(-0.28820257943375,-0.0707292010046517,
-1.13420793103617));
#73529=CARTESIAN_POINT('Ctrl Pts',(-0.275885583475611,-0.103546244551637,
-1.13230309069977));
#73530=CARTESIAN_POINT('Ctrl Pts',(-0.241751865561453,-0.194491123564061,
-1.12702426435811));
#73531=CARTESIAN_POINT('Ctrl Pts',(-0.158227469443138,-0.266898537952673,
-1.12174543801644));
#73532=CARTESIAN_POINT('Ctrl Pts',(-0.0633599908742501,-0.287784974393801,
-1.11646661167477));
#73533=CARTESIAN_POINT('Ctrl Pts',(0.0315074876946384,-0.308671410834929,
-1.1111877853331));
#73534=CARTESIAN_POINT('Ctrl Pts',(0.1377180487141,-0.278036869328573,-1.10590895899143));
#73535=CARTESIAN_POINT('Ctrl Pts',(0.206889941722803,-0.209836202654263,
-1.10063013264977));
#73536=CARTESIAN_POINT('Ctrl Pts',(0.276061834731505,-0.141635535979953,
-1.0953513063081));
#73537=CARTESIAN_POINT('Ctrl Pts',(0.308195059729448,-0.0358687441376901,
-1.09007247996643));
#73538=CARTESIAN_POINT('Ctrl Pts',(0.288652073534054,0.0592845711371557,
-1.08479365362476));
#73539=CARTESIAN_POINT('Ctrl Pts',(0.269109087338661,0.154437886412003,
-1.07951482728309));
#73540=CARTESIAN_POINT('Ctrl Pts',(0.197889889949928,0.238977725119432,
-1.07423600094143));
#73541=CARTESIAN_POINT('Ctrl Pts',(0.107436730076877,0.274393930255051,
-1.06895717459976));
#73542=CARTESIAN_POINT('Ctrl Pts',(0.016983570203827,0.30981013539067,-1.06367834825809));
#73543=CARTESIAN_POINT('Ctrl Pts',(-0.0927035521535406,0.296102706954478,
-1.05839952191642));
#73544=CARTESIAN_POINT('Ctrl Pts',(-0.171659219886249,0.239515745115994,
-1.05312069557475));
#73545=CARTESIAN_POINT('Ctrl Pts',(-0.246958411680323,0.185549353406856,
-1.04808633428615));
#73546=CARTESIAN_POINT('Ctrl Pts',(-0.294306617932949,0.092583010904962,
-1.04305197299756));
#73547=CARTESIAN_POINT('Ctrl Pts',(-0.294649229866944,-8.15492747527925E-5,
-1.03801761170896));
#73548=CARTESIAN_POINT('Origin',(0.,0.,-0.975));
#73549=CARTESIAN_POINT('',(-0.29412526541255,0.000263908637235785,-0.92358238829104));
#73550=CARTESIAN_POINT('',(-0.294098243270401,0.000261754509978144,-0.938017611708962));
#73551=CARTESIAN_POINT('',(-0.2942,-3.60291088309151E-17,-0.975));
#73552=CARTESIAN_POINT('Ctrl Pts',(-0.29412526541255,0.000263908637235785,
-0.92358238829104));
#73553=CARTESIAN_POINT('Ctrl Pts',(-0.294348950217361,0.0255168907584005,
-0.924948027002442));
#73554=CARTESIAN_POINT('Ctrl Pts',(-0.29136559975532,0.0507178350965381,
-0.926313665713845));
#73555=CARTESIAN_POINT('Ctrl Pts',(-0.284967893282825,0.0750199247322646,
-0.927679304425247));
#73556=CARTESIAN_POINT('Ctrl Pts',(-0.260237793607645,0.168958760718316,
-0.932958130766915));
#73557=CARTESIAN_POINT('Ctrl Pts',(-0.184491046602315,0.249467083537742,
-0.938236957108583));
#73558=CARTESIAN_POINT('Ctrl Pts',(-0.0922323208863506,0.279871199470048,
-0.943515783450251));
#73559=CARTESIAN_POINT('Ctrl Pts',(2.64048296138575E-5,0.310275315402353,
-0.948794609791919));
#73560=CARTESIAN_POINT('Ctrl Pts',(0.108797109256212,0.290575224447537,
-0.954073436133588));
#73561=CARTESIAN_POINT('Ctrl Pts',(0.184531828155626,0.229744844787491,
-0.959352262475256));
#73562=CARTESIAN_POINT('Ctrl Pts',(0.260266547055043,0.168914465127443,
-0.964631088816924));
#73563=CARTESIAN_POINT('Ctrl Pts',(0.302965280427273,0.0669537967621638,
-0.969909915158591));
#73564=CARTESIAN_POINT('Ctrl Pts',(0.293177613518818,-0.0296913495869845,
-0.97518874150026));
#73565=CARTESIAN_POINT('Ctrl Pts',(0.283389946610364,-0.126336495936132,
-0.980467567841928));
#73566=CARTESIAN_POINT('Ctrl Pts',(0.221115879421224,-0.21766612026915,
-0.985746394183598));
#73567=CARTESIAN_POINT('Ctrl Pts',(0.134722914674649,-0.262077136680126,
-0.991025220525266));
#73568=CARTESIAN_POINT('Ctrl Pts',(0.0483299499280749,-0.306488153091101,
-0.996304046866934));
#73569=CARTESIAN_POINT('Ctrl Pts',(-0.0621819123759332,-0.30398056158004,
-1.0015828732086));
#73570=CARTESIAN_POINT('Ctrl Pts',(-0.146471564030352,-0.255696637129604,
-1.00686169955027));
#73571=CARTESIAN_POINT('Ctrl Pts',(-0.230761215684771,-0.207412712679169,
-1.01214052589194));
#73572=CARTESIAN_POINT('Ctrl Pts',(-0.2888286566896,-0.113352455289359,
-1.01741935223361));
#73573=CARTESIAN_POINT('Ctrl Pts',(-0.294222615027652,-0.016362827236634,
-1.02269817857527));
#73574=CARTESIAN_POINT('Ctrl Pts',(-0.294523779848533,-0.0109475343980307,
-1.0229929151472));
#73575=CARTESIAN_POINT('Ctrl Pts',(-0.294660740061738,-0.00552310952303855,
-1.02328765171912));
#73576=CARTESIAN_POINT('Ctrl Pts',(-0.294637244334855,-9.74749229996352E-5,
-1.02358238829104));
#73577=CARTESIAN_POINT('Ctrl Pts',(-0.294649229866944,-8.15492747527925E-5,
-1.03801761170896));
#73578=CARTESIAN_POINT('Ctrl Pts',(-0.29466586686215,-0.00458127532211663,
-1.03777314665589));
#73579=CARTESIAN_POINT('Ctrl Pts',(-0.29457166440834,-0.00908028976511084,
-1.03752868160282));
#73580=CARTESIAN_POINT('Ctrl Pts',(-0.294364440693888,-0.0135740924337639,
-1.03728421654975));
#73581=CARTESIAN_POINT('Ctrl Pts',(-0.289889780660768,-0.110610472904263,
-1.03200539020808));
#73582=CARTESIAN_POINT('Ctrl Pts',(-0.232716247486482,-0.20521673860449,
-1.02672656386641));
#73583=CARTESIAN_POINT('Ctrl Pts',(-0.148887914269599,-0.254297205873116,
-1.02144773752474));
#73584=CARTESIAN_POINT('Ctrl Pts',(-0.0650595810527136,-0.303377673141744,
-1.01616891118308));
#73585=CARTESIAN_POINT('Ctrl Pts',(0.0454235522067678,-0.30693234197877,
-1.01089008484141));
#73586=CARTESIAN_POINT('Ctrl Pts',(0.132233464149777,-0.26334196568222,
-1.00561125849974));
#73587=CARTESIAN_POINT('Ctrl Pts',(0.219043376092787,-0.219751589385669,
-1.00033243215807));
#73588=CARTESIAN_POINT('Ctrl Pts',(0.282180066719323,-0.12901616795554,
-0.995053605816403));
#73589=CARTESIAN_POINT('Ctrl Pts',(0.292883085265098,-0.0324681119873491,
-0.989774779474735));
#73590=CARTESIAN_POINT('Ctrl Pts',(0.303586103810872,0.0640799439808387,
-0.984495953133067));
#73591=CARTESIAN_POINT('Ctrl Pts',(0.261855450275889,0.166440634487089,
-0.979217126791399));
#73592=CARTESIAN_POINT('Ctrl Pts',(0.186700553162723,0.227985928028813,
-0.973938300449731));
#73593=CARTESIAN_POINT('Ctrl Pts',(0.111545656049556,0.289531221570537,
-0.968659474108062));
#73594=CARTESIAN_POINT('Ctrl Pts',(0.00296651535820849,0.310261118147735,
-0.963380647766395));
#73595=CARTESIAN_POINT('Ctrl Pts',(-0.0895761670770488,0.280732595582006,
-0.958101821424727));
#73596=CARTESIAN_POINT('Ctrl Pts',(-0.182118849512305,0.251204073016278,
-0.952822995083059));
#73597=CARTESIAN_POINT('Ctrl Pts',(-0.258625073691471,0.171417131307622,
-0.94754416874139));
#73598=CARTESIAN_POINT('Ctrl Pts',(-0.284244208835023,0.0777168557918905,
-0.942265342399722));
#73599=CARTESIAN_POINT('Ctrl Pts',(-0.291115886968034,0.0525841520253224,
-0.940849432169469));
#73600=CARTESIAN_POINT('Ctrl Pts',(-0.294326526593178,0.0264504625115664,
-0.939433521939215));
#73601=CARTESIAN_POINT('Ctrl Pts',(-0.294098243270401,0.000261754509978144,
-0.938017611708962));
#73602=CARTESIAN_POINT('Origin',(0.,0.,-0.975));
#73603=CARTESIAN_POINT('',(-0.293765004739316,-0.0001128917701812,-0.82358238829104));
#73604=CARTESIAN_POINT('',(-0.2937764249955,-0.000126456787260676,-0.838017611708961));
#73605=CARTESIAN_POINT('',(-0.2942,-3.60291088309151E-17,-0.975));
#73606=CARTESIAN_POINT('Ctrl Pts',(-0.293765004739316,-0.0001128917701812,
-0.82358238829104));
#73607=CARTESIAN_POINT('Ctrl Pts',(-0.293570292716816,0.0560165899656169,
-0.826608402285767));
#73608=CARTESIAN_POINT('Ctrl Pts',(-0.278094099980171,0.11224550982072,
-0.829634416280494));
#73609=CARTESIAN_POINT('Ctrl Pts',(-0.248027007594724,0.159114087410551,
-0.832660430275221));
#73610=CARTESIAN_POINT('Ctrl Pts',(-0.195575512136267,0.24087546802836,
-0.837939256616889));
#73611=CARTESIAN_POINT('Ctrl Pts',(-0.0987207464390296,0.294151298259528,
-0.843218082958558));
#73612=CARTESIAN_POINT('Ctrl Pts',(-0.0015826460346202,0.294673012915019,
-0.848496909300226));
#73613=CARTESIAN_POINT('Ctrl Pts',(0.0955554543697892,0.295194727570511,
-0.853775735641894));
#73614=CARTESIAN_POINT('Ctrl Pts',(0.192976889481371,0.242962326650326,
-0.859054561983562));
#73615=CARTESIAN_POINT('Ctrl Pts',(0.24630359069836,0.161769065392555,-0.86433338832523));
#73616=CARTESIAN_POINT('Ctrl Pts',(0.299630291915349,0.0805758041347841,
-0.869612214666898));
#73617=CARTESIAN_POINT('Ctrl Pts',(0.308862259237749,-0.0295783174605727,
-0.874891041008567));
#73618=CARTESIAN_POINT('Ctrl Pts',(0.269794084700736,-0.118515151644751,
-0.880169867350235));
#73619=CARTESIAN_POINT('Ctrl Pts',(0.230725910163722,-0.207451985828931,
-0.885448693691903));
#73620=CARTESIAN_POINT('Ctrl Pts',(0.143357593767295,-0.275171532601932,
-0.89072752003357));
#73621=CARTESIAN_POINT('Ctrl Pts',(0.0474877397325926,-0.290825727685801,
-0.896006346375238));
#73622=CARTESIAN_POINT('Ctrl Pts',(-0.0483821143021094,-0.306479922769669,
-0.901285172716907));
#73623=CARTESIAN_POINT('Ctrl Pts',(-0.152753505975086,-0.270068766164406,
-0.906563999058575));
#73624=CARTESIAN_POINT('Ctrl Pts',(-0.21808247563906,-0.198178513285434,
-0.911842825400243));
#73625=CARTESIAN_POINT('Ctrl Pts',(-0.266510762428707,-0.14488635512481,
-0.915756013030509));
#73626=CARTESIAN_POINT('Ctrl Pts',(-0.293484304810044,-0.0720975852474555,
-0.919669200660775));
#73627=CARTESIAN_POINT('Ctrl Pts',(-0.29412526541255,0.000263908637235785,
-0.92358238829104));
#73628=CARTESIAN_POINT('Ctrl Pts',(-0.294098243270401,0.000261754509978144,
-0.938017611708962));
#73629=CARTESIAN_POINT('Ctrl Pts',(-0.293475435901207,-0.0711868302342345,
-0.934154695597547));
#73630=CARTESIAN_POINT('Ctrl Pts',(-0.267256071083065,-0.143044928045731,
-0.930291779486133));
#73631=CARTESIAN_POINT('Ctrl Pts',(-0.219950575785256,-0.196103095697544,
-0.926428863374718));
#73632=CARTESIAN_POINT('Ctrl Pts',(-0.155305761483999,-0.268609162348436,
-0.92115003703305));
#73633=CARTESIAN_POINT('Ctrl Pts',(-0.0512840867735439,-0.306007686327414,
-0.915871210691381));
#73634=CARTESIAN_POINT('Ctrl Pts',(0.0447297941261825,-0.291262639979547,
-0.910592384349713));
#73635=CARTESIAN_POINT('Ctrl Pts',(0.140743675025909,-0.276517593631679,
-0.905313558008045));
#73636=CARTESIAN_POINT('Ctrl Pts',(0.228749762114909,-0.20962897695697,
-0.900034731666377));
#73637=CARTESIAN_POINT('Ctrl Pts',(0.268658929568512,-0.121066343355727,
-0.894755905324709));
#73638=CARTESIAN_POINT('Ctrl Pts',(0.308568097022116,-0.0325037097544837,
-0.889477078983041));
#73639=CARTESIAN_POINT('Ctrl Pts',(0.30038034484032,0.0777329407732916,
-0.884198252641374));
#73640=CARTESIAN_POINT('Ctrl Pts',(0.247825413070598,0.159427866343413,
-0.878919426299705));
#73641=CARTESIAN_POINT('Ctrl Pts',(0.195270481300876,0.241122791913534,
-0.873640599958037));
#73642=CARTESIAN_POINT('Ctrl Pts',(0.098348369943227,0.294275992526002,
-0.868361773616368));
#73643=CARTESIAN_POINT('Ctrl Pts',(0.00120969227830445,0.294674764062037,
-0.8630829472747));
#73644=CARTESIAN_POINT('Ctrl Pts',(-0.0959289853866181,0.295073535598073,
-0.857804120933032));
#73645=CARTESIAN_POINT('Ctrl Pts',(-0.193284229358815,0.242717878057679,
-0.852525294591365));
#73646=CARTESIAN_POINT('Ctrl Pts',(-0.24650812287037,0.161457193365153,
-0.847246468249697));
#73647=CARTESIAN_POINT('Ctrl Pts',(-0.277524845525826,0.114101767942294,
-0.844170182736118));
#73648=CARTESIAN_POINT('Ctrl Pts',(-0.293554187180766,0.0569299500855454,
-0.84109389722254));
#73649=CARTESIAN_POINT('Ctrl Pts',(-0.2937764249955,-0.000126456787260676,
-0.838017611708961));
#73650=CARTESIAN_POINT('Origin',(0.,0.,-0.975));
#73651=CARTESIAN_POINT('',(-0.294532285647886,-0.000180704995970699,-0.72358238829104));
#73652=CARTESIAN_POINT('',(-0.294553488267971,-0.000168236264217633,-0.738017611708961));
#73653=CARTESIAN_POINT('',(-0.2942,-3.60291088309151E-17,-0.975));
#73654=CARTESIAN_POINT('Ctrl Pts',(-0.294532285647886,-0.000180704995970699,
-0.72358238829104));
#73655=CARTESIAN_POINT('Ctrl Pts',(-0.293907652305694,0.0861696131302375,
-0.728268777569092));
#73656=CARTESIAN_POINT('Ctrl Pts',(-0.253640104222023,0.17302692605204,
-0.732955166847143));
#73657=CARTESIAN_POINT('Ctrl Pts',(-0.186988963747787,0.227749460472281,
-0.737641556125195));
#73658=CARTESIAN_POINT('Ctrl Pts',(-0.111912017475864,0.28938982772331,
-0.742920382466863));
#73659=CARTESIAN_POINT('Ctrl Pts',(-0.00335919464726699,0.310257131838362,
-0.748199208808531));
#73660=CARTESIAN_POINT('Ctrl Pts',(0.0892207913939141,0.280845757831465,
-0.7534780351502));
#73661=CARTESIAN_POINT('Ctrl Pts',(0.181800777435094,0.251434383824568,
-0.758756861491868));
#73662=CARTESIAN_POINT('Ctrl Pts',(0.258407926688858,0.171744331695723,
-0.764035687833536));
#73663=CARTESIAN_POINT('Ctrl Pts',(0.284145634305615,0.0780765509864899,
-0.769314514175204));
#73664=CARTESIAN_POINT('Ctrl Pts',(0.309883341922372,-0.0155912297227443,
-0.774593340516872));
#73665=CARTESIAN_POINT('Ctrl Pts',(0.28475160790212,-0.123236739012367,
-0.77987216685854));
#73666=CARTESIAN_POINT('Ctrl Pts',(0.220198609077346,-0.195824569115543,
-0.785150993200208));
#73667=CARTESIAN_POINT('Ctrl Pts',(0.155645610252571,-0.268412399218721,
-0.790429819541876));
#73668=CARTESIAN_POINT('Ctrl Pts',(0.0516713466232729,-0.305942550135451,
-0.795708645883544));
#73669=CARTESIAN_POINT('Ctrl Pts',(-0.0443611246057961,-0.291319034621144,
-0.800987472225212));
#73670=CARTESIAN_POINT('Ctrl Pts',(-0.140393595834861,-0.276695519106837,
-0.806266298566881));
#73671=CARTESIAN_POINT('Ctrl Pts',(-0.228484274663697,-0.209918337161498,
-0.811545124908549));
#73672=CARTESIAN_POINT('Ctrl Pts',(-0.268505501468278,-0.121406280686605,
-0.816823951250217));
#73673=CARTESIAN_POINT('Ctrl Pts',(-0.285585115012941,-0.0836325331196868,
-0.819076763597158));
#73674=CARTESIAN_POINT('Ctrl Pts',(-0.293909964296394,-0.0419002693904203,
-0.821329575944099));
#73675=CARTESIAN_POINT('Ctrl Pts',(-0.293765004739316,-0.0001128917701812,
-0.82358238829104));
#73676=CARTESIAN_POINT('Ctrl Pts',(-0.2937764249955,-0.000126456787260676,
-0.838017611708961));
#73677=CARTESIAN_POINT('Ctrl Pts',(-0.293935541520392,-0.0409773677598496,
-0.835815070880871));
#73678=CARTESIAN_POINT('Ctrl Pts',(-0.285991637114493,-0.08176911687534,
-0.833612530052781));
#73679=CARTESIAN_POINT('Ctrl Pts',(-0.269643855541951,-0.118856514751599,
-0.831409989224691));
#73680=CARTESIAN_POINT('Ctrl Pts',(-0.230463151651064,-0.207743826331163,
-0.826131162883023));
#73681=CARTESIAN_POINT('Ctrl Pts',(-0.143009200818376,-0.275352737645629,
-0.820852336541356));
#73682=CARTESIAN_POINT('Ctrl Pts',(-0.0471196160404858,-0.29088558182664,
-0.815573510199688));
#73683=CARTESIAN_POINT('Ctrl Pts',(0.0487699687374031,-0.30641842600765,
-0.81029468385802));
#73684=CARTESIAN_POINT('Ctrl Pts',(0.153095187460496,-0.269875203055206,
-0.805015857516351));
#73685=CARTESIAN_POINT('Ctrl Pts',(0.218333113494785,-0.197902328137137,
-0.799737031174683));
#73686=CARTESIAN_POINT('Ctrl Pts',(0.283571039529076,-0.125929453219066,
-0.794458204833014));
#73687=CARTESIAN_POINT('Ctrl Pts',(0.309721672874562,-0.0185269263353678,
-0.789179378491347));
#73688=CARTESIAN_POINT('Ctrl Pts',(0.284872700812218,0.0753805297300195,
-0.783900552149679));
#73689=CARTESIAN_POINT('Ctrl Pts',(0.260023728749873,0.169287985795408,
-0.778621725808011));
#73690=CARTESIAN_POINT('Ctrl Pts',(0.184175151279699,0.249700371042483,
-0.773342899466342));
#73691=CARTESIAN_POINT('Ctrl Pts',(0.0918780235207456,0.27998769388019,
-0.768064073124674));
#73692=CARTESIAN_POINT('Ctrl Pts',(-0.000419104238205001,0.310275016717896,
-0.762785246783006));
#73693=CARTESIAN_POINT('Ctrl Pts',(-0.109164782285933,0.290437277146233,
-0.757506420441339));
#73694=CARTESIAN_POINT('Ctrl Pts',(-0.184822446569363,0.229511095972593,
-0.752227594099671));
#73695=CARTESIAN_POINT('Ctrl Pts',(-0.252709637623149,0.174842380771212,
-0.747490933302768));
#73696=CARTESIAN_POINT('Ctrl Pts',(-0.293956442416001,0.0870918383276761,
-0.742754272505864));
#73697=CARTESIAN_POINT('Ctrl Pts',(-0.294553488267971,-0.000168236264217633,
-0.738017611708961));
#73698=CARTESIAN_POINT('Origin',(0.,0.,-0.975));
#73699=CARTESIAN_POINT('',(-0.294289870872604,0.000257612574092375,-0.62358238829104));
#73700=CARTESIAN_POINT('',(-0.294261921046506,0.000260993808666907,-0.63801761170896));
#73701=CARTESIAN_POINT('',(-0.2942,-3.60291088309151E-17,-0.975));
#73702=CARTESIAN_POINT('Ctrl Pts',(-0.294289870872604,0.000257612574092375,
-0.62358238829104));
#73703=CARTESIAN_POINT('Ctrl Pts',(-0.294469946841187,0.0199773350686368,
-0.624650326510748));
#73704=CARTESIAN_POINT('Ctrl Pts',(-0.292656187844798,0.0396641190350218,
-0.625718264730457));
#73705=CARTESIAN_POINT('Ctrl Pts',(-0.288726891356599,0.0589191948047397,
-0.626786202950165));
#73706=CARTESIAN_POINT('Ctrl Pts',(-0.269304350404941,0.154097173556868,
-0.632065029291833));
#73707=CARTESIAN_POINT('Ctrl Pts',(-0.198192203928323,0.238727087585969,
-0.637343855633501));
#73708=CARTESIAN_POINT('Ctrl Pts',(-0.107783936082899,0.274257748170153,
-0.642622681975169));
#73709=CARTESIAN_POINT('Ctrl Pts',(-0.0173756682374762,0.309788408754337,
-0.647901508316837));
#73710=CARTESIAN_POINT('Ctrl Pts',(0.0923287209767527,0.296219815893605,
-0.653180334658506));
#73711=CARTESIAN_POINT('Ctrl Pts',(0.171355948935814,0.239732826440589,
-0.658459161000174));
#73712=CARTESIAN_POINT('Ctrl Pts',(0.250383176894875,0.183245836987572,
-0.663737987341842));
#73713=CARTESIAN_POINT('Ctrl Pts',(0.298733243598769,0.0838404509422697,
-0.669016813683509));
#73714=CARTESIAN_POINT('Ctrl Pts',(0.29438140085294,-0.0132015203952617,
-0.674295640025178));
#73715=CARTESIAN_POINT('Ctrl Pts',(0.290029558107111,-0.110243491732796,
-0.679574466366846));
#73716=CARTESIAN_POINT('Ctrl Pts',(0.232975805911557,-0.204922048362555,
-0.684853292708514));
#73717=CARTESIAN_POINT('Ctrl Pts',(0.149209653926263,-0.254108576171862,
-0.690132119050183));
#73718=CARTESIAN_POINT('Ctrl Pts',(0.0654435019409706,-0.303295103981167,
-0.695410945391851));
#73719=CARTESIAN_POINT('Ctrl Pts',(-0.0450350498340619,-0.306989602970016,
-0.700689771733518));
#73720=CARTESIAN_POINT('Ctrl Pts',(-0.13190006702843,-0.263509130063423,
-0.705968598075186));
#73721=CARTESIAN_POINT('Ctrl Pts',(-0.218765084222795,-0.22002865715683,
-0.711247424416854));
#73722=CARTESIAN_POINT('Ctrl Pts',(-0.282016566836498,-0.129373212354797,
-0.716526250758523));
#73723=CARTESIAN_POINT('Ctrl Pts',(-0.292841773285728,-0.0328387747602788,
-0.721805077100191));
#73724=CARTESIAN_POINT('Ctrl Pts',(-0.294056674687428,-0.0220048175423813,
-0.722397514163807));
#73725=CARTESIAN_POINT('Ctrl Pts',(-0.294611249626576,-0.011096812446243,
-0.722989951227423));
#73726=CARTESIAN_POINT('Ctrl Pts',(-0.294532285647886,-0.000180704995970699,
-0.72358238829104));
#73727=CARTESIAN_POINT('Ctrl Pts',(-0.294553488267971,-0.000168236264217633,
-0.738017611708961));
#73728=CARTESIAN_POINT('Ctrl Pts',(-0.294621827062633,-0.010156159804845,
-0.737475446164196));
#73729=CARTESIAN_POINT('Ctrl Pts',(-0.294157595202237,-0.0201376575069966,
-0.73693328061943));
#73730=CARTESIAN_POINT('Ctrl Pts',(-0.293139784064339,-0.0300623839563357,
-0.736391115074665));
#73731=CARTESIAN_POINT('Ctrl Pts',(-0.283229806756751,-0.126695059936001,
-0.731112288732997));
#73732=CARTESIAN_POINT('Ctrl Pts',(-0.220840201622442,-0.217945789119709,
-0.725833462391329));
#73733=CARTESIAN_POINT('Ctrl Pts',(-0.134391102008002,-0.262247424451605,
-0.720554636049661));
#73734=CARTESIAN_POINT('Ctrl Pts',(-0.0479420023935621,-0.306549059783502,
-0.715275809707993));
#73735=CARTESIAN_POINT('Ctrl Pts',(0.0625665917010075,-0.303901601263588,
-0.709996983366325));
#73736=CARTESIAN_POINT('Ctrl Pts',(0.14679506082547,-0.255511037036901,
-0.704718157024657));
#73737=CARTESIAN_POINT('Ctrl Pts',(0.231023529949932,-0.207120472810213,
-0.699439330682989));
#73738=CARTESIAN_POINT('Ctrl Pts',(0.288971874104287,-0.112986802876749,
-0.694160504341321));
#73739=CARTESIAN_POINT('Ctrl Pts',(0.294243073071214,-0.0159904308895527,
-0.688881677999653));
#73740=CARTESIAN_POINT('Ctrl Pts',(0.299514272038142,0.0810059410976467,
-0.683602851657985));
#73741=CARTESIAN_POINT('Ctrl Pts',(0.252108325817643,0.180865015138582,
-0.678324025316316));
#73742=CARTESIAN_POINT('Ctrl Pts',(0.17361991047967,0.238098312920224,-0.673045198974648));
#73743=CARTESIAN_POINT('Ctrl Pts',(0.0951314951417017,0.295331610701864,
-0.66776637263298));
#73744=CARTESIAN_POINT('Ctrl Pts',(-0.0144393893137351,0.309939132224215,
-0.662487546291313));
#73745=CARTESIAN_POINT('Ctrl Pts',(-0.105180275250029,0.275266760849823,
-0.657208719949645));
#73746=CARTESIAN_POINT('Ctrl Pts',(-0.195921161186326,0.24059438947543,
-0.651929893607977));
#73747=CARTESIAN_POINT('Ctrl Pts',(-0.267832048603478,0.156642125204293,
-0.646651067266307));
#73748=CARTESIAN_POINT('Ctrl Pts',(-0.288155605489729,0.0616524691741799,
-0.641372240924639));
#73749=CARTESIAN_POINT('Ctrl Pts',(-0.292460728970111,0.0415308831320555,
-0.640254031186079));
#73750=CARTESIAN_POINT('Ctrl Pts',(-0.294451045139812,0.0209140313944282,
-0.63913582144752));
#73751=CARTESIAN_POINT('Ctrl Pts',(-0.294261921046506,0.000260993808666907,
-0.63801761170896));
#73752=CARTESIAN_POINT('Origin',(0.,0.,-0.975));
#73753=CARTESIAN_POINT('',(-0.293725317215226,-2.67421958787539E-5,-0.523582388291039));
#73754=CARTESIAN_POINT('',(-0.293728549452813,-4.17646313764225E-5,-0.538017611708961));
#73755=CARTESIAN_POINT('',(-0.2942,-3.60291088309151E-17,-0.975));
#73756=CARTESIAN_POINT('Ctrl Pts',(-0.293725317215226,-2.67421958787539E-5,
-0.523582388291039));
#73757=CARTESIAN_POINT('Ctrl Pts',(-0.293684051702583,0.0505977877572564,
-0.526310701794073));
#73758=CARTESIAN_POINT('Ctrl Pts',(-0.281256995427662,0.101241301522957,
-0.529039015297106));
#73759=CARTESIAN_POINT('Ctrl Pts',(-0.256560638597973,0.144952847612736,
-0.531767328800139));
#73760=CARTESIAN_POINT('Ctrl Pts',(-0.208777354590888,0.229527314834789,
-0.537046155141807));
#73761=CARTESIAN_POINT('Ctrl Pts',(-0.115063058962679,0.288151461053719,
-0.542324981483475));
#73762=CARTESIAN_POINT('Ctrl Pts',(-0.0181071191562859,0.294120420142335,
-0.547603807825143));
#73763=CARTESIAN_POINT('Ctrl Pts',(0.0788488206501062,0.30008937923095,
-0.552882634166811));
#73764=CARTESIAN_POINT('Ctrl Pts',(0.179046404634681,0.253403151189252,
-0.558161460508479));
#73765=CARTESIAN_POINT('Ctrl Pts',(0.23684295415351,0.17532856121226,-0.563440286850147));
#73766=CARTESIAN_POINT('Ctrl Pts',(0.29463950367234,0.0972539712352662,
-0.568719113191816));
#73767=CARTESIAN_POINT('Ctrl Pts',(0.31003501872542,-0.0122089806770256,
-0.573997939533484));
#73768=CARTESIAN_POINT('Ctrl Pts',(0.276016430552402,-0.103196993047219,
-0.579276765875152));
#73769=CARTESIAN_POINT('Ctrl Pts',(0.241997842379385,-0.194185005417411,
-0.58455559221682));
#73770=CARTESIAN_POINT('Ctrl Pts',(0.158565150980273,-0.266698078245509,
-0.589834418558488));
#73771=CARTESIAN_POINT('Ctrl Pts',(0.0637241781569158,-0.287704567963574,
-0.595113244900156));
#73772=CARTESIAN_POINT('Ctrl Pts',(-0.0311167946664433,-0.30871105768164,
-0.600392071241824));
#73773=CARTESIAN_POINT('Ctrl Pts',(-0.137366048914047,-0.278210964289672,
-0.605670897583492));
#73774=CARTESIAN_POINT('Ctrl Pts',(-0.206624208324501,-0.210097895856109,
-0.61094972392516));
#73775=CARTESIAN_POINT('Ctrl Pts',(-0.261871026828121,-0.155764509559018,
-0.61516061204712));
#73776=CARTESIAN_POINT('Ctrl Pts',(-0.293579830026457,-0.0774973958039037,
-0.61937150016908));
#73777=CARTESIAN_POINT('Ctrl Pts',(-0.294289870872604,0.000257612574092375,
-0.62358238829104));
#73778=CARTESIAN_POINT('Ctrl Pts',(-0.294261921046506,0.000260993808666907,
-0.63801761170896));
#73779=CARTESIAN_POINT('Ctrl Pts',(-0.293558231196988,-0.076584492436715,
-0.633856995105852));
#73780=CARTESIAN_POINT('Ctrl Pts',(-0.262681865646731,-0.15393094394333,
-0.629696378502744));
#73781=CARTESIAN_POINT('Ctrl Pts',(-0.208605769399056,-0.208130518915065,
-0.625535761899636));
#73782=CARTESIAN_POINT('Ctrl Pts',(-0.139996150066782,-0.276896803185108,
-0.620256935557968));
#73783=CARTESIAN_POINT('Ctrl Pts',(-0.0340406850468888,-0.308402323936105,
-0.614978109216299));
#73784=CARTESIAN_POINT('Ctrl Pts',(0.0609950782479923,-0.288295474053871,
-0.609699282874631));
#73785=CARTESIAN_POINT('Ctrl Pts',(0.156030841542874,-0.268188624171638,
-0.604420456532963));
#73786=CARTESIAN_POINT('Ctrl Pts',(0.24014690311274,-0.196469403656172,
-0.599141630191295));
#73787=CARTESIAN_POINT('Ctrl Pts',(0.27502614777056,-0.10580783512061,-0.593862803849627));
#73788=CARTESIAN_POINT('Ctrl Pts',(0.309905392428379,-0.0151462665850486,
-0.588583977507959));
#73789=CARTESIAN_POINT('Ctrl Pts',(0.295547820174153,0.0944576499706106,
-0.58330515116629));
#73790=CARTESIAN_POINT('Ctrl Pts',(0.238493689070395,0.173076399904854,
-0.578026324824622));
#73791=CARTESIAN_POINT('Ctrl Pts',(0.181439557966637,0.251695149839096,
-0.572747498482954));
#73792=CARTESIAN_POINT('Ctrl Pts',(0.081688868013349,0.299328733151925,
-0.567468672141286));
#73793=CARTESIAN_POINT('Ctrl Pts',(-0.0153192743263493,0.294278778991172,
-0.562189845799618));
#73794=CARTESIAN_POINT('Ctrl Pts',(-0.11232741666605,0.289228824830418,
-0.55691101945795));
#73795=CARTESIAN_POINT('Ctrl Pts',(-0.206593011392159,0.231495333196083,
-0.551632193116282));
#73796=CARTESIAN_POINT('Ctrl Pts',(-0.255175559581209,0.147377453237708,
-0.546353366774613));
#73797=CARTESIAN_POINT('Ctrl Pts',(-0.280747672014141,0.10310081555405,
-0.543574781752729));
#73798=CARTESIAN_POINT('Ctrl Pts',(-0.293662874536158,0.0515141394341178,
-0.540796196730845));
#73799=CARTESIAN_POINT('Ctrl Pts',(-0.293728549452813,-4.17646313764225E-5,
-0.538017611708961));
#73800=CARTESIAN_POINT('Origin',(0.,0.,-0.975));
#73801=CARTESIAN_POINT('',(-0.294386747729473,-0.000238138617797895,-0.423582388291039));
#73802=CARTESIAN_POINT('',(-0.294413163117196,-0.000230549972553652,-0.43801761170896));
#73803=CARTESIAN_POINT('',(-0.2942,-3.60291088309151E-17,-0.975));
#73804=CARTESIAN_POINT('Ctrl Pts',(-0.294386747729473,-0.000238138617797895,
-0.423582388291039));
#73805=CARTESIAN_POINT('Ctrl Pts',(-0.293675360816675,0.0807311351263202,
-0.427971077077397));
#73806=CARTESIAN_POINT('Ctrl Pts',(-0.258912863574874,0.162237187363098,
-0.432359765863755));
#73807=CARTESIAN_POINT('Ctrl Pts',(-0.199468139510034,0.216903551444156,
-0.436748454650113));
#73808=CARTESIAN_POINT('Ctrl Pts',(-0.127966515552986,0.282657642645915,
-0.442027280991781));
#73809=CARTESIAN_POINT('Ctrl Pts',(-0.0207549187866649,0.309580369841428,
-0.447306107333449));
#73810=CARTESIAN_POINT('Ctrl Pts',(0.0733289018073996,0.28540771094313,
-0.452584933675117));
#73811=CARTESIAN_POINT('Ctrl Pts',(0.167412722401464,0.261235052044833,
-0.457863760016785));
#73812=CARTESIAN_POINT('Ctrl Pts',(0.248368766823272,0.185967007052725,
-0.463142586358453));
#73813=CARTESIAN_POINT('Ctrl Pts',(0.279319392175962,0.0938901830065047,
-0.468421412700121));
#73814=CARTESIAN_POINT('Ctrl Pts',(0.310270017528652,0.00181335896028451,
-0.47370023904179));
#73815=CARTESIAN_POINT('Ctrl Pts',(0.291215223812225,-0.107072244140048,
-0.478979065383458));
#73816=CARTESIAN_POINT('Ctrl Pts',(0.230834979070049,-0.183166322631758,
-0.484257891725126));
#73817=CARTESIAN_POINT('Ctrl Pts',(0.170454734327874,-0.259260401123467,
-0.489536718066794));
#73818=CARTESIAN_POINT('Ctrl Pts',(0.0687490385599515,-0.302562955006556,
-0.494815544408462));
#73819=CARTESIAN_POINT('Ctrl Pts',(-0.0279524443521768,-0.293348513143104,
-0.50009437075013));
#73820=CARTESIAN_POINT('Ctrl Pts',(-0.124653927264306,-0.284134071279652,
-0.505373197091798));
#73821=CARTESIAN_POINT('Ctrl Pts',(-0.216351197320642,-0.222402633669659,
-0.510652023433466));
#73822=CARTESIAN_POINT('Ctrl Pts',(-0.26127369615583,-0.136274520752074,
-0.515930849775135));
#73823=CARTESIAN_POINT('Ctrl Pts',(-0.282978409023217,-0.0946609416066995,
-0.51848136261377));
#73824=CARTESIAN_POINT('Ctrl Pts',(-0.29376389350775,-0.0473521369687958,
-0.521031875452404));
#73825=CARTESIAN_POINT('Ctrl Pts',(-0.293725317215226,-2.67421958787539E-5,
-0.523582388291039));
#73826=CARTESIAN_POINT('Ctrl Pts',(-0.293728549452813,-4.17646313764225E-5,
-0.538017611708961));
#73827=CARTESIAN_POINT('Ctrl Pts',(-0.293787645409568,-0.0464330755353523,
-0.535517370389177));
#73828=CARTESIAN_POINT('Ctrl Pts',(-0.283442662454548,-0.092799470746512,
-0.533017129069394));
#73829=CARTESIAN_POINT('Ctrl Pts',(-0.262553264006026,-0.133792613735755,
-0.53051688774961));
#73830=CARTESIAN_POINT('Ctrl Pts',(-0.218448918589804,-0.220342532468435,
-0.525238061407942));
#73831=CARTESIAN_POINT('Ctrl Pts',(-0.12734072610537,-0.282940101651383,
-0.519959235066273));
#73832=CARTESIAN_POINT('Ctrl Pts',(-0.0307309043311849,-0.29307045475341,
-0.514680408724605));
#73833=CARTESIAN_POINT('Ctrl Pts',(0.0658789174429986,-0.303200807855436,
-0.509401582382937));
#73834=CARTESIAN_POINT('Ctrl Pts',(0.167990368506934,-0.260863944876541,
-0.504122756041269));
#73835=CARTESIAN_POINT('Ctrl Pts',(0.229088952588978,-0.185345438929759,
-0.498843929699601));
#73836=CARTESIAN_POINT('Ctrl Pts',(0.290187536671023,-0.109826932982976,
-0.493565103357933));
#73837=CARTESIAN_POINT('Ctrl Pts',(0.310273253771179,-0.00112678406830562,
-0.488286277016264));
#73838=CARTESIAN_POINT('Ctrl Pts',(0.280196522685982,0.0912391834978892,
-0.483007450674596));
#73839=CARTESIAN_POINT('Ctrl Pts',(0.250119791600785,0.183605151064081,
-0.477728624332928));
#73840=CARTESIAN_POINT('Ctrl Pts',(0.169880612330235,0.2596369372818,-0.47244979799126));
#73841=CARTESIAN_POINT('Ctrl Pts',(0.0760300765142607,0.284700030550235,
-0.467170971649592));
#73842=CARTESIAN_POINT('Ctrl Pts',(-0.0178204593017165,0.309763123818671,
-0.461892145307924));
#73843=CARTESIAN_POINT('Ctrl Pts',(-0.125282351663119,0.283857524137824,
-0.456613318966256));
#73844=CARTESIAN_POINT('Ctrl Pts',(-0.197403835228254,0.218783924837785,
-0.451334492624587));
#73845=CARTESIAN_POINT('Ctrl Pts',(-0.258050725649971,0.164063593932058,
-0.446895532319378));
#73846=CARTESIAN_POINT('Ctrl Pts',(-0.29370801395702,0.0816471282206012,
-0.442456572014169));
#73847=CARTESIAN_POINT('Ctrl Pts',(-0.294413163117196,-0.000230549972553652,
-0.43801761170896));
#73848=CARTESIAN_POINT('Origin',(0.,0.,-0.975));
#73849=CARTESIAN_POINT('',(-0.294448752700369,0.000218575078071742,-0.323582388291039));
#73850=CARTESIAN_POINT('',(-0.294423182665938,0.000227389813808373,-0.33801761170896));
#73851=CARTESIAN_POINT('',(-0.2942,-3.60291088309151E-17,-0.975));
#73852=CARTESIAN_POINT('Ctrl Pts',(-0.294448752700369,0.000218575078071742,
-0.323582388291039));
#73853=CARTESIAN_POINT('Ctrl Pts',(-0.294566832082909,0.0144213289353346,
-0.324352626019054));
#73854=CARTESIAN_POINT('Ctrl Pts',(-0.293627558021379,0.0286084018818293,
-0.325122863747068));
#73855=CARTESIAN_POINT('Ctrl Pts',(-0.291576951458356,0.0426329811729054,
-0.325893101475082));
#73856=CARTESIAN_POINT('Ctrl Pts',(-0.277523113860461,0.138750473084658,
-0.33117192781675));
#73857=CARTESIAN_POINT('Ctrl Pts',(-0.211269433961597,0.227235556895007,
-0.336450754158418));
#73858=CARTESIAN_POINT('Ctrl Pts',(-0.122996237149932,0.267780908662382,
-0.341729580500087));
#73859=CARTESIAN_POINT('Ctrl Pts',(-0.0347230403382674,0.308326260429757,
-0.347008406841755));
#73860=CARTESIAN_POINT('Ctrl Pts',(0.0755696733861977,0.300931880154159,
-0.352287233183423));
#73861=CARTESIAN_POINT('Ctrl Pts',(0.157640625250177,0.248966106971692,
-0.357566059525091));
#73862=CARTESIAN_POINT('Ctrl Pts',(0.239711577114155,0.197000333789225,
-0.362844885866759));
#73863=CARTESIAN_POINT('Ctrl Pts',(0.293560767117647,0.100463167699891,
-0.368123712208427));
#73864=CARTESIAN_POINT('Ctrl Pts',(0.294658448633633,0.00332986849060328,
-0.373402538550095));
#73865=CARTESIAN_POINT('Ctrl Pts',(0.295756130149619,-0.0938034307186845,
-0.378681364891763));
#73866=CARTESIAN_POINT('Ctrl Pts',(0.244102303178098,-0.191532863047926,
-0.383960191233431));
#73867=CARTESIAN_POINT('Ctrl Pts',(0.163226667435956,-0.245340058596889,
-0.3892390175751));
#73868=CARTESIAN_POINT('Ctrl Pts',(0.0823510316938124,-0.299147254145853,
-0.394517843916768));
#73869=CARTESIAN_POINT('Ctrl Pts',(-0.0277464128189549,-0.309032212914535,
-0.399796670258436));
#73870=CARTESIAN_POINT('Ctrl Pts',(-0.116913336480491,-0.270492072047274,
-0.405075496600104));
#73871=CARTESIAN_POINT('Ctrl Pts',(-0.206080260142024,-0.231951931180014,
-0.410354322941772));
#73872=CARTESIAN_POINT('Ctrl Pts',(-0.274316662952327,-0.144986690676814,
-0.41563314928344));
#73873=CARTESIAN_POINT('Ctrl Pts',(-0.290539038783592,-0.049211342821212,
-0.420911975625108));
#73874=CARTESIAN_POINT('Ctrl Pts',(-0.293274522966844,-0.0330613070971267,
-0.421802113180419));
#73875=CARTESIAN_POINT('Ctrl Pts',(-0.294531035064088,-0.0166607638925458,
-0.422692250735729));
#73876=CARTESIAN_POINT('Ctrl Pts',(-0.294386747729473,-0.000238138617797895,
-0.423582388291039));
#73877=CARTESIAN_POINT('Ctrl Pts',(-0.294413163117196,-0.000230549972553652,
-0.43801761170896));
#73878=CARTESIAN_POINT('Ctrl Pts',(-0.294546579680884,-0.0157220786933341,
-0.437177745672501));
#73879=CARTESIAN_POINT('Ctrl Pts',(-0.293428783164059,-0.0311943199539772,
-0.436337879636042));
#73880=CARTESIAN_POINT('Ctrl Pts',(-0.290992296495885,-0.0464560363369899,
-0.435498013599583));
#73881=CARTESIAN_POINT('Ctrl Pts',(-0.275678199429516,-0.142380799292502,
-0.430219187257915));
#73882=CARTESIAN_POINT('Ctrl Pts',(-0.208268930527908,-0.229988726284298,
-0.424940360916247));
#73883=CARTESIAN_POINT('Ctrl Pts',(-0.1194712142193,-0.269372064068582,
-0.419661534574579));
#73884=CARTESIAN_POINT('Ctrl Pts',(-0.0306734979106905,-0.308755401852867,
-0.414382708232911));
#73885=CARTESIAN_POINT('Ctrl Pts',(0.0795126658049214,-0.299914150429641,
-0.409103881891243));
#73886=CARTESIAN_POINT('Ctrl Pts',(0.160894533168858,-0.246875736204659,
-0.403825055549575));
#73887=CARTESIAN_POINT('Ctrl Pts',(0.242276400532795,-0.193837321979676,
-0.398546229207906));
#73888=CARTESIAN_POINT('Ctrl Pts',(0.294853971545057,-0.0966017449529404,
-0.393267402866238));
#73889=CARTESIAN_POINT('Ctrl Pts',(0.29467675669896,0.000537589563172465,
-0.38798857652457));
#73890=CARTESIAN_POINT('Ctrl Pts',(0.294499541852863,0.0976769240792826,
-0.382709750182902));
#73891=CARTESIAN_POINT('Ctrl Pts',(0.241567541148409,0.194720016084768,
-0.377430923841234));
#73892=CARTESIAN_POINT('Ctrl Pts',(0.159992696350693,0.247461142451306,
-0.372152097499566));
#73893=CARTESIAN_POINT('Ctrl Pts',(0.0784178515529763,0.300202268817844,
-0.366873271157898));
#73894=CARTESIAN_POINT('Ctrl Pts',(-0.0317998373380048,0.308641429545435,
-0.36159444481623));
#73895=CARTESIAN_POINT('Ctrl Pts',(-0.120453266197856,0.268934361133685,
-0.356315618474562));
#73896=CARTESIAN_POINT('Ctrl Pts',(-0.209106695057707,0.229227292721936,
-0.351036792132893));
#73897=CARTESIAN_POINT('Ctrl Pts',(-0.27619586388643,0.141373995170845,
-0.345757965791225));
#73898=CARTESIAN_POINT('Ctrl Pts',(-0.291159861981142,0.0453939948487563,
-0.340479139449557));
#73899=CARTESIAN_POINT('Ctrl Pts',(-0.293485776495486,0.0304754366918415,
-0.339658630202691));
#73900=CARTESIAN_POINT('Ctrl Pts',(-0.29455236057389,0.0153605395301952,
-0.338838120955826));
#73901=CARTESIAN_POINT('Ctrl Pts',(-0.294423182665938,0.000227389813808373,
-0.33801761170896));
#73902=CARTESIAN_POINT('Origin',(0.,0.,-0.975));
#73903=CARTESIAN_POINT('',(-0.293735363568813,6.2383603337629E-5,-0.223582388291039));
#73904=CARTESIAN_POINT('',(-0.293730171905116,4.7521135793488E-5,-0.23801761170896));
#73905=CARTESIAN_POINT('',(-0.2942,-3.60291088309151E-17,-0.975));
#73906=CARTESIAN_POINT('Ctrl Pts',(-0.293735363568813,6.2383603337629E-5,
-0.223582388291039));
#73907=CARTESIAN_POINT('Ctrl Pts',(-0.29382126570124,0.0451591115892455,
-0.226013001302378));
#73908=CARTESIAN_POINT('Ctrl Pts',(-0.284069503228078,0.0902206310502946,
-0.228443614313717));
#73909=CARTESIAN_POINT('Ctrl Pts',(-0.264286630962371,0.130335250310531,
-0.230874227325056));
#73910=CARTESIAN_POINT('Ctrl Pts',(-0.221322018026089,0.21745652706214,
-0.236153053666724));
#73911=CARTESIAN_POINT('Ctrl Pts',(-0.131043140145507,0.281244498566885,
-0.241431880008393));
#73912=CARTESIAN_POINT('Ctrl Pts',(-0.0345745696175421,0.292641926382959,
-0.246710706350061));
#73913=CARTESIAN_POINT('Ctrl Pts',(0.0618940009104224,0.304039354199033,
-0.251989532691729));
#73914=CARTESIAN_POINT('Ctrl Pts',(0.16455226408577,0.263046238326436,-0.257268359033397));
#73915=CARTESIAN_POINT('Ctrl Pts',(0.226636703894443,0.188336097685639,
-0.262547185375065));
#73916=CARTESIAN_POINT('Ctrl Pts',(0.288721143703115,0.113625957044842,
-0.267826011716733));
#73917=CARTESIAN_POINT('Ctrl Pts',(0.310231760145113,0.00519879163584851,
-0.273104838058401));
#73918=CARTESIAN_POINT('Ctrl Pts',(0.281369856774462,-0.0875539561617508,
-0.278383664400069));
#73919=CARTESIAN_POINT('Ctrl Pts',(0.252507953403812,-0.180306703959349,
-0.283662490741737));
#73920=CARTESIAN_POINT('Ctrl Pts',(0.173273530220512,-0.257385034145551,
-0.288941317083405));
#73921=CARTESIAN_POINT('Ctrl Pts',(0.0797600041809775,-0.283677690310886,
-0.294220143425073));
#73922=CARTESIAN_POINT('Ctrl Pts',(-0.0137535218585596,-0.309970346476223,
-0.299498969766742));
#73923=CARTESIAN_POINT('Ctrl Pts',(-0.121546150754334,-0.285477328620691,
-0.30477779610841));
#73924=CARTESIAN_POINT('Ctrl Pts',(-0.194515467553757,-0.221355869686345,
-0.310056622450078));
#73925=CARTESIAN_POINT('Ctrl Pts',(-0.256837773607114,-0.166590423556724,
-0.314565211063732));
#73926=CARTESIAN_POINT('Ctrl Pts',(-0.293757574716917,-0.0829172828452477,
-0.319073799677386));
#73927=CARTESIAN_POINT('Ctrl Pts',(-0.294448752700369,0.000218575078071742,
-0.323582388291039));
#73928=CARTESIAN_POINT('Ctrl Pts',(-0.294423182665938,0.000227389813808373,
-0.33801761170896));
#73929=CARTESIAN_POINT('Ctrl Pts',(-0.293721281892129,-0.0820000565391896,
-0.333559294614158));
#73930=CARTESIAN_POINT('Ctrl Pts',(-0.257715724385328,-0.164766391010743,
-0.329100977519356));
#73931=CARTESIAN_POINT('Ctrl Pts',(-0.196604252665232,-0.219502728012081,
-0.324642660424553));
#73932=CARTESIAN_POINT('Ctrl Pts',(-0.124245817893906,-0.284312747457746,
-0.319363834082885));
#73933=CARTESIAN_POINT('Ctrl Pts',(-0.0166901209905529,-0.309826083255983,
-0.314085007741217));
#73934=CARTESIAN_POINT('Ctrl Pts',(0.0770683438040029,-0.284420727799746,
-0.308806181399548));
#73935=CARTESIAN_POINT('Ctrl Pts',(0.170826808598556,-0.259015372343509,
-0.30352735505788));
#73936=CARTESIAN_POINT('Ctrl Pts',(0.250788041284313,-0.182691325632801,
-0.298248528716212));
#73937=CARTESIAN_POINT('Ctrl Pts',(0.280527559302708,-0.090216233574742,
-0.292969702374544));
#73938=CARTESIAN_POINT('Ctrl Pts',(0.310267077321103,0.00225885848331649,
-0.287690876032876));
#73939=CARTESIAN_POINT('Ctrl Pts',(0.289784880672137,0.110884995888725,
-0.282412049691208));
#73940=CARTESIAN_POINT('Ctrl Pts',(0.228411163365634,0.18618007205291,-0.27713322334954));
#73941=CARTESIAN_POINT('Ctrl Pts',(0.16703744605913,0.261475148217097,-0.271854397007872));
#73942=CARTESIAN_POINT('Ctrl Pts',(0.0647722080950876,0.303439163140058,
-0.266575570666204));
#73943=CARTESIAN_POINT('Ctrl Pts',(-0.0318000112318368,0.292956379272552,
-0.261296744324536));
#73944=CARTESIAN_POINT('Ctrl Pts',(-0.128372230558761,0.282473595405046,
-0.256017917982867));
#73945=CARTESIAN_POINT('Ctrl Pts',(-0.219251431248568,0.219544012747072,
-0.250739091641199));
#73946=CARTESIAN_POINT('Ctrl Pts',(-0.263039686358181,0.132833751630507,
-0.245460265299531));
#73947=CARTESIAN_POINT('Ctrl Pts',(-0.283618807108558,0.0920826203203491,
-0.242979380769341));
#73948=CARTESIAN_POINT('Ctrl Pts',(-0.293796911898982,0.0460790309603713,
-0.240498496239151));
#73949=CARTESIAN_POINT('Ctrl Pts',(-0.293730171905116,4.7521135793488E-5,
-0.23801761170896));
#73950=CARTESIAN_POINT('Origin',(0.,0.,-0.975));
#73951=CARTESIAN_POINT('',(-0.294218898388376,-0.000260431939339084,-0.123582388291039));
#73952=CARTESIAN_POINT('',(-0.29425044853364,-0.000261621567235155,-0.138017611708961));
#73953=CARTESIAN_POINT('',(-0.2942,-3.60291088309151E-17,-0.975));
#73954=CARTESIAN_POINT('Ctrl Pts',(-0.294218898388376,-0.000260431939339084,
-0.123582388291039));
#73955=CARTESIAN_POINT('Ctrl Pts',(-0.293528319942296,0.0753241966819701,
-0.127673376585703));
#73956=CARTESIAN_POINT('Ctrl Pts',(-0.263787073930481,0.151388528324872,
-0.131764364880366));
#73957=CARTESIAN_POINT('Ctrl Pts',(-0.211321206681247,0.205373225174826,
-0.13585535317503));
#73958=CARTESIAN_POINT('Ctrl Pts',(-0.143621623567071,0.275032637339418,
-0.141134179516698));
#73959=CARTESIAN_POINT('Ctrl Pts',(-0.0380851942254879,0.30792911569359,
-0.146413005858366));
#73960=CARTESIAN_POINT('Ctrl Pts',(0.0572071270478631,0.289072004190402,
-0.151691832200035));
#73961=CARTESIAN_POINT('Ctrl Pts',(0.152499448321213,0.270214892687215,
-0.156970658541703));
#73962=CARTESIAN_POINT('Ctrl Pts',(0.237547661526332,0.199604191326667,
-0.162249484883371));
#73963=CARTESIAN_POINT('Ctrl Pts',(0.273613323874537,0.109407805679064,
-0.167528311225039));
#73964=CARTESIAN_POINT('Ctrl Pts',(0.309678986222741,0.0192114200314617,
-0.172807137566707));
#73965=CARTESIAN_POINT('Ctrl Pts',(0.296762097714034,-0.0905706499031973,
-0.178085963908375));
#73966=CARTESIAN_POINT('Ctrl Pts',(0.240744922753791,-0.169931224311318,
-0.183364790250043));
#73967=CARTESIAN_POINT('Ctrl Pts',(0.184727747793547,-0.249291798719439,
-0.188643616591711));
#73968=CARTESIAN_POINT('Ctrl Pts',(0.0856102863817663,-0.29823087760102,
-0.193922442933379));
#73969=CARTESIAN_POINT('Ctrl Pts',(-0.0114559051328922,-0.294454622701047,
-0.199201269275047));
#73970=CARTESIAN_POINT('Ctrl Pts',(-0.108522096647551,-0.290678367801075,
-0.204480095616716));
#73971=CARTESIAN_POINT('Ctrl Pts',(-0.203537018265085,-0.234186779119548,
-0.209758921958384));
#73972=CARTESIAN_POINT('Ctrl Pts',(-0.253219305077861,-0.150713693779547,
-0.215037748300052));
#73973=CARTESIAN_POINT('Ctrl Pts',(-0.28002559542017,-0.105675433567722,
-0.217885961630381));
#73974=CARTESIAN_POINT('Ctrl Pts',(-0.293634702707729,-0.0527823519446433,
-0.22073417496071));
#73975=CARTESIAN_POINT('Ctrl Pts',(-0.293735363568813,6.2383603337629E-5,
-0.223582388291039));
#73976=CARTESIAN_POINT('Ctrl Pts',(-0.293730171905116,4.7521135793488E-5,
-0.23801761170896));
#73977=CARTESIAN_POINT('Ctrl Pts',(-0.293654902533621,-0.0518668200664407,
-0.235219669897483));
#73978=CARTESIAN_POINT('Ctrl Pts',(-0.280548876420359,-0.103816674230558,
-0.232421728086005));
#73979=CARTESIAN_POINT('Ctrl Pts',(-0.254636118965327,-0.14830751416629,
-0.229623786274527));
#73980=CARTESIAN_POINT('Ctrl Pts',(-0.20574698693344,-0.232247579271372,
-0.224344959932859));
#73981=CARTESIAN_POINT('Ctrl Pts',(-0.111271413340247,-0.289636769906379,
-0.219066133591191));
#73982=CARTESIAN_POINT('Ctrl Pts',(-0.0142454713261084,-0.294332728605281,
-0.213787307249522));
#73983=CARTESIAN_POINT('Ctrl Pts',(0.0827804706880292,-0.299028687304183,
-0.208508480907854));
#73984=CARTESIAN_POINT('Ctrl Pts',(0.182356781123111,-0.25103141406698,
-0.203229654566186));
#73985=CARTESIAN_POINT('Ctrl Pts',(0.239123641436347,-0.172205039277174,
-0.197950828224518));
#73986=CARTESIAN_POINT('Ctrl Pts',(0.295890501749582,-0.093378664487369,
-0.19267200188285));
#73987=CARTESIAN_POINT('Ctrl Pts',(0.309847911940974,0.0162768118550433,
-0.187393175541182));
#73988=CARTESIAN_POINT('Ctrl Pts',(0.274638178457899,0.106810558300942,
-0.182114349199514));
#73989=CARTESIAN_POINT('Ctrl Pts',(0.239428444974822,0.197344304746844,
-0.176835522857845));
#73990=CARTESIAN_POINT('Ctrl Pts',(0.155051567817281,0.268756321296234,
-0.171556696516177));
#73991=CARTESIAN_POINT('Ctrl Pts',(0.0599429359410212,0.288516200200336,
-0.166277870174509));
#73992=CARTESIAN_POINT('Ctrl Pts',(-0.0351656959352371,0.308276079104439,
-0.160999043832841));
#73993=CARTESIAN_POINT('Ctrl Pts',(-0.141006082530208,0.276383820363254,
-0.155720217491173));
#73994=CARTESIAN_POINT('Ctrl Pts',(-0.209364076589891,0.207367820782157,
-0.150441391149505));
#73995=CARTESIAN_POINT('Ctrl Pts',(-0.262991189021549,0.153224500457582,
-0.14630013133599));
#73996=CARTESIAN_POINT('Ctrl Pts',(-0.293549899495509,0.0762335090548516,
-0.142158871522476));
#73997=CARTESIAN_POINT('Ctrl Pts',(-0.29425044853364,-0.000261621567235155,
-0.138017611708961));
#73998=CARTESIAN_POINT('Origin',(0.,0.,-0.975));
#73999=CARTESIAN_POINT('',(-0.2942,-3.60291088309151E-17,-0.025));
#74000=CARTESIAN_POINT('',(-0.294543724507234,0.000174101626290112,-0.0380176117089602));
#74001=CARTESIAN_POINT('',(-0.2942,-3.60291088309151E-17,-0.975));
#74002=CARTESIAN_POINT('',(-0.293033728012268,0.0261701021632011,-0.0249999999999999));
#74003=CARTESIAN_POINT('Origin',(0.,0.,-0.025));
#74004=CARTESIAN_POINT('Ctrl Pts',(-0.293033728012268,0.0261701021632011,
-0.0249999999999999));
#74005=CARTESIAN_POINT('Ctrl Pts',(-0.284353669323579,0.123363072257456,
-0.030278826341668));
#74006=CARTESIAN_POINT('Ctrl Pts',(-0.223613800042068,0.215068700053739,
-0.0355576526833361));
#74007=CARTESIAN_POINT('Ctrl Pts',(-0.137883282056386,0.260401867148505,
-0.0408364790250042));
#74008=CARTESIAN_POINT('Ctrl Pts',(-0.0521527640707002,0.305735034243272,
-0.0461153053666725));
#74009=CARTESIAN_POINT('Ctrl Pts',(0.0585684026191602,0.30469574063652,
-0.0513941317083408));
#74010=CARTESIAN_POINT('Ctrl Pts',(0.14347220086852,0.257453935168375,-0.0566729580500089));
#74011=CARTESIAN_POINT('Ctrl Pts',(0.228375999117877,0.21021212970023,-0.0619517843916768));
#74012=CARTESIAN_POINT('Ctrl Pts',(0.287462428926736,0.116767812370693,
-0.0672306107333447));
#74013=CARTESIAN_POINT('Ctrl Pts',(0.293983851229169,0.0198299008762353,
-0.0725094370750127));
#74014=CARTESIAN_POINT('Ctrl Pts',(0.300505273531603,-0.0771080106182236,
-0.0777882634166808));
#74015=CARTESIAN_POINT('Ctrl Pts',(0.254461688327612,-0.177539516277601,
-0.0830670897583489));
#74016=CARTESIAN_POINT('Ctrl Pts',(0.176742574349081,-0.235788167911957,
-0.0883459161000171));
#74017=CARTESIAN_POINT('Ctrl Pts',(0.0990234603705489,-0.294036819546313,
-0.0936247424416854));
#74018=CARTESIAN_POINT('Ctrl Pts',(-0.0103711823825235,-0.310102617155643,
-0.0989035687833535));
#74019=CARTESIAN_POINT('Ctrl Pts',(-0.101565243497955,-0.276629259989442,
-0.104182395125022));
#74020=CARTESIAN_POINT('Ctrl Pts',(-0.192759304613383,-0.243155902823242,
-0.10946122146669));
#74021=CARTESIAN_POINT('Ctrl Pts',(-0.265752784091173,-0.160143390881513,
-0.114740047808358));
#74022=CARTESIAN_POINT('Ctrl Pts',(-0.287318155386683,-0.0654259619231444,
-0.120018874150026));
#74023=CARTESIAN_POINT('Ctrl Pts',(-0.292170781115319,-0.0441127080767178,
-0.12120671219703));
#74024=CARTESIAN_POINT('Ctrl Pts',(-0.294419411148035,-0.0222067909064837,
-0.122394550244035));
#74025=CARTESIAN_POINT('Ctrl Pts',(-0.294218898388376,-0.000260431939339084,
-0.123582388291039));
#74026=CARTESIAN_POINT('Ctrl Pts',(-0.29425044853364,-0.000261621567235155,
-0.138017611708961));
#74027=CARTESIAN_POINT('Ctrl Pts',(-0.294442883003582,-0.0212741404819942,
-0.136880045180808));
#74028=CARTESIAN_POINT('Ctrl Pts',(-0.292382366633133,-0.0422492441672564,
-0.135742478652654));
#74029=CARTESIAN_POINT('Ctrl Pts',(-0.287928169201029,-0.0627030951006328,
-0.134604912124501));
#74030=CARTESIAN_POINT('Ctrl Pts',(-0.267258666228093,-0.157618270981318,
-0.129326085782833));
#74031=CARTESIAN_POINT('Ctrl Pts',(-0.195044058757831,-0.241308882321678,
-0.124047259441165));
#74032=CARTESIAN_POINT('Ctrl Pts',(-0.104176307233433,-0.275649355995977,
-0.118768433099497));
#74033=CARTESIAN_POINT('Ctrl Pts',(-0.0133085557090344,-0.309989829670276,
-0.113489606757829));
#74034=CARTESIAN_POINT('Ctrl Pts',(0.0962123398695022,-0.294980165678509,
-0.10821078041616));
#74035=CARTESIAN_POINT('Ctrl Pts',(0.174489570858358,-0.23746198694934,
-0.102931954074492));
#74036=CARTESIAN_POINT('Ctrl Pts',(0.252766801847212,-0.179943808220172,
-0.097653127732824));
#74037=CARTESIAN_POINT('Ctrl Pts',(0.29980036824639,-0.0799171147536053,
-0.0923743013911559));
#74038=CARTESIAN_POINT('Ctrl Pts',(0.294178806556978,0.0170615097418389,
-0.0870954750494878));
#74039=CARTESIAN_POINT('Ctrl Pts',(0.288557244867566,0.114040134237284,
-0.0818166487078195));
#74040=CARTESIAN_POINT('Ctrl Pts',(0.230280555089563,0.207970689761605,
-0.0765378223661514));
#74041=CARTESIAN_POINT('Ctrl Pts',(0.145869376933614,0.256049538454383,
-0.0712589960244833));
#74042=CARTESIAN_POINT('Ctrl Pts',(0.0614581987776668,0.304128387147161,
-0.0659801696828152));
#74043=CARTESIAN_POINT('Ctrl Pts',(-0.049087467756228,0.306355529008397,
-0.060701343341147));
#74044=CARTESIAN_POINT('Ctrl Pts',(-0.135361470776523,0.261746566404462,
-0.0554225169994788));
#74045=CARTESIAN_POINT('Ctrl Pts',(-0.221635473796818,0.217137603800527,
-0.0501436906578107));
#74046=CARTESIAN_POINT('Ctrl Pts',(-0.283637813303516,0.125692536731422,
-0.0448648643161426));
#74047=CARTESIAN_POINT('Ctrl Pts',(-0.293220335795911,0.0290092329209717,
-0.0395860379744745));
#74048=CARTESIAN_POINT('Ctrl Pts',(-0.294169377558491,0.0194338321709952,
-0.0390632292193031));
#74049=CARTESIAN_POINT('Ctrl Pts',(-0.294604249652088,0.00980705118726834,
-0.0385404204641317));
#74050=CARTESIAN_POINT('Ctrl Pts',(-0.294543724507234,0.000174101626290112,
-0.0380176117089602));
#74051=CARTESIAN_POINT('Origin',(0.,0.,-2.1406589891905));
#74052=CARTESIAN_POINT('',(-0.237190235300011,-0.000209952227111018,-0.0906589891905002));
#74053=CARTESIAN_POINT('',(-0.237452100135973,0.00014035538139405,-0.0709410108094966));
#74054=CARTESIAN_POINT('',(-0.237175,-2.3095687792789E-14,-2.1406589891905));
#74055=CARTESIAN_POINT('',(0.131476569578105,0.197850242677352,-0.0250000000000002));
#74056=CARTESIAN_POINT('Ctrl Pts',(-0.237190235300011,-0.000209952227111019,
-0.0906589891905003));
#74057=CARTESIAN_POINT('Ctrl Pts',(-0.237351882525612,-0.0179024324719509,
-0.0894711511434962));
#74058=CARTESIAN_POINT('Ctrl Pts',(-0.227483014572861,-0.114043905631837,
-0.0830044867548241));
#74059=CARTESIAN_POINT('Ctrl Pts',(-0.0965515281323339,-0.262946953677372,
-0.0712589960244833));
#74060=CARTESIAN_POINT('Ctrl Pts',(0.168020270592608,-0.224091696559834,
-0.0554225169994791));
#74061=CARTESIAN_POINT('Ctrl Pts',(0.276446148350078,0.0124097424002016,
-0.0400028516579843));
#74062=CARTESIAN_POINT('Ctrl Pts',(0.19136777761438,0.157552650588978,-0.0298620126581583));
#74063=CARTESIAN_POINT('Ctrl Pts',(0.131476569578105,0.197850242677352,
-0.0250000000000002));
#74064=CARTESIAN_POINT('',(0.229503519150545,-0.0598340649004849,-0.0249999999999999));
#74065=CARTESIAN_POINT('Origin',(0.,0.,-0.0249999999999999));
#74066=CARTESIAN_POINT('Ctrl Pts',(-0.237452100135973,0.000140355381394047,
-0.0709410108094966));
#74067=CARTESIAN_POINT('Ctrl Pts',(-0.237008223098924,-0.0705054087783698,
-0.0661849932230005));
#74068=CARTESIAN_POINT('Ctrl Pts',(-0.16633709501764,-0.220431044668647,
-0.0561501492948366));
#74069=CARTESIAN_POINT('Ctrl Pts',(0.0886436604710861,-0.265605608028242,
-0.0408364790250042));
#74070=CARTESIAN_POINT('Ctrl Pts',(0.209657849780202,-0.135955434357285,
-0.030278826341668));
#74071=CARTESIAN_POINT('Ctrl Pts',(0.229503519150545,-0.0598340649004849,
-0.0249999999999999));
#74072=CARTESIAN_POINT('Origin',(0.,0.,-2.1406589891905));
#74073=CARTESIAN_POINT('',(-0.236800424386245,5.02917441071152E-5,-0.1906589891905));
#74074=CARTESIAN_POINT('',(-0.237215670057668,-0.000210911268586855,-0.170941010809497));
#74075=CARTESIAN_POINT('',(-0.237175,-2.3095687792789E-14,-2.1406589891905));
#74076=CARTESIAN_POINT('Ctrl Pts',(-0.236800424386245,5.02917441071067E-5,
-0.1906589891905));
#74077=CARTESIAN_POINT('Ctrl Pts',(-0.236719274693082,-0.0425515102735373,
-0.187810775860172));
#74078=CARTESIAN_POINT('Ctrl Pts',(-0.205414127958568,-0.164221921599079,
-0.179683736188175));
#74079=CARTESIAN_POINT('Ctrl Pts',(-0.0108890694688725,-0.279877751287428,
-0.166277870174509));
#74080=CARTESIAN_POINT('Ctrl Pts',(0.228827285837098,-0.161518206415849,
-0.150441391149505));
#74081=CARTESIAN_POINT('Ctrl Pts',(0.260066881677195,0.103990587976603,
-0.134604912124501));
#74082=CARTESIAN_POINT('Ctrl Pts',(0.054377113149757,0.274763121238199,
-0.118768433099496));
#74083=CARTESIAN_POINT('Ctrl Pts',(-0.181718869422876,0.201170273454141,
-0.104119792121496));
#74084=CARTESIAN_POINT('Ctrl Pts',(-0.236633512176461,0.0607240528485506,
-0.0947499774851641));
#74085=CARTESIAN_POINT('Ctrl Pts',(-0.237190235300011,-0.000209952227111019,
-0.0906589891905003));
#74086=CARTESIAN_POINT('Ctrl Pts',(-0.237215670057668,-0.00021091126858686,
-0.170941010809497));
#74087=CARTESIAN_POINT('Ctrl Pts',(-0.237370804814323,-0.0171505583576599,
-0.169803444281345));
#74088=CARTESIAN_POINT('Ctrl Pts',(-0.228001304010126,-0.112527743254352,
-0.163387051411524));
#74089=CARTESIAN_POINT('Ctrl Pts',(-0.0990213293987983,-0.262004605402092,
-0.151691832200035));
#74090=CARTESIAN_POINT('Ctrl Pts',(0.165855812771546,-0.225703615695282,
-0.13585535317503));
#74091=CARTESIAN_POINT('Ctrl Pts',(0.279606860807486,0.0162117244434021,
-0.120018874150026));
#74092=CARTESIAN_POINT('Ctrl Pts',(0.138664230983235,0.2433835073103,-0.104182395125021));
#74093=CARTESIAN_POINT('Ctrl Pts',(-0.128691327754114,0.248769867313068,
-0.0883459161000173));
#74094=CARTESIAN_POINT('Ctrl Pts',(-0.233610483961208,0.0940282986476538,
-0.0772654546615087));
#74095=CARTESIAN_POINT('Ctrl Pts',(-0.237500893647975,0.00790614332200466,
-0.0714638195646687));
#74096=CARTESIAN_POINT('Ctrl Pts',(-0.237452100135973,0.000140355381394047,
-0.0709410108094966));
#74097=CARTESIAN_POINT('Origin',(0.,0.,-2.1406589891905));
#74098=CARTESIAN_POINT('',(-0.237375536783514,0.000176208511683888,-0.2906589891905));
#74099=CARTESIAN_POINT('',(-0.236796239026498,3.83100794477953E-5,-0.270941010809497));
#74100=CARTESIAN_POINT('',(-0.237175,-2.3095687792789E-14,-2.1406589891905));
#74101=CARTESIAN_POINT('Ctrl Pts',(-0.237375536783514,0.000176208511683873,
-0.2906589891905));
#74102=CARTESIAN_POINT('Ctrl Pts',(-0.236818330331351,-0.0668453655976375,
-0.286150400576847));
#74103=CARTESIAN_POINT('Ctrl Pts',(-0.172206359973546,-0.213278616180841,
-0.276362985621525));
#74104=CARTESIAN_POINT('Ctrl Pts',(0.0758114385164903,-0.269634087135906,
-0.261296744324535));
#74105=CARTESIAN_POINT('Ctrl Pts',(0.267440510425046,-0.0832195429967548,
-0.245460265299531));
#74106=CARTESIAN_POINT('Ctrl Pts',(0.215416916394134,0.17901240420799,-0.229623786274526));
#74107=CARTESIAN_POINT('Ctrl Pts',(-0.0328628956583448,0.278154575422294,
-0.213787307249523));
#74108=CARTESIAN_POINT('Ctrl Pts',(-0.211934276390539,0.151628854238979,
-0.200799041554847));
#74109=CARTESIAN_POINT('Ctrl Pts',(-0.236869676045862,0.0364058881413166,
-0.19308960220184));
#74110=CARTESIAN_POINT('Ctrl Pts',(-0.236800424386245,5.02917441071067E-5,
-0.1906589891905));
#74111=CARTESIAN_POINT('Ctrl Pts',(-0.236796239026498,3.83100794478057E-5,
-0.270941010809497));
#74112=CARTESIAN_POINT('Ctrl Pts',(-0.236735559172027,-0.0418134366052485,
-0.26814306899802));
#74113=CARTESIAN_POINT('Ctrl Pts',(-0.206235814196846,-0.16270876290859,
-0.260066300844874));
#74114=CARTESIAN_POINT('Ctrl Pts',(-0.0135402899116431,-0.27976166618424,
-0.246710706350061));
#74115=CARTESIAN_POINT('Ctrl Pts',(0.227285795344374,-0.163679885626449,
-0.230874227325056));
#74116=CARTESIAN_POINT('Ctrl Pts',(0.261041901008646,0.101522741173457,
-0.215037748300052));
#74117=CARTESIAN_POINT('Ctrl Pts',(0.056975763960648,0.274233261483808,
-0.199201269275047));
#74118=CARTESIAN_POINT('Ctrl Pts',(-0.180612775457958,0.202642109780299,
-0.184502356778196));
#74119=CARTESIAN_POINT('Ctrl Pts',(-0.236650908949183,0.0614571125427528,
-0.175082270623013));
#74120=CARTESIAN_POINT('Ctrl Pts',(-0.237215670057668,-0.00021091126858686,
-0.170941010809497));
#74121=CARTESIAN_POINT('Origin',(0.,0.,-2.1406589891905));
#74122=CARTESIAN_POINT('',(-0.23732555028123,-0.000191980036303487,-0.390658989190501));
#74123=CARTESIAN_POINT('',(-0.237354923007457,0.000183314680767349,-0.370941010809497));
#74124=CARTESIAN_POINT('',(-0.237175,-2.3095687792789E-14,-2.1406589891905));
#74125=CARTESIAN_POINT('Ctrl Pts',(-0.23732555028123,-0.000191980036303481,
-0.3906589891905));
#74126=CARTESIAN_POINT('Ctrl Pts',(-0.237441870296821,-0.0134313959082863,
-0.38976885163519));
#74127=CARTESIAN_POINT('Ctrl Pts',(-0.230421693992145,-0.105061794884267,
-0.383599887738212));
#74128=CARTESIAN_POINT('Ctrl Pts',(-0.111125482197992,-0.25710122431668,
-0.372152097499565));
#74129=CARTESIAN_POINT('Ctrl Pts',(0.155146048077143,-0.23319437425588,
-0.356315618474562));
#74130=CARTESIAN_POINT('Ctrl Pts',(0.280071232427623,0.00316502186262762,
-0.340479139449557));
#74131=CARTESIAN_POINT('Ctrl Pts',(0.149836545421379,0.236640912759002,
-0.324642660424553));
#74132=CARTESIAN_POINT('Ctrl Pts',(-0.116907244968831,0.254524279263399,
-0.308806181399548));
#74133=CARTESIAN_POINT('Ctrl Pts',(-0.231523947454547,0.101447974052937,
-0.297478290988198));
#74134=CARTESIAN_POINT('Ctrl Pts',(-0.237470728753447,0.0116260322577658,
-0.291429226918515));
#74135=CARTESIAN_POINT('Ctrl Pts',(-0.237375536783514,0.000176208511683873,
-0.2906589891905));
#74136=CARTESIAN_POINT('Ctrl Pts',(-0.237354923007457,0.000183314680767349,
-0.370941010809497));
#74137=CARTESIAN_POINT('Ctrl Pts',(-0.236789072171188,-0.0661059259336786,
-0.366482693714695));
#74138=CARTESIAN_POINT('Ctrl Pts',(-0.173393869560153,-0.211833111027387,
-0.356745550278225));
#74139=CARTESIAN_POINT('Ctrl Pts',(0.0732530352383368,-0.270340335534277,
-0.341729580500087));
#74140=CARTESIAN_POINT('Ctrl Pts',(0.266639901610645,-0.0857500318774511,
-0.325893101475082));
#74141=CARTESIAN_POINT('Ctrl Pts',(0.217103548889173,0.176963130656145,
-0.310056622450078));
#74142=CARTESIAN_POINT('Ctrl Pts',(-0.0302257286171684,0.27845342881406,
-0.294220143425073));
#74143=CARTESIAN_POINT('Ctrl Pts',(-0.211185581776565,0.153147220674766,
-0.281181606211547));
#74144=CARTESIAN_POINT('Ctrl Pts',(-0.236850042758812,0.0371474988715844,
-0.273421895339688));
#74145=CARTESIAN_POINT('Ctrl Pts',(-0.236796239026498,3.83100794478057E-5,
-0.270941010809497));
#74146=CARTESIAN_POINT('Origin',(0.,0.,-2.1406589891905));
#74147=CARTESIAN_POINT('',(-0.236792325324681,-2.1558736610646E-5,-0.490658989190501));
#74148=CARTESIAN_POINT('',(-0.237346845555136,-0.000185862303693607,-0.470941010809497));
#74149=CARTESIAN_POINT('',(-0.237175,-2.3095687792789E-14,-2.1406589891905));
#74150=CARTESIAN_POINT('Ctrl Pts',(-0.236792325324681,-2.15587366106523E-5,
-0.4906589891905));
#74151=CARTESIAN_POINT('Ctrl Pts',(-0.236823424346363,-0.0381738378163725,
-0.488108476351866));
#74152=CARTESIAN_POINT('Ctrl Pts',(-0.210132507448376,-0.15524928073634,
-0.480279137171563));
#74153=CARTESIAN_POINT('Ctrl Pts',(-0.0265686443687933,-0.278826145720265,
-0.467170971649592));
#74154=CARTESIAN_POINT('Ctrl Pts',(0.219407375961836,-0.174098580622825,
-0.451334492624588));
#74155=CARTESIAN_POINT('Ctrl Pts',(0.265491543531784,0.0892421017223949,
-0.435498013599583));
#74156=CARTESIAN_POINT('Ctrl Pts',(0.0696987171985843,0.271278456967154,
-0.419661534574579));
#74157=CARTESIAN_POINT('Ctrl Pts',(-0.175019066077197,0.209825495554917,
-0.404715193104885));
#74158=CARTESIAN_POINT('Ctrl Pts',(-0.236752052011204,0.065082960481243,
-0.395047677976859));
#74159=CARTESIAN_POINT('Ctrl Pts',(-0.23732555028123,-0.000191980036303481,
-0.3906589891905));
#74160=CARTESIAN_POINT('Ctrl Pts',(-0.237346845555136,-0.000185862303693581,
-0.470941010809497));
#74161=CARTESIAN_POINT('Ctrl Pts',(-0.237454401889236,-0.0126746567440396,
-0.470101144773039));
#74162=CARTESIAN_POINT('Ctrl Pts',(-0.230889358616771,-0.103546234772025,
-0.463982452394912));
#74163=CARTESIAN_POINT('Ctrl Pts',(-0.113556730952469,-0.256036662952951,
-0.452584933675117));
#74164=CARTESIAN_POINT('Ctrl Pts',(0.15292936740834,-0.23465402726664,-0.436748454650113));
#74165=CARTESIAN_POINT('Ctrl Pts',(0.280088633943004,0.000510975941890648,
-0.420911975625108));
#74166=CARTESIAN_POINT('Ctrl Pts',(0.152072176426899,0.235210452621709,
-0.405075496600104));
#74167=CARTESIAN_POINT('Ctrl Pts',(-0.114490165816999,0.255620628817145,
-0.389239017575099));
#74168=CARTESIAN_POINT('Ctrl Pts',(-0.231067303341457,0.102962813414217,
-0.377860855644897));
#74169=CARTESIAN_POINT('Ctrl Pts',(-0.237459062267548,0.0123831949798373,
-0.371761520056363));
#74170=CARTESIAN_POINT('Ctrl Pts',(-0.237354923007457,0.000183314680767349,
-0.370941010809497));
#74171=CARTESIAN_POINT('Origin',(0.,0.,-2.1406589891905));
#74172=CARTESIAN_POINT('',(-0.237247451135996,0.000207679341461782,-0.590658989190501));
#74173=CARTESIAN_POINT('',(-0.236794931055306,-3.36693625221374E-5,-0.570941010809498));
#74174=CARTESIAN_POINT('',(-0.237175,-2.3095687792789E-14,-2.1406589891905));
#74175=CARTESIAN_POINT('Ctrl Pts',(-0.237247451135996,0.000207679341461783,
-0.590658989190501));
#74176=CARTESIAN_POINT('Ctrl Pts',(-0.236675038023536,-0.0624760192039184,
-0.586448101068542));
#74177=CARTESIAN_POINT('Ctrl Pts',(-0.179066675139839,-0.204671240602264,
-0.576958386604914));
#74178=CARTESIAN_POINT('Ctrl Pts',(0.0605694802894751,-0.273461606920063,
-0.562189845799617));
#74179=CARTESIAN_POINT('Ctrl Pts',(0.262352096699239,-0.0980881733918026,
-0.546353366774615));
#74180=CARTESIAN_POINT('Ctrl Pts',(0.225117923184134,0.166648831568735,
-0.530516887749609));
#74181=CARTESIAN_POINT('Ctrl Pts',(-0.0172107170083428,0.279559839071688,
-0.514680408724605));
#74182=CARTESIAN_POINT('Ctrl Pts',(-0.20735700595603,0.160611456954188,
-0.501394442538236));
#74183=CARTESIAN_POINT('Ctrl Pts',(-0.236759058336372,0.0407903817516132,
-0.493387302693534));
#74184=CARTESIAN_POINT('Ctrl Pts',(-0.236792325324681,-2.15587366106523E-5,
-0.4906589891905));
#74185=CARTESIAN_POINT('Ctrl Pts',(-0.236794931055306,-3.366936252212E-5,
-0.570941010809498));
#74186=CARTESIAN_POINT('Ctrl Pts',(-0.236842572399773,-0.0374329187291053,
-0.568440769489714));
#74187=CARTESIAN_POINT('Ctrl Pts',(-0.210894706723823,-0.153731708204917,
-0.560661701828262));
#74188=CARTESIAN_POINT('Ctrl Pts',(-0.0292095552737704,-0.278561852753679,
-0.547603807825144));
#74189=CARTESIAN_POINT('Ctrl Pts',(0.217747787412377,-0.176169818657624,
-0.531767328800138));
#74190=CARTESIAN_POINT('Ctrl Pts',(0.26632525124544,0.0867223412897275,
-0.515930849775135));
#74191=CARTESIAN_POINT('Ctrl Pts',(0.0722661688848724,0.270605810659411,
-0.50009437075013));
#74192=CARTESIAN_POINT('Ctrl Pts',(-0.173847952832261,0.211275626043213,
-0.485097757761584));
#74193=CARTESIAN_POINT('Ctrl Pts',(-0.236778375969605,0.0658214059677648,
-0.475379971114707));
#74194=CARTESIAN_POINT('Ctrl Pts',(-0.237346845555136,-0.000185862303693581,
-0.470941010809497));
#74195=CARTESIAN_POINT('Origin',(0.,0.,-2.1406589891905));
#74196=CARTESIAN_POINT('',(-0.237442878479053,-0.000145678815165409,-0.690658989190501));
#74197=CARTESIAN_POINT('',(-0.23722491884502,0.000210405188862381,-0.670941010809497));
#74198=CARTESIAN_POINT('',(-0.237175,-2.3095687792789E-14,-2.1406589891905));
#74199=CARTESIAN_POINT('Ctrl Pts',(-0.237442878479053,-0.000145678815165355,
-0.690658989190501));
#74200=CARTESIAN_POINT('Ctrl Pts',(-0.237506536812315,-0.00894590921801271,
-0.690066552126885));
#74201=CARTESIAN_POINT('Ctrl Pts',(-0.233075801309679,-0.0960946100168791,
-0.6841952887216));
#74202=CARTESIAN_POINT('Ctrl Pts',(-0.125370287089174,-0.250463976485706,
-0.673045198974649));
#74203=CARTESIAN_POINT('Ctrl Pts',(0.141822954079178,-0.241528801798274,
-0.657208719949644));
#74204=CARTESIAN_POINT('Ctrl Pts',(0.279807899799573,-0.0125479724101313,
-0.64137224092464));
#74205=CARTESIAN_POINT('Ctrl Pts',(0.162872885484516,0.227864730872955,
-0.625535761899635));
#74206=CARTESIAN_POINT('Ctrl Pts',(-0.102448037478282,0.260680478783321,
-0.609699282874631));
#74207=CARTESIAN_POINT('Ctrl Pts',(-0.228702776867451,0.110425870116913,
-0.598073691971586));
#74208=CARTESIAN_POINT('Ctrl Pts',(-0.237392622848602,0.016105113680835,
-0.59172692741021));
#74209=CARTESIAN_POINT('Ctrl Pts',(-0.237247451135996,0.000207679341461783,
-0.590658989190501));
#74210=CARTESIAN_POINT('Ctrl Pts',(-0.23722491884502,0.000210405188862376,
-0.670941010809497));
#74211=CARTESIAN_POINT('Ctrl Pts',(-0.23665762571089,-0.0617400645604461,
-0.666780394206389));
#74212=CARTESIAN_POINT('Ctrl Pts',(-0.180184596641873,-0.203207116348255,
-0.657340951261613));
#74213=CARTESIAN_POINT('Ctrl Pts',(0.057975485860299,-0.274023259903682,
-0.64262268197517));
#74214=CARTESIAN_POINT('Ctrl Pts',(0.261410838370488,-0.100569764399713,
-0.626786202950165));
#74215=CARTESIAN_POINT('Ctrl Pts',(0.22668693762885,0.16450816465285,-0.610949723925161));
#74216=CARTESIAN_POINT('Ctrl Pts',(-0.0145608858552237,0.279710358285275,
-0.595113244900156));
#74217=CARTESIAN_POINT('Ctrl Pts',(-0.206549469757811,0.162125874414636,
-0.581777007194936));
#74218=CARTESIAN_POINT('Ctrl Pts',(-0.236741985955522,0.0415291163163889,
-0.573719595831383));
#74219=CARTESIAN_POINT('Ctrl Pts',(-0.236794931055306,-3.366936252212E-5,
-0.570941010809498));
#74220=CARTESIAN_POINT('Origin',(0.,0.,-2.1406589891905));
#74221=CARTESIAN_POINT('',(-0.236824320187109,-9.1009876261151E-5,-0.790658989190501));
#74222=CARTESIAN_POINT('',(-0.237459971379865,-0.000135626906777819,-0.770941010809498));
#74223=CARTESIAN_POINT('',(-0.237175,-2.3095687792789E-14,-2.1406589891905));
#74224=CARTESIAN_POINT('Ctrl Pts',(-0.236824320187109,-9.10098762611847E-5,
-0.790658989190501));
#74225=CARTESIAN_POINT('Ctrl Pts',(-0.236941182127794,-0.0337787096963821,
-0.788406176843561));
#74226=CARTESIAN_POINT('Ctrl Pts',(-0.214504063690713,-0.146255429941878,
-0.780874538154952));
#74227=CARTESIAN_POINT('Ctrl Pts',(-0.0421650045577871,-0.276897137566454,
-0.768064073124674));
#74228=CARTESIAN_POINT('Ctrl Pts',(0.209297564880806,-0.186130174170711,
-0.752227594099669));
#74229=CARTESIAN_POINT('Ctrl Pts',(0.270078860083927,0.0742113315984893,
-0.736391115074667));
#74230=CARTESIAN_POINT('Ctrl Pts',(0.0848038707134778,0.266942345673866,
-0.720554636049661));
#74231=CARTESIAN_POINT('Ctrl Pts',(-0.167910606883227,0.218362587719398,
-0.705310594088274));
#74232=CARTESIAN_POINT('Ctrl Pts',(-0.236939318271937,0.0694672943377367,
-0.695345378468553));
#74233=CARTESIAN_POINT('Ctrl Pts',(-0.237442878479053,-0.000145678815165355,
-0.690658989190501));
#74234=CARTESIAN_POINT('Ctrl Pts',(-0.237459971379865,-0.000135626906777798,
-0.770941010809498));
#74235=CARTESIAN_POINT('Ctrl Pts',(-0.237515064016247,-0.0081875839623386,
-0.770398845264733));
#74236=CARTESIAN_POINT('Ctrl Pts',(-0.233496912921487,-0.0945822701972211,
-0.764577853378301));
#74237=CARTESIAN_POINT('Ctrl Pts',(-0.127738002114452,-0.249264732252255,
-0.753478035150199));
#74238=CARTESIAN_POINT('Ctrl Pts',(0.139527896638572,-0.242861833124507,
-0.737641556125195));
#74239=CARTESIAN_POINT('Ctrl Pts',(0.279676420005076,-0.015198816471186,
-0.721805077100191));
#74240=CARTESIAN_POINT('Ctrl Pts',(0.165024768460067,0.226311134776178,
-0.705968598075186));
#74241=CARTESIAN_POINT('Ctrl Pts',(-0.0999732721998829,0.261639539776823,
-0.690132119050183));
#74242=CARTESIAN_POINT('Ctrl Pts',(-0.228198205810638,0.111943521562034,
-0.678456256628286));
#74243=CARTESIAN_POINT('Ctrl Pts',(-0.237377384877754,0.0168602494764385,
-0.672059220548058));
#74244=CARTESIAN_POINT('Ctrl Pts',(-0.23722491884502,0.000210405188862376,
-0.670941010809497));
#74245=CARTESIAN_POINT('Origin',(0.,0.,-2.1406589891905));
#74246=CARTESIAN_POINT('',(-0.237114751271997,0.000212755034102921,-0.890658989190501));
#74247=CARTESIAN_POINT('',(-0.236833526846729,-0.000101945576229834,-0.870941010809498));
#74248=CARTESIAN_POINT('',(-0.237175,-2.3095687792789E-14,-2.1406589891905));
#74249=CARTESIAN_POINT('Ctrl Pts',(-0.237114751271997,0.000212755034102929,
-0.890658989190501));
#74250=CARTESIAN_POINT('Ctrl Pts',(-0.236598028529304,-0.0581228578554325,
-0.886745801560236));
#74251=CARTESIAN_POINT('Ctrl Pts',(-0.185518811696717,-0.195961385216037,
-0.877553787588303));
#74252=CARTESIAN_POINT('Ctrl Pts',(0.0451368350116836,-0.276428252041976,
-0.8630829472747));
#74253=CARTESIAN_POINT('Ctrl Pts',(0.256437791245425,-0.112647998752851,
-0.847246468249696));
#74254=CARTESIAN_POINT('Ctrl Pts',(0.23411020610242,0.153760605489627,-0.831409989224693));
#74255=CARTESIAN_POINT('Ctrl Pts',(-0.00150429633730956,0.280085075458125,
-0.815573510199687));
#74256=CARTESIAN_POINT('Ctrl Pts',(-0.20242601141066,0.169566288850719,
-0.801989843521624));
#74257=CARTESIAN_POINT('Ctrl Pts',(-0.236667349337564,0.0451588535863105,
-0.793685003185228));
#74258=CARTESIAN_POINT('Ctrl Pts',(-0.236824320187109,-9.10098762611847E-5,
-0.790658989190501));
#74259=CARTESIAN_POINT('Ctrl Pts',(-0.236833526846729,-0.000101945576229823,
-0.870941010809498));
#74260=CARTESIAN_POINT('Ctrl Pts',(-0.236961801699857,-0.0330346947601913,
-0.868738469981408));
#74261=CARTESIAN_POINT('Ctrl Pts',(-0.21520889725179,-0.144735311414088,
-0.861257102811651));
#74262=CARTESIAN_POINT('Ctrl Pts',(-0.0447869354702739,-0.276485143073116,
-0.848496909300226));
#74263=CARTESIAN_POINT('Ctrl Pts',(0.20752442160637,-0.188105072674614,
-0.832660430275222));
#74264=CARTESIAN_POINT('Ctrl Pts',(0.270769932793133,0.0716487782462665,
-0.816823951250217));
#74265=CARTESIAN_POINT('Ctrl Pts',(0.0873295552116665,0.266126760615149,
-0.800987472225213));
#74266=CARTESIAN_POINT('Ctrl Pts',(-0.166668773296624,0.219791561064743,
-0.785693158744973));
#74267=CARTESIAN_POINT('Ctrl Pts',(-0.236978651359679,0.0702107639543191,
-0.775677671606401));
#74268=CARTESIAN_POINT('Ctrl Pts',(-0.237459971379865,-0.000135626906777798,
-0.770941010809498));
#74269=CARTESIAN_POINT('Origin',(0.,0.,-2.1406589891905));
#74270=CARTESIAN_POINT('',(-0.23752749294738,-7.85812877829553E-5,-0.990658989190501));
#74271=CARTESIAN_POINT('',(-0.237092966851317,0.000211018442878422,-0.970941010809499));
#74272=CARTESIAN_POINT('',(-0.237175,-2.3095687792789E-14,-2.1406589891905));
#74273=CARTESIAN_POINT('Ctrl Pts',(-0.23752749294738,-7.85812877829419E-5,
-0.990658989190501));
#74274=CARTESIAN_POINT('Ctrl Pts',(-0.237546434480431,-0.00445256118670738,
-0.990364252618579));
#74275=CARTESIAN_POINT('Ctrl Pts',(-0.235458487126414,-0.0871474789275883,
-0.984790689704989));
#74276=CARTESIAN_POINT('Ctrl Pts',(-0.139220414716906,-0.24303824499018,
-0.973938300449731));
#74277=CARTESIAN_POINT('Ctrl Pts',(0.128053388226197,-0.249102874663553,
-0.958101821424727));
#74278=CARTESIAN_POINT('Ctrl Pts',(0.278663706570009,-0.0282214642164085,
-0.942265342399722));
#74279=CARTESIAN_POINT('Ctrl Pts',(0.175396486098643,0.218371209334249,
-0.926428863374717));
#74280=CARTESIAN_POINT('Ctrl Pts',(-0.0876663129058996,0.26601603332006,
-0.910592384349715));
#74281=CARTESIAN_POINT('Ctrl Pts',(-0.225593223953284,0.119418790281913,
-0.898669092954974));
#74282=CARTESIAN_POINT('Ctrl Pts',(-0.237295079088385,0.020570933261798,
-0.892024627901903));
#74283=CARTESIAN_POINT('Ctrl Pts',(-0.237114751271997,0.000212755034102929,
-0.890658989190501));
#74284=CARTESIAN_POINT('Ctrl Pts',(-0.237092966851317,0.000211018442878404,
-0.970941010809499));
#74285=CARTESIAN_POINT('Ctrl Pts',(-0.236590878687514,-0.0573886351489161,
-0.967078094698084));
#74286=CARTESIAN_POINT('Ctrl Pts',(-0.186568756555997,-0.19448175581739,
-0.957936352245));
#74287=CARTESIAN_POINT('Ctrl Pts',(0.0425154229059733,-0.276843534770285,
-0.943515783450253));
#74288=CARTESIAN_POINT('Ctrl Pts',(0.255358832545678,-0.115072892419929,
-0.927679304425247));
#74289=CARTESIAN_POINT('Ctrl Pts',(0.2355566898837,0.151535308690796,-0.911842825400244));
#74290=CARTESIAN_POINT('Ctrl Pts',(0.00114980584647748,0.280086739913719,
-0.896006346375237));
#74291=CARTESIAN_POINT('Ctrl Pts',(-0.201557562819165,0.171074866061252,
-0.882372408178324));
#74292=CARTESIAN_POINT('Ctrl Pts',(-0.236654365549286,0.045895176449807,
-0.874017296323077));
#74293=CARTESIAN_POINT('Ctrl Pts',(-0.236833526846729,-0.000101945576229823,
-0.870941010809498));
#74294=CARTESIAN_POINT('Origin',(0.,0.,-2.1406589891905));
#74295=CARTESIAN_POINT('',(-0.236893725685054,-0.000150389252750359,-1.0906589891905));
#74296=CARTESIAN_POINT('',(-0.237537155315066,-6.57425195367267E-5,-1.0709410108095));
#74297=CARTESIAN_POINT('',(-0.237175,-2.3095687792789E-14,-2.1406589891905));
#74298=CARTESIAN_POINT('Ctrl Pts',(-0.236893725685054,-0.000150389252750339,
-1.0906589891905));
#74299=CARTESIAN_POINT('Ctrl Pts',(-0.237064310361161,-0.0293649258802016,
-1.08870387733525));
#74300=CARTESIAN_POINT('Ctrl Pts',(-0.218540890155226,-0.137250396400922,
-1.08146993913834));
#74301=CARTESIAN_POINT('Ctrl Pts',(-0.0576286254410279,-0.2740964318112,
-1.06895717459976));
#74302=CARTESIAN_POINT('Ctrl Pts',(0.198528865854686,-0.197575812852451,
-1.05312069557475));
#74303=CARTESIAN_POINT('Ctrl Pts',(0.273815943606632,0.0589469373985079,
-1.03728421654975));
#74304=CARTESIAN_POINT('Ctrl Pts',(0.0996420538473957,0.261765875367525,
-1.02144773752474));
#74305=CARTESIAN_POINT('Ctrl Pts',(-0.160379968251884,0.226765849567329,
-1.00590599507166));
#74306=CARTESIAN_POINT('Ctrl Pts',(-0.237207185560743,0.0738868188155779,
-0.995643078960248));
#74307=CARTESIAN_POINT('Ctrl Pts',(-0.23752749294738,-7.85812877829419E-5,
-0.990658989190501));
#74308=CARTESIAN_POINT('Ctrl Pts',(-0.237537155315066,-6.57425195367272E-5,
-1.0709410108095));
#74309=CARTESIAN_POINT('Ctrl Pts',(-0.23755056754939,-0.00369328339404799,
-1.07069654575643));
#74310=CARTESIAN_POINT('Ctrl Pts',(-0.235834755836577,-0.0856387249952216,
-1.06517325436169));
#74311=CARTESIAN_POINT('Ctrl Pts',(-0.141517142307931,-0.241708093290185,
-1.05437113662528));
#74312=CARTESIAN_POINT('Ctrl Pts',(0.125687179216381,-0.250305087662256,
-1.03853465760028));
#74313=CARTESIAN_POINT('Ctrl Pts',(0.278383759087368,-0.0308607615811162,
-1.02269817857527));
#74314=CARTESIAN_POINT('Ctrl Pts',(0.177457847270645,0.216699368644785,
-1.00686169955027));
#74315=CARTESIAN_POINT('Ctrl Pts',(-0.0851416533425872,0.26683478557915,
-0.991025220525264));
#74316=CARTESIAN_POINT('Ctrl Pts',(-0.225038857388908,0.120938550544616,
-0.979051657611676));
#74317=CARTESIAN_POINT('Ctrl Pts',(-0.23727700185159,0.0213235501229567,
-0.972356921039753));
#74318=CARTESIAN_POINT('Ctrl Pts',(-0.237092966851317,0.000211018442878404,
-0.970941010809499));
#74319=CARTESIAN_POINT('Origin',(0.,0.,-2.1406589891905));
#74320=CARTESIAN_POINT('',(-0.236992223716617,0.000192184054864515,-1.1906589891905));
#74321=CARTESIAN_POINT('',(-0.236908741130895,-0.000158913860137805,-1.1709410108095));
#74322=CARTESIAN_POINT('',(-0.237175,-2.3095687792789E-14,-2.1406589891905));
#74323=CARTESIAN_POINT('Ctrl Pts',(-0.236992223716617,0.000192184054864528,
-1.1906589891905));
#74324=CARTESIAN_POINT('Ctrl Pts',(-0.236577798658883,-0.0537762028892547,
-1.18704350205193));
#74325=CARTESIAN_POINT('Ctrl Pts',(-0.191572606767969,-0.18716689616996,
-1.17814918857169));
#74326=CARTESIAN_POINT('Ctrl Pts',(0.0295620948351317,-0.278524675658752,
-1.16397604874978));
#74327=CARTESIAN_POINT('Ctrl Pts',(0.249716196091533,-0.126853197876244,
-1.14813956972478));
#74328=CARTESIAN_POINT('Ctrl Pts',(0.242365488607872,0.140388326914034,
-1.13230309069977));
#74329=CARTESIAN_POINT('Ctrl Pts',(0.0142068599963639,0.27972857832352,
-1.11646661167477));
#74330=CARTESIAN_POINT('Ctrl Pts',(-0.197129456028173,0.178481248161311,
-1.10258524450501));
#74331=CARTESIAN_POINT('Ctrl Pts',(-0.236603729612646,0.0495146866057853,
-1.09398270367692));
#74332=CARTESIAN_POINT('Ctrl Pts',(-0.236893725685054,-0.000150389252750339,
-1.0906589891905));
#74333=CARTESIAN_POINT('Ctrl Pts',(-0.236908741130895,-0.000158913860137808,
-1.1709410108095));
#74334=CARTESIAN_POINT('Ctrl Pts',(-0.237085066804682,-0.0286177232752274,
-1.1690361704731));
#74335=CARTESIAN_POINT('Ctrl Pts',(-0.219190380754614,-0.135729270178569,
-1.16185250379504));
#74336=CARTESIAN_POINT('Ctrl Pts',(-0.0602233222835258,-0.273538032789071,
-1.14939001077531));
#74337=CARTESIAN_POINT('Ctrl Pts',(0.196647749876134,-0.199448154660888,
-1.1335535317503));
#74338=CARTESIAN_POINT('Ctrl Pts',(0.274362205745136,0.0563496582744192,
-1.1177170527253));
#74339=CARTESIAN_POINT('Ctrl Pts',(0.102118020082256,0.260809919104815,
-1.1018805737003));
#74340=CARTESIAN_POINT('Ctrl Pts',(-0.159066073200517,0.228170150730898,
-1.08628855972836));
#74341=CARTESIAN_POINT('Ctrl Pts',(-0.237260952101461,0.0746375785566909,
-1.0759753720981));
#74342=CARTESIAN_POINT('Ctrl Pts',(-0.237537155315066,-6.57425195367272E-5,
-1.0709410108095));
#74343=CARTESIAN_POINT('Origin',(0.,0.,-2.1406589891905));
#74344=CARTESIAN_POINT('',(-0.237559752509291,8.12847334188233E-7,-1.2906589891905));
#74345=CARTESIAN_POINT('',(-0.23697343290048,0.000186386972896829,-1.2709410108095));
#74346=CARTESIAN_POINT('',(-0.237175,-2.3095687792789E-14,-2.1406589891905));
#74347=CARTESIAN_POINT('Ctrl Pts',(-0.237559751139412,8.1284444012185E-7,
-1.2906589891905));
#74348=CARTESIAN_POINT('Ctrl Pts',(-0.237555752466613,-0.0782661021016744,
-1.2853831267686));
#74349=CARTESIAN_POINT('Ctrl Pts',(-0.152582383736732,-0.234851345594784,
-1.27482843800504));
#74350=CARTESIAN_POINT('Ctrl Pts',(0.11388069855569,-0.255892748819348,
-1.25899492289981));
#74351=CARTESIAN_POINT('Ctrl Pts',(0.27664225441934,-0.0438061122634664,
-1.2431584438748));
#74352=CARTESIAN_POINT('Ctrl Pts',(0.187367922478493,0.208190235188752,
-1.2273219648498));
#74353=CARTESIAN_POINT('Ctrl Pts',(-0.0726086067354031,0.270514144971751,
-1.2114854858248));
#74354=CARTESIAN_POINT('Ctrl Pts',(-0.222184057315321,0.128422060611755,
-1.19926449393836));
#74355=CARTESIAN_POINT('Ctrl Pts',(-0.237182883901222,0.0250208531363774,
-1.1923223283936));
#74356=CARTESIAN_POINT('Ctrl Pts',(-0.236992223716617,0.000192184054864528,
-1.1906589891905));
#74357=CARTESIAN_POINT('Ctrl Pts',(-0.23697343290048,0.000186386972896805,
-1.2709410108095));
#74358=CARTESIAN_POINT('Ctrl Pts',(-0.236579283171597,-0.0530422438593269,
-1.26737579518978));
#74359=CARTESIAN_POINT('Ctrl Pts',(-0.192556305014578,-0.185674636157468,
-1.25853175322839));
#74360=CARTESIAN_POINT('Ctrl Pts',(0.0269215174987288,-0.278792280783643,
-1.24440888492533));
#74361=CARTESIAN_POINT('Ctrl Pts',(0.248502933681857,-0.129213760414636,
-1.22857240590033));
#74362=CARTESIAN_POINT('Ctrl Pts',(0.243684888061905,0.138085405670681,
-1.21273592687532));
#74363=CARTESIAN_POINT('Ctrl Pts',(0.0168568778538109,0.279581382781475,
-1.19689944785032));
#74364=CARTESIAN_POINT('Ctrl Pts',(-0.196198136324593,0.179981788309436,
-1.18296780916171));
#74365=CARTESIAN_POINT('Ctrl Pts',(-0.236596420804428,0.0502493134640227,
-1.17431499681477));
#74366=CARTESIAN_POINT('Ctrl Pts',(-0.236908741130895,-0.000158913860137808,
-1.1709410108095));
#74367=CARTESIAN_POINT('Origin',(0.,0.,-2.1406589891905));
#74368=CARTESIAN_POINT('',(-0.236994481351619,-0.000192825895592933,-1.3906589891905));
#74369=CARTESIAN_POINT('',(-0.237558599806732,1.45855281510868E-5,-1.3709410108095));
#74370=CARTESIAN_POINT('',(-0.237175,-2.3095687792789E-14,-2.1406589891905));
#74371=CARTESIAN_POINT('Ctrl Pts',(-0.236994481351619,-0.000192825895592965,
-1.3906589891905));
#74372=CARTESIAN_POINT('Ctrl Pts',(-0.237185225043465,-0.0249324145508677,
-1.38900157782695));
#74373=CARTESIAN_POINT('Ctrl Pts',(-0.222254938630742,-0.128242721718558,
-1.38206534012173));
#74374=CARTESIAN_POINT('Ctrl Pts',(-0.0729108261228343,-0.270432845334947,
-1.36985027607484));
#74375=CARTESIAN_POINT('Ctrl Pts',(0.187135179739969,-0.208399464743887,
-1.35401379704983));
#74376=CARTESIAN_POINT('Ctrl Pts',(0.276691029410919,0.0434969728300605,
-1.33817731802483));
#74377=CARTESIAN_POINT('Ctrl Pts',(0.114166554651702,0.255765342063417,
-1.32234083899983));
#74378=CARTESIAN_POINT('Ctrl Pts',(-0.152369756692705,0.235017807085461,
-1.30650435997482));
#74379=CARTESIAN_POINT('Ctrl Pts',(-0.237539870154193,0.0783996340976714,
-1.29594374337171));
#74380=CARTESIAN_POINT('Ctrl Pts',(-0.237559753385822,4.47823110714604E-5,
-1.29066195311027));
#74381=CARTESIAN_POINT('Ctrl Pts',(-0.237559751139412,8.1284444012185E-7,
-1.2906589891905));
#74382=CARTESIAN_POINT('Ctrl Pts',(-0.237558599806732,1.45855281510935E-5,
-1.3709410108095));
#74383=CARTESIAN_POINT('Ctrl Pts',(-0.237489298765113,-0.0775075558748563,
-1.36571541990645));
#74384=CARTESIAN_POINT('Ctrl Pts',(-0.153955582115517,-0.233469766690094,
-1.35521100266174));
#74385=CARTESIAN_POINT('Ctrl Pts',(0.11145078701977,-0.256960358813676,
-1.33942775907536));
#74386=CARTESIAN_POINT('Ctrl Pts',(0.276214720548922,-0.0464255541815164,
-1.32359128005036));
#74387=CARTESIAN_POINT('Ctrl Pts',(0.189332272492804,0.206405413014511,
-1.30775480102535));
#74388=CARTESIAN_POINT('Ctrl Pts',(-0.0700420007471637,0.271190010989185,
-1.29191832200035));
#74389=CARTESIAN_POINT('Ctrl Pts',(-0.221577961557814,0.129943018511057,
-1.27964705859506));
#74390=CARTESIAN_POINT('Ctrl Pts',(-0.23716287984381,0.025770576609058,
-1.27265462153145));
#74391=CARTESIAN_POINT('Ctrl Pts',(-0.23697343290048,0.000186386972896805,
-1.2709410108095));
#74392=CARTESIAN_POINT('Origin',(0.,0.,-2.1406589891905));
#74393=CARTESIAN_POINT('',(-0.236892012300018,0.000149351404289912,-1.4906589891905));
#74394=CARTESIAN_POINT('',(-0.237013962191253,-0.000197906546256954,-1.4709410108095));
#74395=CARTESIAN_POINT('',(-0.237175,-2.3095687792789E-14,-2.1406589891905));
#74396=CARTESIAN_POINT('Ctrl Pts',(-0.236892012300018,0.000149351404289903,
-1.4906589891905));
#74397=CARTESIAN_POINT('Ctrl Pts',(-0.236604661475949,-0.0494280473622855,
-1.48734120254363));
#74398=CARTESIAN_POINT('Ctrl Pts',(-0.197238562986412,-0.178304207004023,
-1.47874458955508));
#74399=CARTESIAN_POINT('Ctrl Pts',(0.0138942904708965,-0.279744278037816,
-1.46486915022487));
#74400=CARTESIAN_POINT('Ctrl Pts',(0.242208471436148,-0.140659051490779,
-1.44903267119986));
#74401=CARTESIAN_POINT('Ctrl Pts',(0.249857782313367,0.12657409300159,-1.43319619217486));
#74402=CARTESIAN_POINT('Ctrl Pts',(0.0298732918310454,0.278491469954,-1.41735971314985));
#74403=CARTESIAN_POINT('Ctrl Pts',(-0.191455883315294,0.187342730509716,
-1.4031806454884));
#74404=CARTESIAN_POINT('Ctrl Pts',(-0.23657770970529,0.0538627446639044,
-1.39428040416862));
#74405=CARTESIAN_POINT('Ctrl Pts',(-0.236994481351619,-0.000192825895592965,
-1.3906589891905));
#74406=CARTESIAN_POINT('Ctrl Pts',(-0.237013962191253,-0.000197906546256975,
-1.4709410108095));
#74407=CARTESIAN_POINT('Ctrl Pts',(-0.237204917491822,-0.0241821198511639,
-1.4693338709648));
#74408=CARTESIAN_POINT('Ctrl Pts',(-0.222851094449599,-0.126721896491833,
-1.46244790477843));
#74409=CARTESIAN_POINT('Ctrl Pts',(-0.0754701205516332,-0.269729799675546,
-1.45028311225039));
#74410=CARTESIAN_POINT('Ctrl Pts',(0.185152012983061,-0.210163355552944,
-1.43444663322539));
#74411=CARTESIAN_POINT('Ctrl Pts',(0.277090761295361,0.0408731444070958,
-1.41861015420038));
#74412=CARTESIAN_POINT('Ctrl Pts',(0.116585008054319,0.254672024034776,
-1.40277367517538));
#74413=CARTESIAN_POINT('Ctrl Pts',(-0.150135922153628,0.236451070642649,
-1.38693719615037));
#74414=CARTESIAN_POINT('Ctrl Pts',(-0.237198772362554,0.0799053226037852,
-1.37632630802841));
#74415=CARTESIAN_POINT('Ctrl Pts',(-0.23755930580753,0.000804338357484877,
-1.37099424624812));
#74416=CARTESIAN_POINT('Ctrl Pts',(-0.237558599806732,1.45855281510935E-5,
-1.3709410108095));
#74417=CARTESIAN_POINT('Origin',(0.,0.,-2.1406589891905));
#74418=CARTESIAN_POINT('',(-0.237526251942735,8.00723330132329E-5,-1.5906589891905));
#74419=CARTESIAN_POINT('',(-0.236877981323345,0.000140284900710816,-1.5709410108095));
#74420=CARTESIAN_POINT('',(-0.237175,-2.3095687792789E-14,-2.1406589891905));
#74421=CARTESIAN_POINT('Ctrl Pts',(-0.237526251942735,8.0072333013226E-5,
-1.5906589891905));
#74422=CARTESIAN_POINT('Ctrl Pts',(-0.237201011701744,-0.0737983853525183,
-1.5856808272603));
#74423=CARTESIAN_POINT('Ctrl Pts',(-0.160534088655561,-0.22659996424131,
-1.57542383898843));
#74424=CARTESIAN_POINT('Ctrl Pts',(0.0993495019835277,-0.261877049183029,
-1.55988802437489));
#74425=CARTESIAN_POINT('Ctrl Pts',(0.273749907070638,-0.059252854615386,
-1.54405154534989));
#74426=CARTESIAN_POINT('Ctrl Pts',(0.198749507440483,0.197353859059745,
-1.52821506632488));
#74427=CARTESIAN_POINT('Ctrl Pts',(-0.057322322005953,0.27416065327936,
-1.51237858729988));
#74428=CARTESIAN_POINT('Ctrl Pts',(-0.21846369760357,0.137429757328886,
-1.49985989492175));
#74429=CARTESIAN_POINT('Ctrl Pts',(-0.237061856365447,0.0294529978690901,
-1.49262002888529));
#74430=CARTESIAN_POINT('Ctrl Pts',(-0.236892012300018,0.000149351404289903,
-1.4906589891905));
#74431=CARTESIAN_POINT('Ctrl Pts',(-0.236877981323345,0.000140284900710819,
-1.5709410108095));
#74432=CARTESIAN_POINT('Ctrl Pts',(-0.236613139832454,-0.0486931615303172,
-1.56767349568147));
#74433=CARTESIAN_POINT('Ctrl Pts',(-0.198157845242651,-0.176801951054827,
-1.55912715421178));
#74434=CARTESIAN_POINT('Ctrl Pts',(0.011242860680614,-0.279863363121343,
-1.54530198640042));
#74435=CARTESIAN_POINT('Ctrl Pts',(0.240864724779504,-0.142947851629034,
-1.52946550737541));
#74436=CARTESIAN_POINT('Ctrl Pts',(0.251045943848778,0.124200797119059,
-1.51362902835041));
#74437=CARTESIAN_POINT('Ctrl Pts',(0.0325108828631745,0.278195877800473,
-1.4977925493254));
#74438=CARTESIAN_POINT('Ctrl Pts',(-0.190459795941901,0.188832794874465,
-1.4835632101451));
#74439=CARTESIAN_POINT('Ctrl Pts',(-0.236577703952162,0.0545966481543488,
-1.47461269730646));
#74440=CARTESIAN_POINT('Ctrl Pts',(-0.237013962191253,-0.000197906546256975,
-1.4709410108095));
#74441=CARTESIAN_POINT('Origin',(0.,0.,-2.1406589891905));
#74442=CARTESIAN_POINT('',(-0.237117339234101,-0.000212911088445047,-1.6906589891905));
#74443=CARTESIAN_POINT('',(-0.237514903826011,9.25041757272732E-5,-1.6709410108095));
#74444=CARTESIAN_POINT('',(-0.237175,-2.3095687792789E-14,-2.1406589891905));
#74445=CARTESIAN_POINT('Ctrl Pts',(-0.237117339234101,-0.000212911088445088,
-1.6906589891905));
#74446=CARTESIAN_POINT('Ctrl Pts',(-0.237297182177879,-0.0204821580555165,
-1.68929927831864));
#74447=CARTESIAN_POINT('Ctrl Pts',(-0.225658028636196,-0.119239611010002,
-1.68266074110512));
#74448=CARTESIAN_POINT('Ctrl Pts',(-0.087963495735764,-0.265917905478881,
-1.67074337754992));
#74449=CARTESIAN_POINT('Ctrl Pts',(0.175152374331677,-0.218567059118628,
-1.65490689852492));
#74450=CARTESIAN_POINT('Ctrl Pts',(0.27869506676358,0.0279100774344748,
-1.63907041949991));
#74451=CARTESIAN_POINT('Ctrl Pts',(0.128331648507507,0.248959635135041,
-1.62323394047491));
#74452=CARTESIAN_POINT('Ctrl Pts',(-0.138948763790046,0.243193654600889,
-1.6073974614499));
#74453=CARTESIAN_POINT('Ctrl Pts',(-0.235413626753898,0.0873254264909276,
-1.5965391443551));
#74454=CARTESIAN_POINT('Ctrl Pts',(-0.237545895370774,0.00454208528307148,
-1.59095965360197));
#74455=CARTESIAN_POINT('Ctrl Pts',(-0.237526251942735,8.0072333013226E-5,
-1.5906589891905));
#74456=CARTESIAN_POINT('Ctrl Pts',(-0.237514903826011,9.25041757272602E-5,
-1.6709410108095));
#74457=CARTESIAN_POINT('Ctrl Pts',(-0.23715004766578,-0.0730491814008578,
-1.66601312039815));
#74458=CARTESIAN_POINT('Ctrl Pts',(-0.161834267745582,-0.225190701072496,
-1.65580640364513));
#74459=CARTESIAN_POINT('Ctrl Pts',(0.0968635373620719,-0.262806695604708,
-1.64032086055044));
#74460=CARTESIAN_POINT('Ctrl Pts',(0.273176132803676,-0.0618441946515969,
-1.62448438152544));
#74461=CARTESIAN_POINT('Ctrl Pts',(0.200610662303521,0.195461674084374,
-1.60864790250043));
#74462=CARTESIAN_POINT('Ctrl Pts',(-0.054721849483307,0.274691505419439,
-1.59281142347543));
#74463=CARTESIAN_POINT('Ctrl Pts',(-0.21780389038128,0.138950785472986,
-1.58024245957845));
#74464=CARTESIAN_POINT('Ctrl Pts',(-0.237041003877058,0.0301995974238838,
-1.57295232202314));
#74465=CARTESIAN_POINT('Ctrl Pts',(-0.236877981323345,0.000140284900710819,
-1.5709410108095));
#74466=CARTESIAN_POINT('Origin',(0.,0.,-2.1406589891905));
#74467=CARTESIAN_POINT('',(-0.2368232568105,8.99543112184168E-5,-1.7906589891905));
#74468=CARTESIAN_POINT('',(-0.237139424499073,-0.000213821819175564,-1.7709410108095));
#74469=CARTESIAN_POINT('',(-0.237175,-2.3095687792789E-14,-2.1406589891905));
#74470=CARTESIAN_POINT('Ctrl Pts',(-0.2368232568105,8.99543112184049E-5,
-1.7906589891905));
#74471=CARTESIAN_POINT('Ctrl Pts',(-0.23666890749081,-0.0450718694273936,
-1.78763890303532));
#74472=CARTESIAN_POINT('Ctrl Pts',(-0.202527805976921,-0.169388758838487,
-1.77933999053847));
#74473=CARTESIAN_POINT('Ctrl Pts',(-0.0018172011087593,-0.280082930068666,
-1.76576225169995));
#74474=CARTESIAN_POINT('Ctrl Pts',(0.23393822438801,-0.154022249166496,
-1.74992577267494));
#74475=CARTESIAN_POINT('Ctrl Pts',(0.256563515396163,0.112361471630493,
-1.73408929364994));
#74476=CARTESIAN_POINT('Ctrl Pts',(0.0454456721551229,0.27637760331013,
-1.71825281462493));
#74477=CARTESIAN_POINT('Ctrl Pts',(-0.185394253897758,0.196135715711487,
-1.70377604647179));
#74478=CARTESIAN_POINT('Ctrl Pts',(-0.23659897516297,0.0582094498664757,
-1.69457810466031));
#74479=CARTESIAN_POINT('Ctrl Pts',(-0.237117339234101,-0.000212911088445088,
-1.6906589891905));
#74480=CARTESIAN_POINT('Ctrl Pts',(-0.237139424499073,-0.00021382181917559,
-1.7709410108095));
#74481=CARTESIAN_POINT('Ctrl Pts',(-0.237314764965966,-0.0197290375198751,
-1.76963157145649));
#74482=CARTESIAN_POINT('Ctrl Pts',(-0.226202839931557,-0.117720212646404,
-1.76304330576182));
#74483=CARTESIAN_POINT('Ctrl Pts',(-0.0904793175238351,-0.265072392539203,
-1.75117621372547));
#74484=CARTESIAN_POINT('Ctrl Pts',(0.173073393005469,-0.22021696378749,
-1.73533973470047));
#74485=CARTESIAN_POINT('Ctrl Pts',(0.278947013657325,0.025267969059772,
-1.71950325567547));
#74486=CARTESIAN_POINT('Ctrl Pts',(0.130684973650179,0.247732392338888,
-1.70366677665046));
#74487=CARTESIAN_POINT('Ctrl Pts',(-0.136638058709272,0.244499378342932,
-1.68783029762546));
#74488=CARTESIAN_POINT('Ctrl Pts',(-0.235028993377773,0.0888348674575675,
-1.6769217090118));
#74489=CARTESIAN_POINT('Ctrl Pts',(-0.2375408867772,0.00530123313075793,
-1.67129194673982));
#74490=CARTESIAN_POINT('Ctrl Pts',(-0.237514903826011,9.25041757272602E-5,
-1.6709410108095));
#74491=CARTESIAN_POINT('Origin',(0.,0.,-2.1406589891905));
#74492=CARTESIAN_POINT('',(-0.2374378448428,0.000162859811871453,-1.8906589891905));
#74493=CARTESIAN_POINT('',(-0.236814675525433,8.00967394152252E-5,-1.8709410108095));
#74494=CARTESIAN_POINT('',(-0.237175,-2.3095687792789E-14,-2.1406589891905));
#74495=CARTESIAN_POINT('Ctrl Pts',(-0.2374378448428,0.00016285981187146,
-1.8906589891905));
#74496=CARTESIAN_POINT('Ctrl Pts',(-0.236931225259905,-0.0693600600496425,
-1.88597852775199));
#74497=CARTESIAN_POINT('Ctrl Pts',(-0.168060902149697,-0.218219163221255,
-1.87601923997182));
#74498=CARTESIAN_POINT('Ctrl Pts',(0.0845081317806936,-0.26702286775457,
-1.86078112584997));
#74499=CARTESIAN_POINT('Ctrl Pts',(0.269994415115787,-0.0745204288506152,
-1.84494464682497));
#74500=CARTESIAN_POINT('Ctrl Pts',(0.209506119993022,0.185900050867469,
-1.82910816779996));
#74501=CARTESIAN_POINT('Ctrl Pts',(-0.0418559526817564,0.27694205992973,
-1.81327168877496));
#74502=CARTESIAN_POINT('Ctrl Pts',(-0.214420236326383,0.146435126422962,
-1.80045529590514));
#74503=CARTESIAN_POINT('Ctrl Pts',(-0.236938695573908,0.033866747730932,
-1.79291772937699));
#74504=CARTESIAN_POINT('Ctrl Pts',(-0.2368232568105,8.99543112184049E-5,
-1.7906589891905));
#74505=CARTESIAN_POINT('Ctrl Pts',(-0.236814675525433,8.00967394152356E-5,
-1.8709410108095));
#74506=CARTESIAN_POINT('Ctrl Pts',(-0.236682471177008,-0.0443344101141993,
-1.86797119617317));
#74507=CARTESIAN_POINT('Ctrl Pts',(-0.203385542392388,-0.167881339256242,
-1.85972255519517));
#74508=CARTESIAN_POINT('Ctrl Pts',(-0.00447048967563682,-0.280051476296464,
-1.8461950878755));
#74509=CARTESIAN_POINT('Ctrl Pts',(0.232467885064925,-0.156232942395582,
-1.8303586088505));
#74510=CARTESIAN_POINT('Ctrl Pts',(0.257616875906963,0.109925723244754,
-1.81452212982549));
#74511=CARTESIAN_POINT('Ctrl Pts',(0.0480624401227571,0.27593430904298,
-1.79868565080049));
#74512=CARTESIAN_POINT('Ctrl Pts',(-0.18433154866488,0.197612718219552,
-1.78415861112849));
#74513=CARTESIAN_POINT('Ctrl Pts',(-0.236607903763674,0.0589438956462287,
-1.77491039779816));
#74514=CARTESIAN_POINT('Ctrl Pts',(-0.237139424499073,-0.00021382181917559,
-1.7709410108095));
#74515=CARTESIAN_POINT('Origin',(3.51939854619125E-17,0.,-0.0249999999999999));
#74516=CARTESIAN_POINT('Ctrl Pts',(0.131476569578105,0.197850242677352,
-0.0250000000000002));
#74517=CARTESIAN_POINT('Ctrl Pts',(0.126716365602224,0.201929436190152,
-0.0250000000000002));
#74518=CARTESIAN_POINT('Ctrl Pts',(0.121794351938759,0.20579944606451,-0.0250000000000006));
#74519=CARTESIAN_POINT('Ctrl Pts',(0.116719086571287,0.20944676365964,-0.0250000000000006));
#74520=CARTESIAN_POINT('Ctrl Pts',(0.106659704771955,0.216675895059939,
-0.0250000000000007));
#74521=CARTESIAN_POINT('Ctrl Pts',(0.0959995500509429,0.223031524528497,
-0.0250000000000006));
#74522=CARTESIAN_POINT('Ctrl Pts',(0.0848629171244075,0.228527486118004,
-0.0250000000000008));
#74523=CARTESIAN_POINT('Ctrl Pts',(0.0793089010339903,0.231268409636073,
-0.025000000000001));
#74524=CARTESIAN_POINT('Ctrl Pts',(0.0736338496400286,0.233795650870042,
-0.0250000000000003));
#74525=CARTESIAN_POINT('Ctrl Pts',(0.0678738710164064,0.236101576769272,
-0.0250000000000002));
#74526=CARTESIAN_POINT('Ctrl Pts',(0.0569403363432262,0.240478662592059,
-0.0250000000000001));
#74527=CARTESIAN_POINT('Ctrl Pts',(0.0456859446130353,0.244067694746422,
-0.0250000000000007));
#74528=CARTESIAN_POINT('Ctrl Pts',(0.0342108064996598,0.246877609869612,
-0.0250000000000009));
#74529=CARTESIAN_POINT('Ctrl Pts',(0.0287705040427049,0.248209775809358,
-0.025000000000001));
#74530=CARTESIAN_POINT('Ctrl Pts',(0.0232804045968881,0.249366613402048,
-0.0250000000000005));
#74531=CARTESIAN_POINT('Ctrl Pts',(0.0177504039195654,0.250347887861532,
-0.0250000000000006));
#74532=CARTESIAN_POINT('Ctrl Pts',(0.0130278961939813,0.251185876224686,
-0.0250000000000008));
#74533=CARTESIAN_POINT('Ctrl Pts',(0.00828050256328347,0.251894890254572,
-0.0250000000000001));
#74534=CARTESIAN_POINT('Ctrl Pts',(0.0035240847247141,0.25247435018727,
-0.0250000000000001));
#74535=CARTESIAN_POINT('Ctrl Pts',(-0.0123782977924341,0.254411689129278,
-0.0250000000000002));
#74536=CARTESIAN_POINT('Ctrl Pts',(-0.0284103017332684,0.254910094217844,
-0.0250000000000004));
#74537=CARTESIAN_POINT('Ctrl Pts',(-0.0443431569787997,0.253981160003125,
-0.0250000000000001));
#74538=CARTESIAN_POINT('Ctrl Pts',(-0.0551143822635383,0.253353164609503,
-0.025));
#74539=CARTESIAN_POINT('Ctrl Pts',(-0.0658410506795728,0.252071912508136,
-0.0250000000000004));
#74540=CARTESIAN_POINT('Ctrl Pts',(-0.0764558373066276,0.25012806300835,
-0.0250000000000005));
#74541=CARTESIAN_POINT('Ctrl Pts',(-0.0819514088173798,0.249121677830057,
-0.0250000000000005));
#74542=CARTESIAN_POINT('Ctrl Pts',(-0.0874204046766468,0.24793629687224,
-0.0250000000000001));
#74543=CARTESIAN_POINT('Ctrl Pts',(-0.0928277779543753,0.246576938729842,
-0.0250000000000002));
#74544=CARTESIAN_POINT('Ctrl Pts',(-0.103820657960877,0.243813441523762,
-0.0250000000000004));
#74545=CARTESIAN_POINT('Ctrl Pts',(-0.114579390862407,0.240328871965648,
-0.0250000000000003));
#74546=CARTESIAN_POINT('Ctrl Pts',(-0.125027804890083,0.236123432466162,
-0.0250000000000002));
#74547=CARTESIAN_POINT('Ctrl Pts',(-0.135775670547118,0.231797465037082,
-0.0250000000000002));
#74548=CARTESIAN_POINT('Ctrl Pts',(-0.146195566282993,0.226708934356136,
-0.0250000000000006));
#74549=CARTESIAN_POINT('Ctrl Pts',(-0.156252054460305,0.220927740860517,
-0.0250000000000006));
#74550=CARTESIAN_POINT('Ctrl Pts',(-0.162623320317708,0.21726507849924,
-0.0250000000000006));
#74551=CARTESIAN_POINT('Ctrl Pts',(-0.168848671260019,0.213324078716014,
-0.0250000000000001));
#74552=CARTESIAN_POINT('Ctrl Pts',(-0.174918101511351,0.209119677449694,
-0.025));
#74553=CARTESIAN_POINT('Ctrl Pts',(-0.178478882090543,0.206653062008656,
-0.025));
#74554=CARTESIAN_POINT('Ctrl Pts',(-0.181984449689504,0.204096577325674,
-0.0250000000000006));
#74555=CARTESIAN_POINT('Ctrl Pts',(-0.185423585478161,0.201460877808261,
-0.0250000000000006));
#74556=CARTESIAN_POINT('Ctrl Pts',(-0.198547347273593,0.191403033408821,
-0.0250000000000004));
#74557=CARTESIAN_POINT('Ctrl Pts',(-0.210743690822958,0.180169353014819,
-0.0250000000000002));
#74558=CARTESIAN_POINT('Ctrl Pts',(-0.221915859342723,0.167954146424944,
-0.0249999999999998));
#74559=CARTESIAN_POINT('Ctrl Pts',(-0.232159167234076,0.156754519258988,
-0.0249999999999995));
#74560=CARTESIAN_POINT('Ctrl Pts',(-0.241542045610028,0.144728551000905,
-0.0250000000000004));
#74561=CARTESIAN_POINT('Ctrl Pts',(-0.249971624146837,0.131994872381627,
-0.0250000000000007));
#74562=CARTESIAN_POINT('Ctrl Pts',(-0.252429636980731,0.128281810651176,
-0.0250000000000007));
#74563=CARTESIAN_POINT('Ctrl Pts',(-0.254804760717037,0.124510660490947,
-0.025));
#74564=CARTESIAN_POINT('Ctrl Pts',(-0.257089474046572,0.120693732425444,
-0.025));
#74565=CARTESIAN_POINT('Ctrl Pts',(-0.266057137277679,0.105712016764972,
-0.0249999999999999));
#74566=CARTESIAN_POINT('Ctrl Pts',(-0.273660374531991,0.08998965119933,
-0.0250000000000001));
#74567=CARTESIAN_POINT('Ctrl Pts',(-0.279780120884689,0.0737160442147271,
-0.025));
#74568=CARTESIAN_POINT('Ctrl Pts',(-0.285570983375405,0.0583170039858358,
-0.025));
#74569=CARTESIAN_POINT('Ctrl Pts',(-0.290034213990896,0.0424230946399918,
-0.0249999999999999));
#74570=CARTESIAN_POINT('Ctrl Pts',(-0.293033728012268,0.0261701021632011,
-0.0249999999999999));
#74571=CARTESIAN_POINT('',(-0.201387638828722,-0.215099443244976,-0.0249999999999996));
#74572=CARTESIAN_POINT('Origin',(0.,0.,-0.025));
#74573=CARTESIAN_POINT('Ctrl Pts',(-0.201391095966877,-0.215105632705572,
-0.0250000000000002));
#74574=CARTESIAN_POINT('Ctrl Pts',(-0.195338847091654,-0.219844285114016,
-0.0250000000000002));
#74575=CARTESIAN_POINT('Ctrl Pts',(-0.189099169329539,-0.224321659220154,
-0.025));
#74576=CARTESIAN_POINT('Ctrl Pts',(-0.182677962217615,-0.228519790588707,
-0.025));
#74577=CARTESIAN_POINT('Ctrl Pts',(-0.172360604925975,-0.235265192275904,
-0.0249999999999999));
#74578=CARTESIAN_POINT('Ctrl Pts',(-0.161574657667912,-0.241290326536744,
-0.0249999999999998));
#74579=CARTESIAN_POINT('Ctrl Pts',(-0.150403499846521,-0.246587801858931,
-0.0249999999999996));
#74580=CARTESIAN_POINT('Ctrl Pts',(-0.145346996730436,-0.248985646460386,
-0.0249999999999995));
#74581=CARTESIAN_POINT('Ctrl Pts',(-0.140211528852807,-0.251234232658866,
-0.0249999999999997));
#74582=CARTESIAN_POINT('Ctrl Pts',(-0.135004748169044,-0.253332011186455,
-0.0249999999999997));
#74583=CARTESIAN_POINT('Ctrl Pts',(-0.12994533197591,-0.255370417506351,
-0.0249999999999997));
#74584=CARTESIAN_POINT('Ctrl Pts',(-0.124827943389512,-0.25726265675066,
-0.0249999999999999));
#74585=CARTESIAN_POINT('Ctrl Pts',(-0.119660402636152,-0.259008400564028,
-0.0249999999999999));
#74586=CARTESIAN_POINT('Ctrl Pts',(-0.110196620014646,-0.262205538380852,
-0.0249999999999998));
#74587=CARTESIAN_POINT('Ctrl Pts',(-0.100564090906767,-0.264911882417756,
-0.0249999999999998));
#74588=CARTESIAN_POINT('Ctrl Pts',(-0.0908073980509052,-0.267122077440192,
-0.0249999999999994));
#74589=CARTESIAN_POINT('Ctrl Pts',(-0.0835768486991839,-0.268760022225657,
-0.0249999999999992));
#74590=CARTESIAN_POINT('Ctrl Pts',(-0.0762780787142024,-0.27012535733669,
-0.0249999999999998));
#74591=CARTESIAN_POINT('Ctrl Pts',(-0.0689294737833452,-0.271213850448778,
-0.0249999999999998));
#74592=CARTESIAN_POINT('Ctrl Pts',(-0.0632148208849618,-0.272060318639189,
-0.0249999999999998));
#74593=CARTESIAN_POINT('Ctrl Pts',(-0.0574681181846967,-0.272739188122278,
-0.0249999999999998));
#74594=CARTESIAN_POINT('Ctrl Pts',(-0.051719859743331,-0.273246779822699,
-0.0249999999999998));
#74595=CARTESIAN_POINT('Ctrl Pts',(-0.0350403730953272,-0.27471963791984,
-0.0249999999999999));
#74596=CARTESIAN_POINT('Ctrl Pts',(-0.0183065933647195,-0.274761316818117,
-0.0249999999999997));
#74597=CARTESIAN_POINT('Ctrl Pts',(-0.00173104857140306,-0.27333838879637,
-0.0249999999999999));
#74598=CARTESIAN_POINT('Ctrl Pts',(0.00953470964504997,-0.27237127952471,
-0.0250000000000001));
#74599=CARTESIAN_POINT('Ctrl Pts',(0.0207273828667504,-0.270726566241235,
-0.0250000000000006));
#74600=CARTESIAN_POINT('Ctrl Pts',(0.0317746405774151,-0.268380747632881,
-0.0250000000000006));
#74601=CARTESIAN_POINT('Ctrl Pts',(0.0362763732629953,-0.267424831822799,
-0.0250000000000006));
#74602=CARTESIAN_POINT('Ctrl Pts',(0.0407560491401004,-0.266351784795418,
-0.0249999999999997));
#74603=CARTESIAN_POINT('Ctrl Pts',(0.045201428945242,-0.265161414452212,
-0.0249999999999998));
#74604=CARTESIAN_POINT('Ctrl Pts',(0.0584062062305173,-0.261625479176028,
-0.0249999999999999));
#74605=CARTESIAN_POINT('Ctrl Pts',(0.0712526578246137,-0.257072554296891,
-0.0249999999999997));
#74606=CARTESIAN_POINT('Ctrl Pts',(0.0836175868965339,-0.251475521354251,
-0.0249999999999999));
#74607=CARTESIAN_POINT('Ctrl Pts',(0.0983243165227789,-0.244818463338163,
-0.0250000000000001));
#74608=CARTESIAN_POINT('Ctrl Pts',(0.112351532683777,-0.236684173702826,
-0.0249999999999998));
#74609=CARTESIAN_POINT('Ctrl Pts',(0.125552777046004,-0.227237104745598,
-0.0249999999999998));
#74610=CARTESIAN_POINT('Ctrl Pts',(0.129065689842232,-0.224723195562791,
-0.0249999999999998));
#74611=CARTESIAN_POINT('Ctrl Pts',(0.132522069792216,-0.222114399692458,
-0.0250000000000002));
#74612=CARTESIAN_POINT('Ctrl Pts',(0.135911222128229,-0.219419463926651,
-0.0250000000000001));
#74613=CARTESIAN_POINT('Ctrl Pts',(0.148285308267569,-0.209580022083998,
-0.025));
#74614=CARTESIAN_POINT('Ctrl Pts',(0.159725584980566,-0.198630141850697,
-0.0250000000000001));
#74615=CARTESIAN_POINT('Ctrl Pts',(0.170107075094728,-0.186737543339766,
-0.0250000000000002));
#74616=CARTESIAN_POINT('Ctrl Pts',(0.17813376360681,-0.177542506519736,
-0.0250000000000002));
#74617=CARTESIAN_POINT('Ctrl Pts',(0.185526921828335,-0.167782839977552,
-0.025));
#74618=CARTESIAN_POINT('Ctrl Pts',(0.19220906976002,-0.157527458546528,
-0.0250000000000002));
#74619=CARTESIAN_POINT('Ctrl Pts',(0.194577331723896,-0.153892784484171,
-0.0250000000000002));
#74620=CARTESIAN_POINT('Ctrl Pts',(0.196857099713073,-0.150194088388506,
-0.0249999999999999));
#74621=CARTESIAN_POINT('Ctrl Pts',(0.199041135849217,-0.146439874642851,
-0.0249999999999999));
#74622=CARTESIAN_POINT('Ctrl Pts',(0.206823250530982,-0.133062933929713,
-0.0250000000000001));
#74623=CARTESIAN_POINT('Ctrl Pts',(0.213351473427119,-0.119058256565258,
-0.0249999999999998));
#74624=CARTESIAN_POINT('Ctrl Pts',(0.218485133420207,-0.104575147054428,
-0.0249999999999999));
#74625=CARTESIAN_POINT('Ctrl Pts',(0.223304523482539,-0.0909786575825654,
-0.0249999999999999));
#74626=CARTESIAN_POINT('Ctrl Pts',(0.226894965471101,-0.0769592713588295,
-0.0249999999999996));
#74627=CARTESIAN_POINT('Ctrl Pts',(0.22909166963358,-0.0626392569880559,
-0.0249999999999996));
#74628=CARTESIAN_POINT('Ctrl Pts',(0.229234915574686,-0.0617054562650307,
-0.0249999999999996));
#74629=CARTESIAN_POINT('Ctrl Pts',(0.229372216589657,-0.0607703803898239,
-0.0249999999999999));
#74630=CARTESIAN_POINT('Ctrl Pts',(0.229503519150545,-0.0598340649004849,
-0.0249999999999999));
#74631=CARTESIAN_POINT('Ctrl Pts',(-0.103908919352511,0.213201587949043,
-1.98872339910054));
#74632=CARTESIAN_POINT('Ctrl Pts',(-0.174623289681621,0.178737239562729,
-1.98344457275887));
#74633=CARTESIAN_POINT('Ctrl Pts',(-0.277869171354646,0.0345363745701341,
-1.97288692007553));
#74634=CARTESIAN_POINT('Ctrl Pts',(-0.180080572943209,-0.214762747691729,
-1.95705044105053));
#74635=CARTESIAN_POINT('Ctrl Pts',(0.0820053757571985,-0.267731452091956,
-1.94121396202553));
#74636=CARTESIAN_POINT('Ctrl Pts',(0.269259772704402,-0.077117310153115,
-1.92537748300052));
#74637=CARTESIAN_POINT('Ctrl Pts',(0.211266823136741,0.183928328504729,
-1.90954100397552));
#74638=CARTESIAN_POINT('Ctrl Pts',(-0.0392343044552656,0.277314777777813,
-1.89370452495051));
#74639=CARTESIAN_POINT('Ctrl Pts',(-0.253973708582438,0.118100076701569,
-1.87786804592551));
#74640=CARTESIAN_POINT('Ctrl Pts',(-0.237338474913823,-0.148734949670181,
-1.8620315669005));
#74641=CARTESIAN_POINT('Ctrl Pts',(-0.00447048967563682,-0.280051476296464,
-1.8461950878755));
#74642=CARTESIAN_POINT('Ctrl Pts',(0.232467885064925,-0.156232942395582,
-1.8303586088505));
#74643=CARTESIAN_POINT('Ctrl Pts',(0.257616875906963,0.109925723244754,
-1.81452212982549));
#74644=CARTESIAN_POINT('Ctrl Pts',(0.0480624401227571,0.27593430904298,
-1.79868565080049));
#74645=CARTESIAN_POINT('Ctrl Pts',(-0.205279094840265,0.190552960999229,
-1.78284917177548));
#74646=CARTESIAN_POINT('Ctrl Pts',(-0.271600582044837,-0.0684328367816128,
-1.76701269275048));
#74647=CARTESIAN_POINT('Ctrl Pts',(-0.0904793175238351,-0.265072392539203,
-1.75117621372547));
#74648=CARTESIAN_POINT('Ctrl Pts',(0.173073393005469,-0.22021696378749,
-1.73533973470047));
#74649=CARTESIAN_POINT('Ctrl Pts',(0.278947013657325,0.025267969059772,
-1.71950325567547));
#74650=CARTESIAN_POINT('Ctrl Pts',(0.130684973650179,0.247732392338888,
-1.70366677665046));
#74651=CARTESIAN_POINT('Ctrl Pts',(-0.136638058709272,0.244499378342932,
-1.68783029762546));
#74652=CARTESIAN_POINT('Ctrl Pts',(-0.279476516397372,0.018514345000666,
-1.67199381860045));
#74653=CARTESIAN_POINT('Ctrl Pts',(-0.167696920049829,-0.224338241203619,
-1.65615733957545));
#74654=CARTESIAN_POINT('Ctrl Pts',(0.0968635373620719,-0.262806695604708,
-1.64032086055044));
#74655=CARTESIAN_POINT('Ctrl Pts',(0.273176132803676,-0.0618441946515969,
-1.62448438152544));
#74656=CARTESIAN_POINT('Ctrl Pts',(0.200610662303521,0.195461674084374,
-1.60864790250043));
#74657=CARTESIAN_POINT('Ctrl Pts',(-0.054721849483307,0.274691505419439,
-1.59281142347543));
#74658=CARTESIAN_POINT('Ctrl Pts',(-0.260199830103213,0.103662685391739,
-1.57697494445043));
#74659=CARTESIAN_POINT('Ctrl Pts',(-0.22862185072271,-0.161808384494801,
-1.56113846542542));
#74660=CARTESIAN_POINT('Ctrl Pts',(0.011242860680614,-0.279863363121343,
-1.54530198640042));
#74661=CARTESIAN_POINT('Ctrl Pts',(0.240864724779504,-0.142947851629034,
-1.52946550737541));
#74662=CARTESIAN_POINT('Ctrl Pts',(0.251045943848778,0.124200797119059,
-1.51362902835041));
#74663=CARTESIAN_POINT('Ctrl Pts',(0.0325108828631745,0.278195877800473,
-1.4977925493254));
#74664=CARTESIAN_POINT('Ctrl Pts',(-0.215643331000489,0.178739636689401,
-1.4819560703004));
#74665=CARTESIAN_POINT('Ctrl Pts',(-0.267334938339562,-0.083557971922713,
-1.46611959127539));
#74666=CARTESIAN_POINT('Ctrl Pts',(-0.0754701205516332,-0.269729799675546,
-1.45028311225039));
#74667=CARTESIAN_POINT('Ctrl Pts',(0.185152012983061,-0.210163355552944,
-1.43444663322539));
#74668=CARTESIAN_POINT('Ctrl Pts',(0.277090761295361,0.0408731444070958,
-1.41861015420038));
#74669=CARTESIAN_POINT('Ctrl Pts',(0.116585008054319,0.254672024034776,
-1.40277367517538));
#74670=CARTESIAN_POINT('Ctrl Pts',(-0.150135922153628,0.236451070642649,
-1.38693719615037));
#74671=CARTESIAN_POINT('Ctrl Pts',(-0.280074998444266,0.00281054717502342,
-1.37110071712537));
#74672=CARTESIAN_POINT('Ctrl Pts',(-0.154850773550475,-0.233390535069016,
-1.35526423810037));
#74673=CARTESIAN_POINT('Ctrl Pts',(0.11145078701977,-0.256960358813676,
-1.33942775907536));
#74674=CARTESIAN_POINT('Ctrl Pts',(0.276214720548922,-0.0464255541815164,
-1.32359128005036));
#74675=CARTESIAN_POINT('Ctrl Pts',(0.189332272492804,0.206405413014511,
-1.30775480102535));
#74676=CARTESIAN_POINT('Ctrl Pts',(-0.0700420007471637,0.271190010989185,
-1.29191832200035));
#74677=CARTESIAN_POINT('Ctrl Pts',(-0.265604265662634,0.0889060064944594,
-1.27608184297534));
#74678=CARTESIAN_POINT('Ctrl Pts',(-0.219186840810713,-0.174376124353075,
-1.26024536395034));
#74679=CARTESIAN_POINT('Ctrl Pts',(0.0269215174987288,-0.278792280783643,
-1.24440888492533));
#74680=CARTESIAN_POINT('Ctrl Pts',(0.248502933681857,-0.129213760414636,
-1.22857240590033));
#74681=CARTESIAN_POINT('Ctrl Pts',(0.243684888061905,0.138085405670681,
-1.21273592687532));
#74682=CARTESIAN_POINT('Ctrl Pts',(0.0168568778538109,0.279581382781475,
-1.19689944785032));
#74683=CARTESIAN_POINT('Ctrl Pts',(-0.22532864953623,0.166363768973774,
-1.18106296882532));
#74684=CARTESIAN_POINT('Ctrl Pts',(-0.262227727273618,-0.0984201350227347,
-1.16522648980031));
#74685=CARTESIAN_POINT('Ctrl Pts',(-0.0602233222835258,-0.273538032789071,
-1.14939001077531));
#74686=CARTESIAN_POINT('Ctrl Pts',(0.196647749876134,-0.199448154660888,
-1.1335535317503));
#74687=CARTESIAN_POINT('Ctrl Pts',(0.274362205745136,0.0563496582744192,
-1.1177170527253));
#74688=CARTESIAN_POINT('Ctrl Pts',(0.102118020082256,0.260809919104815,
-1.1018805737003));
#74689=CARTESIAN_POINT('Ctrl Pts',(-0.16316114285223,0.227658396269794,
-1.08604409467529));
#74690=CARTESIAN_POINT('Ctrl Pts',(-0.279791779261826,-0.012902100080281,
-1.07020761565029));
#74691=CARTESIAN_POINT('Ctrl Pts',(-0.141517142307931,-0.241708093290185,
-1.05437113662528));
#74692=CARTESIAN_POINT('Ctrl Pts',(0.125687179216381,-0.250305087662256,
-1.03853465760028));
#74693=CARTESIAN_POINT('Ctrl Pts',(0.278383759087368,-0.0308607615811162,
-1.02269817857527));
#74694=CARTESIAN_POINT('Ctrl Pts',(0.177457847270645,0.216699368644785,
-1.00686169955027));
#74695=CARTESIAN_POINT('Ctrl Pts',(-0.0851416533425872,0.26683478557915,
-0.991025220525264));
#74696=CARTESIAN_POINT('Ctrl Pts',(-0.270172554631098,0.0738694432975277,
-0.975188741500262));
#74697=CARTESIAN_POINT('Ctrl Pts',(-0.209061810603051,-0.186394912152542,
-0.959352262475254));
#74698=CARTESIAN_POINT('Ctrl Pts',(0.0425154229059733,-0.276843534770285,
-0.943515783450253));
#74699=CARTESIAN_POINT('Ctrl Pts',(0.255358832545678,-0.115072892419929,
-0.927679304425247));
#74700=CARTESIAN_POINT('Ctrl Pts',(0.2355566898837,0.151535308690796,-0.911842825400244));
#74701=CARTESIAN_POINT('Ctrl Pts',(0.00114980584647748,0.280086739913719,
-0.896006346375237));
#74702=CARTESIAN_POINT('Ctrl Pts',(-0.23430461280518,0.153464172845634,
-0.880169867350236));
#74703=CARTESIAN_POINT('Ctrl Pts',(-0.25629499925759,-0.112972462505392,
-0.86433338832523));
#74704=CARTESIAN_POINT('Ctrl Pts',(-0.0447869354702739,-0.276485143073116,
-0.848496909300226));
#74705=CARTESIAN_POINT('Ctrl Pts',(0.20752442160637,-0.188105072674614,
-0.832660430275222));
#74706=CARTESIAN_POINT('Ctrl Pts',(0.270769932793133,0.0716487782462665,
-0.816823951250217));
#74707=CARTESIAN_POINT('Ctrl Pts',(0.0873295552116665,0.266126760615149,
-0.800987472225213));
#74708=CARTESIAN_POINT('Ctrl Pts',(-0.175672717299923,0.218149032373378,
-0.785150993200208));
#74709=CARTESIAN_POINT('Ctrl Pts',(-0.278627749881924,-0.0285741303405044,
-0.769314514175204));
#74710=CARTESIAN_POINT('Ctrl Pts',(-0.127738002114452,-0.249264732252255,
-0.753478035150199));
#74711=CARTESIAN_POINT('Ctrl Pts',(0.139527896638572,-0.242861833124507,
-0.737641556125195));
#74712=CARTESIAN_POINT('Ctrl Pts',(0.279676420005076,-0.015198816471186,
-0.721805077100191));
#74713=CARTESIAN_POINT('Ctrl Pts',(0.165024768460067,0.226311134776178,
-0.705968598075186));
#74714=CARTESIAN_POINT('Ctrl Pts',(-0.0999732721998829,0.261639539776823,
-0.690132119050183));
#74715=CARTESIAN_POINT('Ctrl Pts',(-0.273890315603988,0.0586003323141388,
-0.674295640025178));
#74716=CARTESIAN_POINT('Ctrl Pts',(-0.198278634630123,-0.197826911663192,
-0.658459161000173));
#74717=CARTESIAN_POINT('Ctrl Pts',(0.057975485860299,-0.274023259903682,
-0.64262268197517));
#74718=CARTESIAN_POINT('Ctrl Pts',(0.261410838370488,-0.100569764399713,
-0.626786202950165));
#74719=CARTESIAN_POINT('Ctrl Pts',(0.22668693762885,0.16450816465285,-0.610949723925161));
#74720=CARTESIAN_POINT('Ctrl Pts',(-0.0145608858552237,0.279710358285275,
-0.595113244900156));
#74721=CARTESIAN_POINT('Ctrl Pts',(-0.242542963650923,0.140081457418103,
-0.579276765875153));
#74722=CARTESIAN_POINT('Ctrl Pts',(-0.249555431064008,-0.12716914230876,
-0.563440286850147));
#74723=CARTESIAN_POINT('Ctrl Pts',(-0.0292095552737704,-0.278561852753679,
-0.547603807825144));
#74724=CARTESIAN_POINT('Ctrl Pts',(0.217747787412377,-0.176169818657624,
-0.531767328800138));
#74725=CARTESIAN_POINT('Ctrl Pts',(0.26632525124544,0.0867223412897275,
-0.515930849775135));
#74726=CARTESIAN_POINT('Ctrl Pts',(0.0722661688848724,0.270605810659411,
-0.50009437075013));
#74727=CARTESIAN_POINT('Ctrl Pts',(-0.187631257907944,0.207952915306194,
-0.484257891725126));
#74728=CARTESIAN_POINT('Ctrl Pts',(-0.276586574783934,-0.0441562066210817,
-0.468421412700122));
#74729=CARTESIAN_POINT('Ctrl Pts',(-0.113556730952469,-0.256036662952951,
-0.452584933675117));
#74730=CARTESIAN_POINT('Ctrl Pts',(0.15292936740834,-0.23465402726664,-0.436748454650113));
#74731=CARTESIAN_POINT('Ctrl Pts',(0.280088633943004,0.000510975941890648,
-0.420911975625108));
#74732=CARTESIAN_POINT('Ctrl Pts',(0.152072176426899,0.235210452621709,
-0.405075496600104));
#74733=CARTESIAN_POINT('Ctrl Pts',(-0.114490165816999,0.255620628817145,
-0.389239017575099));
#74734=CARTESIAN_POINT('Ctrl Pts',(-0.276745845119702,0.0431467418693552,
-0.373402538550095));
#74735=CARTESIAN_POINT('Ctrl Pts',(-0.18687125857253,-0.208636133447806,
-0.357566059525091));
#74736=CARTESIAN_POINT('Ctrl Pts',(0.0732530352383368,-0.270340335534277,
-0.341729580500087));
#74737=CARTESIAN_POINT('Ctrl Pts',(0.266639901610645,-0.0857500318774511,
-0.325893101475082));
#74738=CARTESIAN_POINT('Ctrl Pts',(0.217103548889173,0.176963130656145,
-0.310056622450078));
#74739=CARTESIAN_POINT('Ctrl Pts',(-0.0302257286171684,0.27845342881406,
-0.294220143425073));
#74740=CARTESIAN_POINT('Ctrl Pts',(-0.250017785961877,0.126257741184162,
-0.27838366440007));
#74741=CARTESIAN_POINT('Ctrl Pts',(-0.242030203238965,-0.140965459975633,
-0.262547185375064));
#74742=CARTESIAN_POINT('Ctrl Pts',(-0.0135402899116431,-0.27976166618424,
-0.246710706350061));
#74743=CARTESIAN_POINT('Ctrl Pts',(0.227285795344374,-0.163679885626449,
-0.230874227325056));
#74744=CARTESIAN_POINT('Ctrl Pts',(0.261041901008646,0.101522741173457,
-0.215037748300052));
#74745=CARTESIAN_POINT('Ctrl Pts',(0.056975763960648,0.274233261483808,
-0.199201269275047));
#74746=CARTESIAN_POINT('Ctrl Pts',(-0.199000038459435,0.197101584390596,
-0.183364790250044));
#74747=CARTESIAN_POINT('Ctrl Pts',(-0.27367292212579,-0.0595982075980484,
-0.167528311225039));
#74748=CARTESIAN_POINT('Ctrl Pts',(-0.0990213293987983,-0.262004605402092,
-0.151691832200035));
#74749=CARTESIAN_POINT('Ctrl Pts',(0.165855812771546,-0.225703615695282,
-0.13585535317503));
#74750=CARTESIAN_POINT('Ctrl Pts',(0.279606860807486,0.0162117244434021,
-0.120018874150026));
#74751=CARTESIAN_POINT('Ctrl Pts',(0.138664230983235,0.2433835073103,-0.104182395125021));
#74752=CARTESIAN_POINT('Ctrl Pts',(-0.128691327754114,0.248769867313068,
-0.0883459161000173));
#74753=CARTESIAN_POINT('Ctrl Pts',(-0.278644470573634,0.027609257706179,
-0.0725094370750125));
#74754=CARTESIAN_POINT('Ctrl Pts',(-0.175042138878516,-0.218888784921681,
-0.0566729580500086));
#74755=CARTESIAN_POINT('Ctrl Pts',(0.0886436604710861,-0.265605608028242,
-0.0408364790250042));
#74756=CARTESIAN_POINT('Ctrl Pts',(0.209657849780202,-0.135955434357285,
-0.030278826341668));
#74757=CARTESIAN_POINT('Ctrl Pts',(0.229503519150545,-0.0598340649004849,
-0.0249999999999999));
#74758=CARTESIAN_POINT('Ctrl Pts',(-0.112236674703449,0.230288577939267,
-1.97774893273369));
#74759=CARTESIAN_POINT('Ctrl Pts',(-0.188618431235458,0.193062092640366,
-1.97247010639202));
#74760=CARTESIAN_POINT('Ctrl Pts',(-0.300138929264063,0.0373042840039045,
-1.96191245370869));
#74761=CARTESIAN_POINT('Ctrl Pts',(-0.194513087151547,-0.231974856454063,
-1.94607597468368));
#74762=CARTESIAN_POINT('Ctrl Pts',(0.0885776768745912,-0.289188724929234,
-1.93023949565868));
#74763=CARTESIAN_POINT('Ctrl Pts',(0.290839532429595,-0.0832978584282747,
-1.91440301663368));
#74764=CARTESIAN_POINT('Ctrl Pts',(0.228198751866404,0.198669220157139,
-1.89856653760867));
#74765=CARTESIAN_POINT('Ctrl Pts',(-0.0423787283498021,0.29954010394735,
-1.88273005858367));
#74766=CARTESIAN_POINT('Ctrl Pts',(-0.274328370374944,0.127565178945213,
-1.86689357955866));
#74767=CARTESIAN_POINT('Ctrl Pts',(-0.25635990990481,-0.160655276440064,
-1.85105710053366));
#74768=CARTESIAN_POINT('Ctrl Pts',(-0.00482877599551976,-0.30249613451059,
-1.83522062150865));
#74769=CARTESIAN_POINT('Ctrl Pts',(0.251098967803868,-0.168754193989144,
-1.81938414248365));
#74770=CARTESIAN_POINT('Ctrl Pts',(0.278263518468496,0.118735693896566,
-1.80354766345864));
#74771=CARTESIAN_POINT('Ctrl Pts',(0.0519143928271621,0.298048997877773,
-1.78771118443364));
#74772=CARTESIAN_POINT('Ctrl Pts',(-0.22173113852568,0.20582478222966,-1.77187470540863));
#74773=CARTESIAN_POINT('Ctrl Pts',(-0.293367945371645,-0.0739173700270646,
-1.75603822638363));
#74774=CARTESIAN_POINT('Ctrl Pts',(-0.0977307606660977,-0.28631655568814,
-1.74020174735863));
#74775=CARTESIAN_POINT('Ctrl Pts',(0.186944318462953,-0.237866199387058,
-1.72436526833362));
#74776=CARTESIAN_POINT('Ctrl Pts',(0.301303154978865,0.0272930643630038,
-1.70852878930862));
#74777=CARTESIAN_POINT('Ctrl Pts',(0.141158689433044,0.26758684534212,-1.69269231028361));
#74778=CARTESIAN_POINT('Ctrl Pts',(-0.14758888306245,0.264094722217014,
-1.67685583125861));
#74779=CARTESIAN_POINT('Ctrl Pts',(-0.301875094588665,0.0199981727279622,
-1.6610193522336));
#74780=CARTESIAN_POINT('Ctrl Pts',(-0.181136949375352,-0.242317775590514,
-1.6451828732086));
#74781=CARTESIAN_POINT('Ctrl Pts',(0.104626642267832,-0.283869275017742,
-1.6293463941836));
#74782=CARTESIAN_POINT('Ctrl Pts',(0.295069768267124,-0.066800682758141,
-1.61350991515859));
#74783=CARTESIAN_POINT('Ctrl Pts',(0.216688555586061,0.211126902944442,
-1.59767343613359));
#74784=CARTESIAN_POINT('Ctrl Pts',(-0.0591075189492908,0.296706590056724,
-1.58183695710859));
#74785=CARTESIAN_POINT('Ctrl Pts',(-0.281053482907591,0.111970706381115,
-1.56600047808358));
#74786=CARTESIAN_POINT('Ctrl Pts',(-0.246944693964287,-0.174776478554483,
-1.55016399905858));
#74787=CARTESIAN_POINT('Ctrl Pts',(0.0121439170459008,-0.302292945050291,
-1.53432752003357));
#74788=CARTESIAN_POINT('Ctrl Pts',(0.260168770217893,-0.154404372818236,
-1.51849104100857));
#74789=CARTESIAN_POINT('Ctrl Pts',(0.271165960640848,0.134154840133307,
-1.50265456198356));
#74790=CARTESIAN_POINT('Ctrl Pts',(0.0351164597512303,0.300491819519417,
-1.48681808295856));
#74791=CARTESIAN_POINT('Ctrl Pts',(-0.23292601390032,0.193064681884179,
-1.47098160393355));
#74792=CARTESIAN_POINT('Ctrl Pts',(-0.288760432677517,-0.0902547054863841,
-1.45514512490855));
#74793=CARTESIAN_POINT('Ctrl Pts',(-0.0815186552123387,-0.291347229599299,
-1.43930864588355));
#74794=CARTESIAN_POINT('Ctrl Pts',(0.199990976533686,-0.227006847138492,
-1.42347216685854));
#74795=CARTESIAN_POINT('Ctrl Pts',(0.299298133717789,0.0441489127354228,
-1.40763568783354));
#74796=CARTESIAN_POINT('Ctrl Pts',(0.12592868548561,0.275082652151262,-1.39179920880853));
#74797=CARTESIAN_POINT('Ctrl Pts',(-0.162168529526256,0.255401384831746,
-1.37596272978353));
#74798=CARTESIAN_POINT('Ctrl Pts',(-0.30252154183527,0.00303579780241857,
-1.36012625075852));
#74799=CARTESIAN_POINT('Ctrl Pts',(-0.167261251554365,-0.252095563370635,
-1.34428977173352));
#74800=CARTESIAN_POINT('Ctrl Pts',(0.120382983541046,-0.277554384970663,
-1.32845329270851));
#74801=CARTESIAN_POINT('Ctrl Pts',(0.298351882896418,-0.0501463190558393,
-1.31261681368351));
#74802=CARTESIAN_POINT('Ctrl Pts',(0.204506261936469,0.222947725199116,
-1.2967803346585));
#74803=CARTESIAN_POINT('Ctrl Pts',(-0.0756555000516231,0.292924469197482,
-1.2809438556335));
#74804=CARTESIAN_POINT('Ctrl Pts',(-0.286891055655131,0.0960313570026611,
-1.2651073766085));
#74805=CARTESIAN_POINT('Ctrl Pts',(-0.236753517452057,-0.188351456901099,
-1.24927089758349));
#74806=CARTESIAN_POINT('Ctrl Pts',(0.0290791360439149,-0.301136021076236,
-1.23343441855849));
#74807=CARTESIAN_POINT('Ctrl Pts',(0.268419141535702,-0.139569566166572,
-1.21759793953348));
#74808=CARTESIAN_POINT('Ctrl Pts',(0.263214954808303,0.149152227297988,
-1.20176146050848));
#74809=CARTESIAN_POINT('Ctrl Pts',(0.0182078682752508,0.301988365463902,
-1.18592498148348));
#74810=CARTESIAN_POINT('Ctrl Pts',(-0.243387559960744,0.179696953226935,
-1.17008850245847));
#74811=CARTESIAN_POINT('Ctrl Pts',(-0.283243905409001,-0.10630799307364,
-1.15425202343347));
#74812=CARTESIAN_POINT('Ctrl Pts',(-0.0650499059639579,-0.295460672639808,
-1.13841554440846));
#74813=CARTESIAN_POINT('Ctrl Pts',(0.212408036495276,-0.215432879047998,
-1.12257906538346));
#74814=CARTESIAN_POINT('Ctrl Pts',(0.296350898739221,0.0608657880844716,
-1.10674258635845));
#74815=CARTESIAN_POINT('Ctrl Pts',(0.110302244241902,0.281712467345497,
-1.09090610733345));
#74816=CARTESIAN_POINT('Ctrl Pts',(-0.176237653405123,0.245904023685958,
-1.07506962830844));
#74817=CARTESIAN_POINT('Ctrl Pts',(-0.302215624119569,-0.0139361357881993,
-1.05923314928344));
#74818=CARTESIAN_POINT('Ctrl Pts',(-0.152858999642686,-0.261079730295029,
-1.04339667025844));
#74819=CARTESIAN_POINT('Ctrl Pts',(0.135760347966338,-0.270365728713436,
-1.02756019123343));
#74820=CARTESIAN_POINT('Ctrl Pts',(0.300694758506864,-0.033334089895883,
-1.01172371220843));
#74821=CARTESIAN_POINT('Ctrl Pts',(0.191680163760733,0.234066687427635,
-0.995887233183423));
#74822=CARTESIAN_POINT('Ctrl Pts',(-0.091965310672772,0.288220195294412,
-0.980050754158418));
#74823=CARTESIAN_POINT('Ctrl Pts',(-0.291825469044278,0.0797896920646727,
-0.964214275133414));
#74824=CARTESIAN_POINT('Ctrl Pts',(-0.225817019133517,-0.201333487558182,
-0.94837779610841));
#74825=CARTESIAN_POINT('Ctrl Pts',(0.0459228112496179,-0.29903109328232,
-0.932541317083406));
#74826=CARTESIAN_POINT('Ctrl Pts',(0.275824504765089,-0.124295381707372,
-0.9167048380584));
#74827=CARTESIAN_POINT('Ctrl Pts',(0.254435324141974,0.163680069560886,
-0.900868359033398));
#74828=CARTESIAN_POINT('Ctrl Pts',(0.00124195675951194,0.302534224321969,
-0.885031880008392));
#74829=CARTESIAN_POINT('Ctrl Pts',(-0.253082899647124,0.165763522069517,
-0.869195400983389));
#74830=CARTESIAN_POINT('Ctrl Pts',(-0.276835700332977,-0.122026613342493,
-0.853358921958384));
#74831=CARTESIAN_POINT('Ctrl Pts',(-0.0483763736420793,-0.298643978368776,
-0.83752244293338));
#74832=CARTESIAN_POINT('Ctrl Pts',(0.224156416465443,-0.203180708483996,
-0.821685963908375));
#74833=CARTESIAN_POINT('Ctrl Pts',(0.292470723935438,0.0773910523469543,
-0.805849484883371));
#74834=CARTESIAN_POINT('Ctrl Pts',(0.0943285614109523,0.287455425839952,
-0.790013005858366));
#74835=CARTESIAN_POINT('Ctrl Pts',(-0.189751964977836,0.235632534107109,
-0.774176526833362));
#74836=CARTESIAN_POINT('Ctrl Pts',(-0.300958303884969,-0.0308641971444335,
-0.758340047808358));
#74837=CARTESIAN_POINT('Ctrl Pts',(-0.137975533572346,-0.269241994269309,
-0.742503568783354));
#74838=CARTESIAN_POINT('Ctrl Pts',(0.150710326357575,-0.262325936330895,
-0.726667089758349));
#74839=CARTESIAN_POINT('Ctrl Pts',(0.30209101942293,-0.0164169219618871,
-0.710830610733345));
#74840=CARTESIAN_POINT('Ctrl Pts',(0.178250638839094,0.244448786243956,
-0.69499413170834));
#74841=CARTESIAN_POINT('Ctrl Pts',(-0.107985606056314,0.282608577766738,
-0.679157652683337));
#74842=CARTESIAN_POINT('Ctrl Pts',(-0.295841189076202,0.0632968418538111,
-0.663321173658332));
#74843=CARTESIAN_POINT('Ctrl Pts',(-0.214169628115642,-0.213681701920165,
-0.647484694633328));
#74844=CARTESIAN_POINT('Ctrl Pts',(0.0626219172312024,-0.295984788164822,
-0.631648215608323));
#74845=CARTESIAN_POINT('Ctrl Pts',(0.282361547141194,-0.108629903980044,
-0.615811736583319));
#74846=CARTESIAN_POINT('Ctrl Pts',(0.244854707725876,0.177692631943989,
-0.599975257558314));
#74847=CARTESIAN_POINT('Ctrl Pts',(-0.015727864550129,0.302127677678435,
-0.584138778533311));
#74848=CARTESIAN_POINT('Ctrl Pts',(-0.261981511140039,0.151308252132651,
-0.568302299508305));
#74849=CARTESIAN_POINT('Ctrl Pts',(-0.269555991067417,-0.137361082634337,
-0.552465820483302));
#74850=CARTESIAN_POINT('Ctrl Pts',(-0.0315505480561581,-0.30088712544723,
-0.536629341458297));
#74851=CARTESIAN_POINT('Ctrl Pts',(0.235199131465207,-0.190288906404298,
-0.520792862433293));
#74852=CARTESIAN_POINT('Ctrl Pts',(0.287669824454071,0.0936726824752729,
-0.504956383408288));
#74853=CARTESIAN_POINT('Ctrl Pts',(0.0780579236098103,0.29229344827278,
-0.489119904383284));
#74854=CARTESIAN_POINT('Ctrl Pts',(-0.202668919946804,0.224619251689788,
-0.473283425358279));
#74855=CARTESIAN_POINT('Ctrl Pts',(-0.298753539299663,-0.0476950951809576,
-0.457446946333276));
#74856=CARTESIAN_POINT('Ctrl Pts',(-0.122657707843746,-0.276556659727332,
-0.441610467308271));
#74857=CARTESIAN_POINT('Ctrl Pts',(0.165185854779071,-0.253460317846565,
-0.425773988283267));
#74858=CARTESIAN_POINT('Ctrl Pts',(0.302536270147776,0.000551927985859205,
-0.409937509258262));
#74859=CARTESIAN_POINT('Ctrl Pts',(0.164259964432584,0.254061337777891,
-0.394101030233258));
#74860=CARTESIAN_POINT('Ctrl Pts',(-0.123665952620994,0.276107282635772,
-0.378264551208253));
#74861=CARTESIAN_POINT('Ctrl Pts',(-0.298925574318185,0.0466047271194889,
-0.362428072183249));
#74862=CARTESIAN_POINT('Ctrl Pts',(-0.201848010647438,-0.22535722618504,
-0.346591593158245));
#74863=CARTESIAN_POINT('Ctrl Pts',(0.0791238821298226,-0.292006696707592,
-0.330755114133241));
#74864=CARTESIAN_POINT('Ctrl Pts',(0.28800969239712,-0.0926224475589986,
-0.314918635108236));
#74865=CARTESIAN_POINT('Ctrl Pts',(0.234503260600505,0.191145798202142,
-0.299082156083232));
#74866=CARTESIAN_POINT('Ctrl Pts',(-0.0326481623677637,0.300770011897047,
-0.283245677058228));
#74867=CARTESIAN_POINT('Ctrl Pts',(-0.270055401287376,0.136376637485807,
-0.267409198033223));
#74868=CARTESIAN_POINT('Ctrl Pts',(-0.261427655668188,-0.152263102862543,
-0.251572719008219));
#74869=CARTESIAN_POINT('Ctrl Pts',(-0.0146254731901128,-0.302183097636622,
-0.235736239983215));
#74870=CARTESIAN_POINT('Ctrl Pts',(0.245501560748979,-0.176797970694225,
-0.21989976095821));
#74871=CARTESIAN_POINT('Ctrl Pts',(0.281963041383219,0.109659256848121,
-0.204063281933207));
#74872=CARTESIAN_POINT('Ctrl Pts',(0.0615420728603457,0.29621162027108,
-0.188226802908201));
#74873=CARTESIAN_POINT('Ctrl Pts',(-0.21494884868135,0.212898243467754,
-0.172390323883198));
#74874=CARTESIAN_POINT('Ctrl Pts',(-0.295606372649979,-0.0643746916123519,
-0.156553844858193));
#74875=CARTESIAN_POINT('Ctrl Pts',(-0.106957370028386,-0.283002901488742,
-0.140717365833189));
#74876=CARTESIAN_POINT('Ctrl Pts',(0.179148286997041,-0.243792577692436,
-0.124880886808184));
#74877=CARTESIAN_POINT('Ctrl Pts',(0.30201588542018,0.0175110091999229,
-0.10904440778318));
#74878=CARTESIAN_POINT('Ctrl Pts',(0.149777442426009,0.262889419968842,
-0.0932079287581753));
#74879=CARTESIAN_POINT('Ctrl Pts',(-0.139005263266115,0.268707468498589,
-0.0773714497331711));
#74880=CARTESIAN_POINT('Ctrl Pts',(-0.300976364652495,0.0298219950248908,
-0.0615349707081665));
#74881=CARTESIAN_POINT('Ctrl Pts',(-0.189070849000505,-0.236431573945479,
-0.0456984916831625));
#74882=CARTESIAN_POINT('Ctrl Pts',(0.0957479853203354,-0.286892505604309,
-0.0298620126581582));
#74883=CARTESIAN_POINT('Ctrl Pts',(0.226460827727168,-0.146851549945951,
-0.0193043599748219));
#74884=CARTESIAN_POINT('Ctrl Pts',(0.247897023496224,-0.0646294516415712,
-0.0140255336331538));
#74885=CARTESIAN_POINT('Ctrl Pts',(-0.120564430054386,0.247375567929492,
-1.96677446636685));
#74886=CARTESIAN_POINT('Ctrl Pts',(-0.202613572789294,0.207386945718002,
-1.96149564002518));
#74887=CARTESIAN_POINT('Ctrl Pts',(-0.322408687173481,0.0400721934376747,
-1.95093798734184));
#74888=CARTESIAN_POINT('Ctrl Pts',(-0.208945601359885,-0.249186965216397,
-1.93510150831684));
#74889=CARTESIAN_POINT('Ctrl Pts',(0.0951499779919838,-0.310645997766512,
-1.91926502929183));
#74890=CARTESIAN_POINT('Ctrl Pts',(0.312419292154789,-0.0894784067034342,
-1.90342855026683));
#74891=CARTESIAN_POINT('Ctrl Pts',(0.245130680596067,0.213410111809549,
-1.88759207124182));
#74892=CARTESIAN_POINT('Ctrl Pts',(-0.0455231522443386,0.321765430116887,
-1.87175559221682));
#74893=CARTESIAN_POINT('Ctrl Pts',(-0.29468303216745,0.137030281188856,
-1.85591911319181));
#74894=CARTESIAN_POINT('Ctrl Pts',(-0.275381344895796,-0.172575603209946,
-1.84008263416681));
#74895=CARTESIAN_POINT('Ctrl Pts',(-0.00518706231540278,-0.324940792724715,
-1.82424615514181));
#74896=CARTESIAN_POINT('Ctrl Pts',(0.269730050542811,-0.181275445582706,
-1.8084096761168));
#74897=CARTESIAN_POINT('Ctrl Pts',(0.29891016103003,0.127545664548378,-1.7925731970918));
#74898=CARTESIAN_POINT('Ctrl Pts',(0.0557663455315671,0.320163686712565,
-1.7767367180668));
#74899=CARTESIAN_POINT('Ctrl Pts',(-0.238183182211095,0.22109660346009,
-1.76090023904179));
#74900=CARTESIAN_POINT('Ctrl Pts',(-0.315135308698453,-0.0794019032725162,
-1.74506376001679));
#74901=CARTESIAN_POINT('Ctrl Pts',(-0.10498220380836,-0.307560718837078,
-1.72922728099178));
#74902=CARTESIAN_POINT('Ctrl Pts',(0.200815243920436,-0.255515434986625,
-1.71339080196678));
#74903=CARTESIAN_POINT('Ctrl Pts',(0.323659296300406,0.0293181596662353,
-1.69755432294177));
#74904=CARTESIAN_POINT('Ctrl Pts',(0.151632405215908,0.287441298345352,
-1.68171784391677));
#74905=CARTESIAN_POINT('Ctrl Pts',(-0.158539707415627,0.283690066091096,
-1.66588136489176));
#74906=CARTESIAN_POINT('Ctrl Pts',(-0.324273672779959,0.0214820004552588,
-1.65004488586676));
#74907=CARTESIAN_POINT('Ctrl Pts',(-0.194576978700875,-0.26029730997741,
-1.63420840684176));
#74908=CARTESIAN_POINT('Ctrl Pts',(0.112389747173591,-0.304931854430775,
-1.61837192781675));
#74909=CARTESIAN_POINT('Ctrl Pts',(0.316963403730571,-0.0717571708646853,
-1.60253544879175));
#74910=CARTESIAN_POINT('Ctrl Pts',(0.232766448868601,0.226792131804511,
-1.58669896976674));
#74911=CARTESIAN_POINT('Ctrl Pts',(-0.0634931884152743,0.318721674694008,
-1.57086249074174));
#74912=CARTESIAN_POINT('Ctrl Pts',(-0.30190713571197,0.12027872737049,-1.55502601171673));
#74913=CARTESIAN_POINT('Ctrl Pts',(-0.265267537205865,-0.187744572614164,
-1.53918953269173));
#74914=CARTESIAN_POINT('Ctrl Pts',(0.0130449734111871,-0.324722526979239,
-1.52335305366672));
#74915=CARTESIAN_POINT('Ctrl Pts',(0.279472815656283,-0.165860894007438,
-1.50751657464172));
#74916=CARTESIAN_POINT('Ctrl Pts',(0.291285977432917,0.144108883147556,
-1.49168009561671));
#74917=CARTESIAN_POINT('Ctrl Pts',(0.0377220366392867,0.322787761238361,
-1.47584361659171));
#74918=CARTESIAN_POINT('Ctrl Pts',(-0.25020869680015,0.207389727078957,
-1.46000713756671));
#74919=CARTESIAN_POINT('Ctrl Pts',(-0.310185927015473,-0.0969514390500553,
-1.4441706585417));
#74920=CARTESIAN_POINT('Ctrl Pts',(-0.0875671898730442,-0.312964659523051,
-1.4283341795167));
#74921=CARTESIAN_POINT('Ctrl Pts',(0.21482994008431,-0.243850338724041,
-1.4124977004917));
#74922=CARTESIAN_POINT('Ctrl Pts',(0.321505506140217,0.0474246810637503,
-1.39666122146669));
#74923=CARTESIAN_POINT('Ctrl Pts',(0.135272362916901,0.295493280267748,
-1.38082474244169));
#74924=CARTESIAN_POINT('Ctrl Pts',(-0.174201136898885,0.274351699020844,
-1.36498826341668));
#74925=CARTESIAN_POINT('Ctrl Pts',(-0.324968085226274,0.00326104842981355,
-1.34915178439168));
#74926=CARTESIAN_POINT('Ctrl Pts',(-0.179671729558254,-0.270800591672255,
-1.33331530536667));
#74927=CARTESIAN_POINT('Ctrl Pts',(0.129315180062322,-0.298148411127651,
-1.31747882634167));
#74928=CARTESIAN_POINT('Ctrl Pts',(0.320489045243914,-0.0538670839301619,
-1.30164234731666));
#74929=CARTESIAN_POINT('Ctrl Pts',(0.219680251380133,0.239490037383722,
-1.28580586829166));
#74930=CARTESIAN_POINT('Ctrl Pts',(-0.0812689993560826,0.314658927405779,
-1.26996938926666));
#74931=CARTESIAN_POINT('Ctrl Pts',(-0.308177845647628,0.103156707510862,
-1.25413291024165));
#74932=CARTESIAN_POINT('Ctrl Pts',(-0.2543201940934,-0.202326789449123,
-1.23829643121665));
#74933=CARTESIAN_POINT('Ctrl Pts',(0.0312367545891007,-0.323479761368829,
-1.22245995219164));
#74934=CARTESIAN_POINT('Ctrl Pts',(0.288335349389547,-0.149925371918507,
-1.20662347316664));
#74935=CARTESIAN_POINT('Ctrl Pts',(0.282745021554701,0.160219048925294,
-1.19078699414163));
#74936=CARTESIAN_POINT('Ctrl Pts',(0.0195588586966912,0.324395348146328,
-1.17495051511663));
#74937=CARTESIAN_POINT('Ctrl Pts',(-0.261446470385259,0.193030137480096,
-1.15911403609162));
#74938=CARTESIAN_POINT('Ctrl Pts',(-0.304260083544383,-0.114195851124544,
-1.14327755706662));
#74939=CARTESIAN_POINT('Ctrl Pts',(-0.0698764896443907,-0.317383312490547,
-1.12744107804161));
#74940=CARTESIAN_POINT('Ctrl Pts',(0.228168323114419,-0.231417603435108,
-1.11160459901661));
#74941=CARTESIAN_POINT('Ctrl Pts',(0.318339591733306,0.0653819178945236,
-1.09576811999161));
#74942=CARTESIAN_POINT('Ctrl Pts',(0.118486468401548,0.302615015586179,
-1.0799316409666));
#74943=CARTESIAN_POINT('Ctrl Pts',(-0.189314163958016,0.264149651102121,
-1.0640951619416));
#74944=CARTESIAN_POINT('Ctrl Pts',(-0.324639468977312,-0.0149701714961173,
-1.04825868291659));
#74945=CARTESIAN_POINT('Ctrl Pts',(-0.16420085697744,-0.280451367299874,
-1.03242220389159));
#74946=CARTESIAN_POINT('Ctrl Pts',(0.145833516716294,-0.290426369764615,
-1.01658572486659));
#74947=CARTESIAN_POINT('Ctrl Pts',(0.32300575792636,-0.0358074182106502,
-1.00074924584158));
#74948=CARTESIAN_POINT('Ctrl Pts',(0.205902480250821,0.251434006210486,
-0.984912766816576));
#74949=CARTESIAN_POINT('Ctrl Pts',(-0.0987889680029566,0.309605605009673,
-0.969076287791573));
#74950=CARTESIAN_POINT('Ctrl Pts',(-0.313478383457458,0.0857099408318177,
-0.953239808766568));
#74951=CARTESIAN_POINT('Ctrl Pts',(-0.242572227663983,-0.216272062963821,
-0.937403329741564));
#74952=CARTESIAN_POINT('Ctrl Pts',(0.0493301995932623,-0.321218651794355,
-0.921566850716559));
#74953=CARTESIAN_POINT('Ctrl Pts',(0.2962901769845,-0.133517870994815,-0.905730371691556));
#74954=CARTESIAN_POINT('Ctrl Pts',(0.273313958400249,0.175824830430977,
-0.889893892666551));
#74955=CARTESIAN_POINT('Ctrl Pts',(0.00133410767254648,0.324981708730219,
-0.874057413641547));
#74956=CARTESIAN_POINT('Ctrl Pts',(-0.271861186489069,0.1780628712934,-0.858220934616542));
#74957=CARTESIAN_POINT('Ctrl Pts',(-0.297376401408364,-0.131080764179595,
-0.842384455591539));
#74958=CARTESIAN_POINT('Ctrl Pts',(-0.0519658118138847,-0.320802813664435,
-0.826547976566532));
#74959=CARTESIAN_POINT('Ctrl Pts',(0.240788411324516,-0.218256344293379,
-0.81071149754153));
#74960=CARTESIAN_POINT('Ctrl Pts',(0.314171515077743,0.0831333264476419,
-0.794875018516525));
#74961=CARTESIAN_POINT('Ctrl Pts',(0.101327567610238,0.308784091064756,
-0.77903853949152));
#74962=CARTESIAN_POINT('Ctrl Pts',(-0.203831212655749,0.253116035840839,
-0.763202060466517));
#74963=CARTESIAN_POINT('Ctrl Pts',(-0.323288857888015,-0.0331542639483626,
-0.747365581441511));
#74964=CARTESIAN_POINT('Ctrl Pts',(-0.14821306503024,-0.289219256286362,
-0.731529102416508));
#74965=CARTESIAN_POINT('Ctrl Pts',(0.161892756076577,-0.281790039537284,
-0.715692623391503));
#74966=CARTESIAN_POINT('Ctrl Pts',(0.324505618840786,-0.0176350274525877,
-0.699856144366499));
#74967=CARTESIAN_POINT('Ctrl Pts',(0.19147650921812,0.262586437711734,-0.684019665341494));
#74968=CARTESIAN_POINT('Ctrl Pts',(-0.115997939912744,0.303577615756652,
-0.668183186316491));
#74969=CARTESIAN_POINT('Ctrl Pts',(-0.317792062548416,0.0679933513934832,
-0.652346707291485));
#74970=CARTESIAN_POINT('Ctrl Pts',(-0.230060621601161,-0.229536492177137,
-0.636510228266482));
#74971=CARTESIAN_POINT('Ctrl Pts',(0.0672683486021056,-0.317946316425962,
-0.620673749241476));
#74972=CARTESIAN_POINT('Ctrl Pts',(0.3033122559119,-0.116690043560375,-0.604837270216474));
#74973=CARTESIAN_POINT('Ctrl Pts',(0.263022477822901,0.190877099235128,
-0.589000791191468));
#74974=CARTESIAN_POINT('Ctrl Pts',(-0.0168948432450345,0.324544997071594,
-0.573164312166465));
#74975=CARTESIAN_POINT('Ctrl Pts',(-0.281420058629155,0.162535046847199,
-0.557327833141459));
#74976=CARTESIAN_POINT('Ctrl Pts',(-0.289556551070826,-0.147553022959913,
-0.541491354116455));
#74977=CARTESIAN_POINT('Ctrl Pts',(-0.0338915408385456,-0.32321239814078,
-0.525654875091451));
#74978=CARTESIAN_POINT('Ctrl Pts',(0.252650475518037,-0.204407994150972,
-0.509818396066447));
#74979=CARTESIAN_POINT('Ctrl Pts',(0.309014397662703,0.100623023660818,
-0.493981917041442));
#74980=CARTESIAN_POINT('Ctrl Pts',(0.0838496783347481,0.313981085886149,
-0.478145438016439));
#74981=CARTESIAN_POINT('Ctrl Pts',(-0.217706581985663,0.241285588073381,
-0.462308958991433));
#74982=CARTESIAN_POINT('Ctrl Pts',(-0.320920503815392,-0.0512339837408334,
-0.44647247996643));
#74983=CARTESIAN_POINT('Ctrl Pts',(-0.131758684735023,-0.297076656501713,
-0.430636000941424));
#74984=CARTESIAN_POINT('Ctrl Pts',(0.177442342149801,-0.272266608426489,
-0.414799521916421));
#74985=CARTESIAN_POINT('Ctrl Pts',(0.324983906352547,0.000592880029827996,
-0.398963042891416));
#74986=CARTESIAN_POINT('Ctrl Pts',(0.17644775243827,0.272912222934072,-0.383126563866412));
#74987=CARTESIAN_POINT('Ctrl Pts',(-0.13284173942499,0.296593936454399,
-0.367290084841407));
#74988=CARTESIAN_POINT('Ctrl Pts',(-0.321105303516668,0.050062712369623,
-0.351453605816403));
#74989=CARTESIAN_POINT('Ctrl Pts',(-0.216824762722347,-0.242078318922273,
-0.335617126791399));
#74990=CARTESIAN_POINT('Ctrl Pts',(0.0849947290213087,-0.313673057880906,
-0.319780647766394));
#74991=CARTESIAN_POINT('Ctrl Pts',(0.309379483183595,-0.0994948632405462,
-0.303944168741391));
#74992=CARTESIAN_POINT('Ctrl Pts',(0.251902972311837,0.205328465748139,
-0.288107689716385));
#74993=CARTESIAN_POINT('Ctrl Pts',(-0.0350705961183589,0.323086594980033,
-0.272271210691382));
#74994=CARTESIAN_POINT('Ctrl Pts',(-0.290093016612875,0.146495533787453,
-0.256434731666377));
#74995=CARTESIAN_POINT('Ctrl Pts',(-0.280825108097411,-0.163560745749454,
-0.240598252641373));
#74996=CARTESIAN_POINT('Ctrl Pts',(-0.0157106564685821,-0.324604529089004,
-0.224761773616368));
#74997=CARTESIAN_POINT('Ctrl Pts',(0.263717326153585,-0.189916055762002,
-0.208925294591364));
#74998=CARTESIAN_POINT('Ctrl Pts',(0.302884181757793,0.117795772522785,
-0.19308881556636));
#74999=CARTESIAN_POINT('Ctrl Pts',(0.0661083817600436,0.318189979058352,
-0.177252336541355));
#75000=CARTESIAN_POINT('Ctrl Pts',(-0.230897658903266,0.228694902544912,
-0.161415857516351));
#75001=CARTESIAN_POINT('Ctrl Pts',(-0.317539823174168,-0.0691511756266552,
-0.145579378491346));
#75002=CARTESIAN_POINT('Ctrl Pts',(-0.114893410657975,-0.304001197575392,
-0.129742899466343));
#75003=CARTESIAN_POINT('Ctrl Pts',(0.192440761222538,-0.261881539689589,
-0.113906420441338));
#75004=CARTESIAN_POINT('Ctrl Pts',(0.324424910032874,0.0188102939564436,
-0.0980699414163339));
#75005=CARTESIAN_POINT('Ctrl Pts',(0.160890653868784,0.282395332627384,
-0.0822334623913293));
#75006=CARTESIAN_POINT('Ctrl Pts',(-0.149319198778117,0.288645069684111,
-0.0663969833663251));
#75007=CARTESIAN_POINT('Ctrl Pts',(-0.323308258731355,0.0320347323436027,
-0.0505605043413203));
#75008=CARTESIAN_POINT('Ctrl Pts',(-0.203099559122495,-0.253974362969278,
-0.0347240253163165));
#75009=CARTESIAN_POINT('Ctrl Pts',(0.102852310169585,-0.308179403180376,
-0.0188875462913121));
#75010=CARTESIAN_POINT('Ctrl Pts',(0.243263805674134,-0.157747665534617,
-0.00832989360797585));
#75011=CARTESIAN_POINT('Ctrl Pts',(0.266290527841904,-0.0694248383826575,
-0.00305106726630777));
#75012=CARTESIAN_POINT('Ctrl Pts',(-0.128892185405323,0.264462557919717,
-1.9558));
#75013=CARTESIAN_POINT('Ctrl Pts',(-0.216608714343131,0.221711798795639,
-1.95052117365833));
#75014=CARTESIAN_POINT('Ctrl Pts',(-0.344678445082899,0.0428401028714452,
-1.93996352097499));
#75015=CARTESIAN_POINT('Ctrl Pts',(-0.223378115568222,-0.266399073978732,
-1.92412704194999));
#75016=CARTESIAN_POINT('Ctrl Pts',(0.101722279109376,-0.33210327060379,
-1.90829056292499));
#75017=CARTESIAN_POINT('Ctrl Pts',(0.333999051879982,-0.0956589549785939,
-1.89245408389998));
#75018=CARTESIAN_POINT('Ctrl Pts',(0.262062609325731,0.228151003461959,
-1.87661760487498));
#75019=CARTESIAN_POINT('Ctrl Pts',(-0.0486675761388747,0.343990756286424,
-1.86078112584997));
#75020=CARTESIAN_POINT('Ctrl Pts',(-0.315037693959957,0.1464953834325,-1.84494464682497));
#75021=CARTESIAN_POINT('Ctrl Pts',(-0.294402779886782,-0.184495929979829,
-1.82910816779997));
#75022=CARTESIAN_POINT('Ctrl Pts',(-0.00554534863528576,-0.347385450938841,
-1.81327168877496));
#75023=CARTESIAN_POINT('Ctrl Pts',(0.288361133281754,-0.193796697176269,
-1.79743520974996));
#75024=CARTESIAN_POINT('Ctrl Pts',(0.319556803591563,0.13635563520019,-1.78159873072495));
#75025=CARTESIAN_POINT('Ctrl Pts',(0.059618298235972,0.342278375547357,
-1.76576225169995));
#75026=CARTESIAN_POINT('Ctrl Pts',(-0.25463522589651,0.236368424690521,
-1.74992577267494));
#75027=CARTESIAN_POINT('Ctrl Pts',(-0.336902672025262,-0.0848864365179679,
-1.73408929364994));
#75028=CARTESIAN_POINT('Ctrl Pts',(-0.112233646950622,-0.328804881986015,
-1.71825281462494));
#75029=CARTESIAN_POINT('Ctrl Pts',(0.214686169377919,-0.273164670586193,
-1.70241633559993));
#75030=CARTESIAN_POINT('Ctrl Pts',(0.346015437621946,0.0313432549694672,
-1.68657985657493));
#75031=CARTESIAN_POINT('Ctrl Pts',(0.162106120998773,0.307295751348583,
-1.67074337754992));
#75032=CARTESIAN_POINT('Ctrl Pts',(-0.169490531768806,0.303285409965179,
-1.65490689852492));
#75033=CARTESIAN_POINT('Ctrl Pts',(-0.346672250971252,0.0229658281825551,
-1.63907041949991));
#75034=CARTESIAN_POINT('Ctrl Pts',(-0.208017008026398,-0.278276844364305,
-1.62323394047491));
#75035=CARTESIAN_POINT('Ctrl Pts',(0.120152852079351,-0.325994433843809,
-1.6073974614499));
#75036=CARTESIAN_POINT('Ctrl Pts',(0.338857039194018,-0.0767136589712294,
-1.5915609824249));
#75037=CARTESIAN_POINT('Ctrl Pts',(0.248844342151141,0.242457360664579,
-1.5757245033999));
#75038=CARTESIAN_POINT('Ctrl Pts',(-0.067878857881258,0.340736759331293,
-1.55988802437489));
#75039=CARTESIAN_POINT('Ctrl Pts',(-0.322760788516348,0.128586748359866,
-1.54405154534989));
#75040=CARTESIAN_POINT('Ctrl Pts',(-0.283590380447442,-0.200712666673845,
-1.52821506632488));
#75041=CARTESIAN_POINT('Ctrl Pts',(0.0139460297764737,-0.347152108908187,
-1.51237858729988));
#75042=CARTESIAN_POINT('Ctrl Pts',(0.298776861094673,-0.17731741519664,
-1.49654210827488));
#75043=CARTESIAN_POINT('Ctrl Pts',(0.311405994224987,0.154062926161804,
-1.48070562924987));
#75044=CARTESIAN_POINT('Ctrl Pts',(0.0403276135273424,0.345083702957305,
-1.46486915022487));
#75045=CARTESIAN_POINT('Ctrl Pts',(-0.267491379699981,0.221714772273735,
-1.44903267119986));
#75046=CARTESIAN_POINT('Ctrl Pts',(-0.331611421353429,-0.103648172613727,
-1.43319619217486));
#75047=CARTESIAN_POINT('Ctrl Pts',(-0.0936157245337495,-0.334582089446802,
-1.41735971314985));
#75048=CARTESIAN_POINT('Ctrl Pts',(0.229668903634934,-0.26069383030959,
-1.40152323412485));
#75049=CARTESIAN_POINT('Ctrl Pts',(0.343712878562645,0.0507004493920776,
-1.38568675509984));
#75050=CARTESIAN_POINT('Ctrl Pts',(0.144616040348191,0.315903908384234,
-1.36985027607484));
#75051=CARTESIAN_POINT('Ctrl Pts',(-0.186233744271513,0.293302013209942,
-1.35401379704983));
#75052=CARTESIAN_POINT('Ctrl Pts',(-0.347414628617279,0.00348629905720863,
-1.33817731802483));
#75053=CARTESIAN_POINT('Ctrl Pts',(-0.192082207562143,-0.289505619973874,
-1.32234083899983));
#75054=CARTESIAN_POINT('Ctrl Pts',(0.138247376583598,-0.318742437284638,
-1.30650435997482));
#75055=CARTESIAN_POINT('Ctrl Pts',(0.34262620759141,-0.0575878488044848,
-1.29066788094982));
#75056=CARTESIAN_POINT('Ctrl Pts',(0.234854240823797,0.256032349568327,
-1.27483140192481));
#75057=CARTESIAN_POINT('Ctrl Pts',(-0.0868824986605421,0.336393385614076,
-1.25899492289981));
#75058=CARTESIAN_POINT('Ctrl Pts',(-0.329464635640125,0.110282058019064,
-1.2431584438748));
#75059=CARTESIAN_POINT('Ctrl Pts',(-0.271886870734743,-0.216302121997147,
-1.2273219648498));
#75060=CARTESIAN_POINT('Ctrl Pts',(0.0333943731342868,-0.345823501661423,
-1.2114854858248));
#75061=CARTESIAN_POINT('Ctrl Pts',(0.308251557243392,-0.160281177670443,
-1.19564900679979));
#75062=CARTESIAN_POINT('Ctrl Pts',(0.302275088301099,0.171285870552601,
-1.17981252777479));
#75063=CARTESIAN_POINT('Ctrl Pts',(0.0209098491181311,0.346802330828755,
-1.16397604874978));
#75064=CARTESIAN_POINT('Ctrl Pts',(-0.279505380809773,0.206363321733258,
-1.14813956972478));
#75065=CARTESIAN_POINT('Ctrl Pts',(-0.325276261679767,-0.122083709175449,
-1.13230309069977));
#75066=CARTESIAN_POINT('Ctrl Pts',(-0.0747030733248228,-0.339305952341285,
-1.11646661167477));
#75067=CARTESIAN_POINT('Ctrl Pts',(0.243928609733561,-0.247402327822217,
-1.10063013264977));
#75068=CARTESIAN_POINT('Ctrl Pts',(0.340328284727392,0.0698980477045754,
-1.08479365362476));
#75069=CARTESIAN_POINT('Ctrl Pts',(0.126670692561194,0.323517563826862,
-1.06895717459976));
#75070=CARTESIAN_POINT('Ctrl Pts',(-0.202390674510908,0.282395278518285,
-1.05312069557475));
#75071=CARTESIAN_POINT('Ctrl Pts',(-0.347063313835056,-0.0160042072040358,
-1.03728421654975));
#75072=CARTESIAN_POINT('Ctrl Pts',(-0.175542714312195,-0.299823004304718,
-1.02144773752474));
#75073=CARTESIAN_POINT('Ctrl Pts',(0.15590668546625,-0.310487010815796,
-1.00561125849974));
#75074=CARTESIAN_POINT('Ctrl Pts',(0.345316757345856,-0.0382807465254171,
-0.989774779474735));
#75075=CARTESIAN_POINT('Ctrl Pts',(0.220124796740909,0.268801324993337,
-0.973938300449731));
#75076=CARTESIAN_POINT('Ctrl Pts',(-0.105612625333141,0.330991014724935,
-0.958101821424727));
#75077=CARTESIAN_POINT('Ctrl Pts',(-0.335131297870638,0.0916301895989631,
-0.942265342399722));
#75078=CARTESIAN_POINT('Ctrl Pts',(-0.259327436194449,-0.23121063836946,
-0.926428863374718));
#75079=CARTESIAN_POINT('Ctrl Pts',(0.0527375879369066,-0.34340621030639,
-0.910592384349713));
#75080=CARTESIAN_POINT('Ctrl Pts',(0.316755849203911,-0.142740360282258,
-0.894755905324709));
#75081=CARTESIAN_POINT('Ctrl Pts',(0.292192592658523,0.187969591301068,
-0.878919426299706));
#75082=CARTESIAN_POINT('Ctrl Pts',(0.00142625858558128,0.347429193138468,
-0.863082947274699));
#75083=CARTESIAN_POINT('Ctrl Pts',(-0.290639473331014,0.190362220517284,
-0.847246468249698));
#75084=CARTESIAN_POINT('Ctrl Pts',(-0.31791710248375,-0.140134915016696,
-0.83140998922469));
#75085=CARTESIAN_POINT('Ctrl Pts',(-0.0555552499856906,-0.342961648960095,
-0.815573510199689));
#75086=CARTESIAN_POINT('Ctrl Pts',(0.25742040618359,-0.233331980102762,
-0.799737031174682));
#75087=CARTESIAN_POINT('Ctrl Pts',(0.335872306220048,0.08887560054833,-0.78390055214968));
#75088=CARTESIAN_POINT('Ctrl Pts',(0.108326573809524,0.330112756289559,
-0.768064073124673));
#75089=CARTESIAN_POINT('Ctrl Pts',(-0.217910460333662,0.270599537574571,
-0.752227594099671));
#75090=CARTESIAN_POINT('Ctrl Pts',(-0.34561941189106,-0.0354443307522923,
-0.736391115074665));
#75091=CARTESIAN_POINT('Ctrl Pts',(-0.158450596488134,-0.309196518303415,
-0.720554636049662));
#75092=CARTESIAN_POINT('Ctrl Pts',(0.173075185795579,-0.301254142743674,
-0.704718157024656));
#75093=CARTESIAN_POINT('Ctrl Pts',(0.346920218258641,-0.0188531329432885,
-0.688881677999654));
#75094=CARTESIAN_POINT('Ctrl Pts',(0.204702379597146,0.280724089179512,
-0.673045198974647));
#75095=CARTESIAN_POINT('Ctrl Pts',(-0.124010273769175,0.324546653746567,
-0.657208719949646));
#75096=CARTESIAN_POINT('Ctrl Pts',(-0.33974293602063,0.0726898609331555,
-0.641372240924638));
#75097=CARTESIAN_POINT('Ctrl Pts',(-0.24595161508668,-0.24539128243411,
-0.625535761899637));
#75098=CARTESIAN_POINT('Ctrl Pts',(0.0719147799730091,-0.339907844687102,
-0.609699282874629));
#75099=CARTESIAN_POINT('Ctrl Pts',(0.324262964682606,-0.124750183140707,
-0.593862803849628));
#75100=CARTESIAN_POINT('Ctrl Pts',(0.281190247919927,0.204061566526267,
-0.578026324824621));
#75101=CARTESIAN_POINT('Ctrl Pts',(-0.0180618219399402,0.346962316464754,
-0.562189845799619));
#75102=CARTESIAN_POINT('Ctrl Pts',(-0.30085860611827,0.173761841561747,
-0.546353366774613));
#75103=CARTESIAN_POINT('Ctrl Pts',(-0.309557111074236,-0.157744963285489,
-0.53051688774961));
#75104=CARTESIAN_POINT('Ctrl Pts',(-0.036232533620933,-0.34553767083433,
-0.514680408724605));
#75105=CARTESIAN_POINT('Ctrl Pts',(0.270101819570867,-0.218527081897646,
-0.498843929699601));
#75106=CARTESIAN_POINT('Ctrl Pts',(0.330358970871335,0.107573364846364,
-0.483007450674596));
#75107=CARTESIAN_POINT('Ctrl Pts',(0.0896414330596858,0.335668723499518,
-0.467170971649592));
#75108=CARTESIAN_POINT('Ctrl Pts',(-0.232744244024522,0.257951924456976,
-0.451334492624587));
#75109=CARTESIAN_POINT('Ctrl Pts',(-0.343087468331121,-0.0547728723007094,
-0.435498013599583));
#75110=CARTESIAN_POINT('Ctrl Pts',(-0.1408596616263,-0.317596653276093,
-0.419661534574579));
#75111=CARTESIAN_POINT('Ctrl Pts',(0.189698829520533,-0.291072899006414,
-0.403825055549575));
#75112=CARTESIAN_POINT('Ctrl Pts',(0.347431542557318,0.00063383207379672,
-0.38798857652457));
#75113=CARTESIAN_POINT('Ctrl Pts',(0.188635540443955,0.291763108090254,
-0.372152097499566));
#75114=CARTESIAN_POINT('Ctrl Pts',(-0.142017526228985,0.317080590273025,
-0.356315618474562));
#75115=CARTESIAN_POINT('Ctrl Pts',(-0.343285032715151,0.053520697619757,
-0.340479139449557));
#75116=CARTESIAN_POINT('Ctrl Pts',(-0.231801514797257,-0.258799411659507,
-0.324642660424553));
#75117=CARTESIAN_POINT('Ctrl Pts',(0.0908655759127951,-0.33533941905422,
-0.308806181399548));
#75118=CARTESIAN_POINT('Ctrl Pts',(0.33074927397007,-0.106367278922094,
-0.292969702374544));
#75119=CARTESIAN_POINT('Ctrl Pts',(0.269302684023171,0.219511133294136,
-0.27713322334954));
#75120=CARTESIAN_POINT('Ctrl Pts',(-0.0374930298689546,0.34540317806302,
-0.261296744324536));
#75121=CARTESIAN_POINT('Ctrl Pts',(-0.310130631938373,0.156614430089098,
-0.245460265299531));
#75122=CARTESIAN_POINT('Ctrl Pts',(-0.300222560526634,-0.174858388636364,
-0.229623786274527));
#75123=CARTESIAN_POINT('Ctrl Pts',(-0.0167958397470517,-0.347025960541386,
-0.213787307249522));
#75124=CARTESIAN_POINT('Ctrl Pts',(0.28193309155819,-0.203034140829778,
-0.197950828224518));
#75125=CARTESIAN_POINT('Ctrl Pts',(0.323805322132367,0.125932288197448,
-0.182114349199514));
#75126=CARTESIAN_POINT('Ctrl Pts',(0.0706746906597415,0.340168337845624,
-0.166277870174509));
#75127=CARTESIAN_POINT('Ctrl Pts',(-0.246846469125181,0.24449156162207,
-0.150441391149505));
#75128=CARTESIAN_POINT('Ctrl Pts',(-0.339473273698357,-0.0739276596409582,
-0.134604912124501));
#75129=CARTESIAN_POINT('Ctrl Pts',(-0.122829451287563,-0.324999493662042,
-0.118768433099497));
#75130=CARTESIAN_POINT('Ctrl Pts',(0.205733235448034,-0.279970501686742,
-0.102931954074492));
#75131=CARTESIAN_POINT('Ctrl Pts',(0.346833934645568,0.0201095787129644,
-0.0870954750494877));
#75132=CARTESIAN_POINT('Ctrl Pts',(0.172003865311559,0.301901245285926,
-0.0712589960244833));
#75133=CARTESIAN_POINT('Ctrl Pts',(-0.159633134290119,0.308582670869633,
-0.055422516999479));
#75134=CARTESIAN_POINT('Ctrl Pts',(-0.345640152810216,0.0342474696623144,
-0.0395860379744743));
#75135=CARTESIAN_POINT('Ctrl Pts',(-0.217128269244485,-0.271517151993076,
-0.0237495589494704));
#75136=CARTESIAN_POINT('Ctrl Pts',(0.109956635018834,-0.329466300756443,
-0.00791307992446606));
#75137=CARTESIAN_POINT('Ctrl Pts',(0.260066783621101,-0.168643781123282,
0.00264457275887023));
#75138=CARTESIAN_POINT('Ctrl Pts',(0.284684032187583,-0.0742202251237438,
0.0079233991005383));
#75139=CARTESIAN_POINT('Ctrl Pts',(-0.294543724507234,0.000174101626290112,
-0.0380176117089602));
#75140=CARTESIAN_POINT('Ctrl Pts',(-0.294041378396576,-0.0797773756946391,
-0.0336784078059734));
#75141=CARTESIAN_POINT('Ctrl Pts',(-0.259412827341036,-0.160153784999754,
-0.0293392039029866));
#75142=CARTESIAN_POINT('Ctrl Pts',(-0.201391095966871,-0.215105632705578,
-0.0249999999999998));
#75143=CARTESIAN_POINT('',(-0.137702479013099,-0.193106208855767,-1.9558));
#75144=CARTESIAN_POINT('Ctrl Pts',(-0.137997372405516,-0.193358576631783,
-1.9558));
#75145=CARTESIAN_POINT('Ctrl Pts',(-0.143505274448249,-0.19036485287795,
-1.9558));
#75146=CARTESIAN_POINT('Ctrl Pts',(-0.14887540128292,-0.187145389562404,
-1.9558));
#75147=CARTESIAN_POINT('Ctrl Pts',(-0.154092081256687,-0.183703367937111,
-1.9558));
#75148=CARTESIAN_POINT('Ctrl Pts',(-0.16443175217884,-0.176881141714411,
-1.9558));
#75149=CARTESIAN_POINT('Ctrl Pts',(-0.174169408604617,-0.169186267076578,
-1.9558));
#75150=CARTESIAN_POINT('Ctrl Pts',(-0.183273675663744,-0.160739807585122,
-1.9558));
#75151=CARTESIAN_POINT('Ctrl Pts',(-0.187814117952941,-0.156527424356474,
-1.9558));
#75152=CARTESIAN_POINT('Ctrl Pts',(-0.192198049343805,-0.152125795074728,
-1.9558));
#75153=CARTESIAN_POINT('Ctrl Pts',(-0.196405468670295,-0.147565936149503,
-1.9558));
#75154=CARTESIAN_POINT('Ctrl Pts',(-0.204392135759571,-0.138910256174714,
-1.9558));
#75155=CARTESIAN_POINT('Ctrl Pts',(-0.211756830622369,-0.129673890671042,
-1.9558));
#75156=CARTESIAN_POINT('Ctrl Pts',(-0.218472220131354,-0.119953568208016,
-1.9558));
#75157=CARTESIAN_POINT('Ctrl Pts',(-0.221655180907846,-0.115346329105464,
-1.9558));
#75158=CARTESIAN_POINT('Ctrl Pts',(-0.224692139350014,-0.110630122164558,
-1.9558));
#75159=CARTESIAN_POINT('Ctrl Pts',(-0.227579351596024,-0.105814103687251,
-1.9558));
#75160=CARTESIAN_POINT('Ctrl Pts',(-0.230045055361972,-0.101701183027268,
-1.9558));
#75161=CARTESIAN_POINT('Ctrl Pts',(-0.232399169828432,-0.0975190606622559,
-1.9558));
#75162=CARTESIAN_POINT('Ctrl Pts',(-0.234635497318627,-0.0932823518783036,
-1.9558));
#75163=CARTESIAN_POINT('Ctrl Pts',(-0.24211369915942,-0.0791149441234151,
-1.9558));
#75164=CARTESIAN_POINT('Ctrl Pts',(-0.248293672678524,-0.0643135493120521,
-1.9558));
#75165=CARTESIAN_POINT('Ctrl Pts',(-0.253104718557175,-0.0490960513030699,
-1.9558));
#75166=CARTESIAN_POINT('Ctrl Pts',(-0.256357398355311,-0.0388077169989578,
-1.9558));
#75167=CARTESIAN_POINT('Ctrl Pts',(-0.258983760288555,-0.0283281491712129,
-1.9558));
#75168=CARTESIAN_POINT('Ctrl Pts',(-0.260951076224304,-0.0177169355128009,
-1.9558));
#75169=CARTESIAN_POINT('Ctrl Pts',(-0.261969717926436,-0.0122226351077254,
-1.9558));
#75170=CARTESIAN_POINT('Ctrl Pts',(-0.262811586922912,-0.00668935134157141,
-1.9558));
#75171=CARTESIAN_POINT('Ctrl Pts',(-0.263468876989419,-0.00115163278850291,
-1.9558));
#75172=CARTESIAN_POINT('Ctrl Pts',(-0.264804897455981,0.0101044407503528,
-1.9558));
#75173=CARTESIAN_POINT('Ctrl Pts',(-0.265383724412674,0.0213987430783344,
-1.9558));
#75174=CARTESIAN_POINT('Ctrl Pts',(-0.265178397174566,0.0326600289712171,
-1.9558));
#75175=CARTESIAN_POINT('Ctrl Pts',(-0.26496718827068,0.0442438980754525,
-1.9558));
#75176=CARTESIAN_POINT('Ctrl Pts',(-0.263926601173681,0.055793119684933,
-1.9558));
#75177=CARTESIAN_POINT('Ctrl Pts',(-0.262109315712585,0.0672496706236925,
-1.9558));
#75178=CARTESIAN_POINT('Ctrl Pts',(-0.260957978128992,0.0745079456479108,
-1.9558));
#75179=CARTESIAN_POINT('Ctrl Pts',(-0.259494575539872,0.081729090187899,
-1.9558));
#75180=CARTESIAN_POINT('Ctrl Pts',(-0.257729496911758,0.0888984323365508,
-1.9558));
#75181=CARTESIAN_POINT('Ctrl Pts',(-0.256693970271012,0.0931045026346703,
-1.9558));
#75182=CARTESIAN_POINT('Ctrl Pts',(-0.255554797525397,0.0972910160978816,
-1.9558));
#75183=CARTESIAN_POINT('Ctrl Pts',(-0.254317934884101,0.101443693338831,
-1.9558));
#75184=CARTESIAN_POINT('Ctrl Pts',(-0.249598061917379,0.117290326905624,
-1.9558));
#75185=CARTESIAN_POINT('Ctrl Pts',(-0.243449028228328,0.132689526577699,
-1.9558));
#75186=CARTESIAN_POINT('Ctrl Pts',(-0.236017898320946,0.147481637055776,
-1.9558));
#75187=CARTESIAN_POINT('Ctrl Pts',(-0.229204595498085,0.161043925608455,
-1.9558));
#75188=CARTESIAN_POINT('Ctrl Pts',(-0.221312550750061,0.174096807174637,
-1.9558));
#75189=CARTESIAN_POINT('Ctrl Pts',(-0.212419504558069,0.186511230090778,
-1.9558));
#75190=CARTESIAN_POINT('Ctrl Pts',(-0.209826346911981,0.19013119956038,
-1.9558));
#75191=CARTESIAN_POINT('Ctrl Pts',(-0.207149372890048,0.193694426785744,
-1.9558));
#75192=CARTESIAN_POINT('Ctrl Pts',(-0.204397403906373,0.197189496801417,
-1.9558));
#75193=CARTESIAN_POINT('Ctrl Pts',(-0.193595728644106,0.210907896809613,
-1.9558));
#75194=CARTESIAN_POINT('Ctrl Pts',(-0.181615745101179,0.223615451460463,
-1.9558));
#75195=CARTESIAN_POINT('Ctrl Pts',(-0.168591987669066,0.235133409074003,
-1.9558));
#75196=CARTESIAN_POINT('Ctrl Pts',(-0.156268150773333,0.246032370586542,
-1.9558));
#75197=CARTESIAN_POINT('Ctrl Pts',(-0.143008760997121,0.255867267553694,
-1.9558));
#75198=CARTESIAN_POINT('Ctrl Pts',(-0.128892185405323,0.264462557919717,
-1.9558));
#75199=CARTESIAN_POINT('Ctrl Pts',(-0.137997372405514,-0.193358576631784,
-1.9558));
#75200=CARTESIAN_POINT('Ctrl Pts',(-0.0790002241827612,-0.234954131459917,
-1.95093798734184));
#75201=CARTESIAN_POINT('Ctrl Pts',(0.0869338825813326,-0.262714517298233,
-1.94079714834202));
#75202=CARTESIAN_POINT('Ctrl Pts',(0.269259772704402,-0.077117310153115,
-1.92537748300052));
#75203=CARTESIAN_POINT('Ctrl Pts',(0.211266823136741,0.183928328504729,
-1.90954100397552));
#75204=CARTESIAN_POINT('Ctrl Pts',(-0.0392343044552656,0.277314777777813,
-1.89370452495051));
#75205=CARTESIAN_POINT('Ctrl Pts',(-0.213703631858497,0.147957606827352,
-1.88083786056184));
#75206=CARTESIAN_POINT('Ctrl Pts',(-0.236917463552764,0.0346120890587808,
-1.87325002251484));
#75207=CARTESIAN_POINT('Ctrl Pts',(-0.236814675525433,8.00967394152356E-5,
-1.8709410108095));
#75208=CARTESIAN_POINT('Origin',(-3.51939854619125E-17,0.,-1.9558));
#75209=CARTESIAN_POINT('',(-0.2942,-3.60291088309151E-17,-1.9558));
#75210=CARTESIAN_POINT('Origin',(0.,0.,-1.9558));
#75211=CARTESIAN_POINT('Origin',(0.,0.,-1.9558));
#75212=CARTESIAN_POINT('',(0.137702479013102,-0.193106208855765,-1.9558));
#75213=CARTESIAN_POINT('Ctrl Pts',(0.129201276660418,0.26483169369169,-1.9558));
#75214=CARTESIAN_POINT('Ctrl Pts',(0.135785829563373,0.260865815094269,
-1.9558));
#75215=CARTESIAN_POINT('Ctrl Pts',(0.142193064090495,0.256631694188274,
-1.9558));
#75216=CARTESIAN_POINT('Ctrl Pts',(0.148404092834589,0.25212844043442,-1.9558));
#75217=CARTESIAN_POINT('Ctrl Pts',(0.158383745515504,0.244892777833401,
-1.9558));
#75218=CARTESIAN_POINT('Ctrl Pts',(0.167857441197493,0.23696258771659,-1.9558));
#75219=CARTESIAN_POINT('Ctrl Pts',(0.176788556648393,0.228413138989074,
-1.9558));
#75220=CARTESIAN_POINT('Ctrl Pts',(0.180831129606409,0.22454332335162,-1.9558));
#75221=CARTESIAN_POINT('Ctrl Pts',(0.184762389846773,0.220546531359166,
-1.9558));
#75222=CARTESIAN_POINT('Ctrl Pts',(0.188578162618967,0.216429360238014,
-1.9558));
#75223=CARTESIAN_POINT('Ctrl Pts',(0.192285937148445,0.212428717870695,
-1.9558));
#75224=CARTESIAN_POINT('Ctrl Pts',(0.195877805523516,0.208321814842972,
-1.9558));
#75225=CARTESIAN_POINT('Ctrl Pts',(0.199350673797985,0.204115840696008,
-1.9558));
#75226=CARTESIAN_POINT('Ctrl Pts',(0.205710856757708,0.19641305355167,-1.9558));
#75227=CARTESIAN_POINT('Ctrl Pts',(0.211672619239862,0.188377677017422,
-1.9558));
#75228=CARTESIAN_POINT('Ctrl Pts',(0.217215067993658,0.180049457174739,
-1.9558));
#75229=CARTESIAN_POINT('Ctrl Pts',(0.221322515103539,0.173877506103499,
-1.9558));
#75230=CARTESIAN_POINT('Ctrl Pts',(0.225199567589628,0.167544651916967,
-1.9558));
#75231=CARTESIAN_POINT('Ctrl Pts',(0.228835718112123,0.161066564540105,
-1.9558));
#75232=CARTESIAN_POINT('Ctrl Pts',(0.23166334902431,0.156028918269595,-1.9558));
#75233=CARTESIAN_POINT('Ctrl Pts',(0.234345811865076,0.15090159384628,-1.9558));
#75234=CARTESIAN_POINT('Ctrl Pts',(0.236868800988663,0.145711771031545,
-1.9558));
#75235=CARTESIAN_POINT('Ctrl Pts',(0.244189693097608,0.130652596762418,
-1.9558));
#75236=CARTESIAN_POINT('Ctrl Pts',(0.250192743403271,0.115032605157703,
-1.9558));
#75237=CARTESIAN_POINT('Ctrl Pts',(0.254770972596117,0.099038452029079,
-1.9558));
#75238=CARTESIAN_POINT('Ctrl Pts',(0.257882624658325,0.0881678211651359,
-1.9558));
#75239=CARTESIAN_POINT('Ctrl Pts',(0.26033512079411,0.0771239681159206,
-1.9558));
#75240=CARTESIAN_POINT('Ctrl Pts',(0.262080723507159,0.0659660971856748,
-1.9558));
#75241=CARTESIAN_POINT('Ctrl Pts',(0.262792052894065,0.0614192885512388,
-1.9558));
#75242=CARTESIAN_POINT('Ctrl Pts',(0.263386081399267,0.056851340822549,
-1.9558));
#75243=CARTESIAN_POINT('Ctrl Pts',(0.263858267251122,0.0522736216863439,
-1.9558));
#75244=CARTESIAN_POINT('Ctrl Pts',(0.265260862420264,0.0386758259859476,
-1.9558));
#75245=CARTESIAN_POINT('Ctrl Pts',(0.26558555294751,0.0250503556577028,
-1.9558));
#75246=CARTESIAN_POINT('Ctrl Pts',(0.264763093706556,0.011502649672878,
-1.9558));
#75247=CARTESIAN_POINT('Ctrl Pts',(0.263784864463184,-0.00461092959650045,
-1.9558));
#75248=CARTESIAN_POINT('Ctrl Pts',(0.261184230539979,-0.0206161268211077,
-1.9558));
#75249=CARTESIAN_POINT('Ctrl Pts',(0.257062644120522,-0.0363174874293233,
-1.9558));
#75250=CARTESIAN_POINT('Ctrl Pts',(0.255965870831883,-0.0404956924110467,
-1.9558));
#75251=CARTESIAN_POINT('Ctrl Pts',(0.254760293306619,-0.0446548960531295,
-1.9558));
#75252=CARTESIAN_POINT('Ctrl Pts',(0.253450272167277,-0.0487819884203261,
-1.9558));
#75253=CARTESIAN_POINT('Ctrl Pts',(0.248667272494634,-0.0638503570507704,
-1.9558));
#75254=CARTESIAN_POINT('Ctrl Pts',(0.242513938635288,-0.0784420159944107,
-1.9558));
#75255=CARTESIAN_POINT('Ctrl Pts',(0.235102432119141,-0.0923804165550677,
-1.9558));
#75256=CARTESIAN_POINT('Ctrl Pts',(0.229372055048817,-0.103157212176276,
-1.9558));
#75257=CARTESIAN_POINT('Ctrl Pts',(0.222888330661629,-0.113543323222854,
-1.9558));
#75258=CARTESIAN_POINT('Ctrl Pts',(0.215688032875387,-0.123441795139812,
-1.9558));
#75259=CARTESIAN_POINT('Ctrl Pts',(0.213136130361168,-0.126949974401518,
-1.9558));
#75260=CARTESIAN_POINT('Ctrl Pts',(0.210492869904086,-0.130398289364971,
-1.9558));
#75261=CARTESIAN_POINT('Ctrl Pts',(0.207763617706553,-0.133776946374647,
-1.9558));
#75262=CARTESIAN_POINT('Ctrl Pts',(0.198038798706408,-0.145815712126074,
-1.9558));
#75263=CARTESIAN_POINT('Ctrl Pts',(0.187280564674133,-0.15690666222773,
-1.9558));
#75264=CARTESIAN_POINT('Ctrl Pts',(0.175578277424442,-0.166865148238431,
-1.9558));
#75265=CARTESIAN_POINT('Ctrl Pts',(0.164592385110822,-0.176213991980338,
-1.9558));
#75266=CARTESIAN_POINT('Ctrl Pts',(0.152773356677846,-0.184565318985801,
-1.9558));
#75267=CARTESIAN_POINT('Ctrl Pts',(0.140176697278149,-0.191721582677799,
-1.9558));
#75268=CARTESIAN_POINT('Ctrl Pts',(0.139355263502201,-0.19218824582393,
-1.9558));
#75269=CARTESIAN_POINT('Ctrl Pts',(0.138530519371653,-0.192649808777216,
-1.9558));
#75270=CARTESIAN_POINT('Ctrl Pts',(0.137702479013106,-0.193106208855762,
-1.9558));
#75271=CARTESIAN_POINT('Origin',(0.,0.,-1.9558));
#75272=CARTESIAN_POINT('Origin',(0.,0.,-2.1406589891905));
#75273=CARTESIAN_POINT('Ctrl Pts',(0.137702479013101,-0.193106208855765,
-1.9558));
#75274=CARTESIAN_POINT('Ctrl Pts',(0.201751645331416,-0.147433265282304,
-1.95052117365833));
#75275=CARTESIAN_POINT('Ctrl Pts',(0.279756535851592,0.0118428723253114,
-1.939963520975));
#75276=CARTESIAN_POINT('Ctrl Pts',(0.142127113353835,0.241561378807579,
-1.92412704194999));
#75277=CARTESIAN_POINT('Ctrl Pts',(-0.125108372180837,0.250505423930283,
-1.90829056292499));
#75278=CARTESIAN_POINT('Ctrl Pts',(-0.23302431186425,0.0962800630305547,
-1.89713454533849));
#75279=CARTESIAN_POINT('Ctrl Pts',(-0.237502612682818,0.00905088842975674,
-1.89125735409366));
#75280=CARTESIAN_POINT('Ctrl Pts',(-0.2374378448428,0.00016285981187146,
-1.8906589891905));
#75281=CARTESIAN_POINT('Ctrl Pts',(0.170810875200393,-0.239535560853239,
-1.98872339910054));
#75282=CARTESIAN_POINT('Ctrl Pts',(0.250259656610106,-0.182881276045346,
-1.98344457275887));
#75283=CARTESIAN_POINT('Ctrl Pts',(0.34701959670091,0.014690304788047,-1.97288692007553));
#75284=CARTESIAN_POINT('Ctrl Pts',(0.176299343306418,0.299641014631343,
-1.95705044105053));
#75285=CARTESIAN_POINT('Ctrl Pts',(-0.155188713378732,0.310735514789881,
-1.94121396202552));
#75286=CARTESIAN_POINT('Ctrl Pts',(-0.34521286206057,0.0391672645750027,
-1.92537748300052));
#75287=CARTESIAN_POINT('Ctrl Pts',(-0.220770872998109,-0.268309353725055,
-1.90954100397551));
#75288=CARTESIAN_POINT('Ctrl Pts',(0.104826783471608,-0.331224318302498,
-1.89370452495051));
#75289=CARTESIAN_POINT('Ctrl Pts',(0.334910327509493,-0.0924376943938123,
-1.87786804592551));
#75290=CARTESIAN_POINT('Ctrl Pts',(0.259878572792024,0.23059679546836,-1.8620315669005));
#75291=CARTESIAN_POINT('Ctrl Pts',(-0.0519195584651473,0.34352842429146,
-1.8461950878755));
#75292=CARTESIAN_POINT('Ctrl Pts',(-0.316414572914817,0.143496108596634,
-1.8303586088505));
#75293=CARTESIAN_POINT('Ctrl Pts',(-0.292639839963886,-0.187273453877836,
-1.81452212982549));
#75294=CARTESIAN_POINT('Ctrl Pts',(-0.00225411854621495,-0.347424467276068,
-1.79868565080049));
#75295=CARTESIAN_POINT('Ctrl Pts',(0.290184992579116,-0.191054477515693,
-1.78284917177548));
#75296=CARTESIAN_POINT('Ctrl Pts',(0.318250179106363,0.13937702099163,-1.76701269275048));
#75297=CARTESIAN_POINT('Ctrl Pts',(0.0563723695500736,0.342828252951786,
-1.75117621372547));
#75298=CARTESIAN_POINT('Ctrl Pts',(-0.256863649886797,0.233944794646829,
-1.73533973470047));
#75299=CARTESIAN_POINT('Ctrl Pts',(-0.336083165442897,-0.0880749773678852,
-1.71950325567546));
#75300=CARTESIAN_POINT('Ctrl Pts',(-0.109112935366136,-0.329853685219295,
-1.70366677665046));
#75301=CARTESIAN_POINT('Ctrl Pts',(0.21726500907928,-0.271118072278702,
-1.68783029762546));
#75302=CARTESIAN_POINT('Ctrl Pts',(0.345702914058587,0.0346206167649245,
-1.67199381860045));
#75303=CARTESIAN_POINT('Ctrl Pts',(0.159186975823379,0.308818065380956,
-1.65615733957545));
#75304=CARTESIAN_POINT('Ctrl Pts',(-0.172356809558471,0.301665745477315,
-1.64032086055044));
#75305=CARTESIAN_POINT('Ctrl Pts',(-0.346874324648551,0.0196797972731843,
-1.62448438152544));
#75306=CARTESIAN_POINT('Ctrl Pts',(-0.20537077995855,-0.280235497640334,
-1.60864790250043));
#75307=CARTESIAN_POINT('Ctrl Pts',(0.123236527810909,-0.324841268555487,
-1.59281142347543));
#75308=CARTESIAN_POINT('Ctrl Pts',(0.339568768462871,-0.0734992719630991,
-1.57697494445043));
#75309=CARTESIAN_POINT('Ctrl Pts',(0.246535701861457,0.244804491769266,
-1.56113846542542));
#75310=CARTESIAN_POINT('Ctrl Pts',(-0.07110457313861,0.340078272139931,
-1.54530198640042));
#75311=CARTESIAN_POINT('Ctrl Pts',(-0.323964779549688,0.125522560147371,
-1.52946550737541));
#75312=CARTESIAN_POINT('Ctrl Pts',(-0.28167574708672,-0.203390916702184,
-1.51362902835041));
#75313=CARTESIAN_POINT('Ctrl Pts',(0.0172349541753397,-0.347004391688523,
-1.4977925493254));
#75314=CARTESIAN_POINT('Ctrl Pts',(0.300443690509177,-0.174478309048545,
-1.4819560703004));
#75315=CARTESIAN_POINT('Ctrl Pts',(0.309932157928084,0.157006843727486,
-1.46611959127539));
#75316=CARTESIAN_POINT('Ctrl Pts',(0.0370558551984614,0.345450365596992,
-1.45028311225039));
#75317=CARTESIAN_POINT('Ctrl Pts',(-0.269580313257183,0.219170130719346,
-1.43444663322538));
#75318=CARTESIAN_POINT('Ctrl Pts',(-0.330614399959186,-0.106785813828543,
-1.41861015420038));
#75319=CARTESIAN_POINT('Ctrl Pts',(-0.0904410879955278,-0.335454171382065,
-1.40277367517538));
#75320=CARTESIAN_POINT('Ctrl Pts',(0.232128891660156,-0.258505839686529,
-1.38693719615037));
#75321=CARTESIAN_POINT('Ctrl Pts',(0.34321703743098,0.0539551361087899,
-1.37110071712537));
#75322=CARTESIAN_POINT('Ctrl Pts',(0.141616107846662,0.317260097544246,
-1.35526423810036));
#75323=CARTESIAN_POINT('Ctrl Pts',(-0.18900466920625,0.291524143963502,
-1.33942775907536));
#75324=CARTESIAN_POINT('Ctrl Pts',(-0.34743208518864,0.000194105363083371,
-1.32359128005036));
#75325=CARTESIAN_POINT('Ctrl Pts',(-0.189330291900079,-0.291312773603304,
-1.30775480102535));
#75326=CARTESIAN_POINT('Ctrl Pts',(0.141261522146442,-0.317418137251619,
-1.29191832200035));
#75327=CARTESIAN_POINT('Ctrl Pts',(0.34315653525949,-0.0543386032588314,
-1.27608184297534));
#75328=CARTESIAN_POINT('Ctrl Pts',(0.2324175937311,0.258246304174259,-1.26024536395034));
#75329=CARTESIAN_POINT('Ctrl Pts',(-0.0900662047077227,0.335555018238388,
-1.24440888492533));
#75330=CARTESIAN_POINT('Ctrl Pts',(-0.330494874177406,0.107155166174472,
-1.22857240590033));
#75331=CARTESIAN_POINT('Ctrl Pts',(-0.269825039360483,-0.218868772623077,
-1.21273592687533));
#75332=CARTESIAN_POINT('Ctrl Pts',(0.0366698357773552,-0.345491555091409,
-1.19689944785032));
#75333=CARTESIAN_POINT('Ctrl Pts',(0.309756529525153,-0.15735305498131,
-1.18106296882532));
#75334=CARTESIAN_POINT('Ctrl Pts',(0.3006384599913,0.17414249300351,-1.16522648980031));
#75335=CARTESIAN_POINT('Ctrl Pts',(0.0176226761291528,0.346984917224748,
-1.14939001077531));
#75336=CARTESIAN_POINT('Ctrl Pts',(-0.281448308096457,0.203705526103394,
-1.1335535317503));
#75337=CARTESIAN_POINT('Ctrl Pts',(-0.324104832603851,-0.125160492881134,
-1.1177170527253));
#75338=CARTESIAN_POINT('Ctrl Pts',(-0.0714845224191077,-0.339998609629407,
-1.10188057370029));
#75339=CARTESIAN_POINT('Ctrl Pts',(0.246262010475165,-0.245079810861989,
-1.08604409467529));
#75340=CARTESIAN_POINT('Ctrl Pts',(0.339650682445754,0.0731198017608916,
-1.07020761565029));
#75341=CARTESIAN_POINT('Ctrl Pts',(0.123599419171098,0.324703364743862,
-1.05437113662528));
#75342=CARTESIAN_POINT('Ctrl Pts',(-0.205057524708256,0.280464798247376,
-1.03853465760028));
#75343=CARTESIAN_POINT('Ctrl Pts',(-0.346896097694429,-0.0192921978995482,
-1.02269817857527));
#75344=CARTESIAN_POINT('Ctrl Pts',(-0.172693774679941,-0.301472970068979,
-1.00686169955027));
#75345=CARTESIAN_POINT('Ctrl Pts',(0.158841812232089,-0.308995744602162,
-0.991025220525266));
#75346=CARTESIAN_POINT('Ctrl Pts',(0.345664013799501,-0.0350068716031159,
-0.975188741500259));
#75347=CARTESIAN_POINT('Ctrl Pts',(0.217567813682816,0.270875133492718,
-0.959352262475257));
#75348=CARTESIAN_POINT('Ctrl Pts',(-0.108744299596982,0.329975406357171,
-0.943515783450251));
#75349=CARTESIAN_POINT('Ctrl Pts',(-0.335984540612977,0.0884504378988902,
-0.927679304425247));
#75350=CARTESIAN_POINT('Ctrl Pts',(-0.257124897648059,-0.233657609559144,
-0.911842825400244));
#75351=CARTESIAN_POINT('Ctrl Pts',(0.0559892773708684,-0.342891079374932,
-0.896006346375238));
#75352=CARTESIAN_POINT('Ctrl Pts',(0.318094226560149,-0.13973243905593,
-0.880169867350236));
#75353=CARTESIAN_POINT('Ctrl Pts',(0.290398324592949,0.190729925730144,
-0.864333388325229));
#75354=CARTESIAN_POINT('Ctrl Pts',(-0.00186598074179355,0.347427128490695,
-0.848496909300226));
#75355=CARTESIAN_POINT('Ctrl Pts',(-0.292430277833504,0.187599637797193,
-0.83266043027522));
#75356=CARTESIAN_POINT('Ctrl Pts',(-0.316574953492537,-0.143141155216159,
-0.816823951250218));
#75357=CARTESIAN_POINT('Ctrl Pts',(-0.0523029170060187,-0.343472701052179,
-0.800987472225212));
#75358=CARTESIAN_POINT('Ctrl Pts',(0.259619873881868,-0.230882248301989,
-0.785150993200208));
#75359=CARTESIAN_POINT('Ctrl Pts',(0.335015075942623,0.0920542795668767,
-0.769314514175204));
#75360=CARTESIAN_POINT('Ctrl Pts',(0.105193628181329,0.331124435953414,
-0.753478035150199));
#75361=CARTESIAN_POINT('Ctrl Pts',(-0.220464840304462,0.268522523608257,
-0.737641556125195));
#75362=CARTESIAN_POINT('Ctrl Pts',(-0.345268049450204,-0.0387177675527577,
-0.721805077100192));
#75363=CARTESIAN_POINT('Ctrl Pts',(-0.155513601609092,-0.310684101958866,
-0.705968598075186));
#75364=CARTESIAN_POINT('Ctrl Pts',(0.175922053716002,-0.299600604992318,
-0.690132119050183));
#75365=CARTESIAN_POINT('Ctrl Pts',(0.347083310302664,-0.0155649351030341,
-0.674295640025177));
#75366=CARTESIAN_POINT('Ctrl Pts',(0.20203311019098,0.282651223032876,-0.658459161000174));
#75367=CARTESIAN_POINT('Ctrl Pts',(-0.127080057451709,0.323357001615068,
-0.642622681975168));
#75368=CARTESIAN_POINT('Ctrl Pts',(-0.34041649688156,0.0694672595277645,
-0.626786202950166));
#75369=CARTESIAN_POINT('Ctrl Pts',(-0.243615303161651,-0.247710870897704,
-0.61094972392516));
#75370=CARTESIAN_POINT('Ctrl Pts',(0.0751324595811616,-0.339211151073608,
-0.595113244900157));
#75371=CARTESIAN_POINT('Ctrl Pts',(0.325430533778499,-0.121671932589311,
-0.579276765875152));
#75372=CARTESIAN_POINT('Ctrl Pts',(0.27924398861926,0.206716923147551,-0.563440286850148));
#75373=CARTESIAN_POINT('Ctrl Pts',(-0.0213487633344698,0.346775607272649,
-0.547603807825143));
#75374=CARTESIAN_POINT('Ctrl Pts',(-0.302491650219096,0.17090316861586,
-0.531767328800139));
#75375=CARTESIAN_POINT('Ctrl Pts',(-0.308048467376976,-0.160671196059666,
-0.515930849775135));
#75376=CARTESIAN_POINT('Ctrl Pts',(-0.0329566572079708,-0.345865508889646,
-0.50009437075013));
#75377=CARTESIAN_POINT('Ctrl Pts',(0.272160430095799,-0.215957847240377,
-0.484257891725126));
#75378=CARTESIAN_POINT('Ctrl Pts',(0.329324811245078,0.110698962060618,
-0.468421412700121));
#75379=CARTESIAN_POINT('Ctrl Pts',(0.0864566779796564,0.336503097036941,
-0.452584933675117));
#75380=CARTESIAN_POINT('Ctrl Pts',(-0.235178112319307,0.255734915450402,
-0.436748454650113));
#75381=CARTESIAN_POINT('Ctrl Pts',(-0.342553065762632,-0.0580214501736126,
-0.420911975625108));
#75382=CARTESIAN_POINT('Ctrl Pts',(-0.13784385733172,-0.318917171683215,
-0.405075496600104));
#75383=CARTESIAN_POINT('Ctrl Pts',(0.192448476206574,-0.289262295377172,
-0.3892390175751));
#75384=CARTESIAN_POINT('Ctrl Pts',(0.347409957121141,0.00392600161055561,
-0.373402538550095));
#75385=CARTESIAN_POINT('Ctrl Pts',(0.185862387110661,0.293537499878561,
-0.357566059525091));
#75386=CARTESIAN_POINT('Ctrl Pts',(-0.145015754062733,0.315720640705355,
-0.341729580500086));
#75387=CARTESIAN_POINT('Ctrl Pts',(-0.343776793759324,0.0502653892743109,
-0.325893101475083));
#75388=CARTESIAN_POINT('Ctrl Pts',(-0.229338779650105,-0.260984310765158,
-0.310056622450078));
#75389=CARTESIAN_POINT('Ctrl Pts',(0.0940391070372089,-0.334463364331755,
-0.294220143425074));
#75390=CARTESIAN_POINT('Ctrl Pts',(0.331742376587111,-0.10322837377315,
-0.27838366440007));
#75391=CARTESIAN_POINT('Ctrl Pts',(0.267210527261116,0.22205312245384,-0.262547185375064));
#75392=CARTESIAN_POINT('Ctrl Pts',(-0.0407642622649248,0.34503247007163,
-0.246710706350061));
#75393=CARTESIAN_POINT('Ctrl Pts',(-0.31160089590667,0.153668555557396,
-0.230874227325056));
#75394=CARTESIAN_POINT('Ctrl Pts',(-0.298551939882619,-0.177695190438021,
-0.215037748300052));
#75395=CARTESIAN_POINT('Ctrl Pts',(-0.0135071750300152,-0.347169956482602,
-0.199201269275047));
#75396=CARTESIAN_POINT('Ctrl Pts',(0.283845209205327,-0.200352719837858,
-0.183364790250043));
#75397=CARTESIAN_POINT('Ctrl Pts',(0.322595874731448,0.128993489966123,
-0.167528311225039));
#75398=CARTESIAN_POINT('Ctrl Pts',(0.0674512351160957,0.340825594047761,
-0.151691832200035));
#75399=CARTESIAN_POINT('Ctrl Pts',(-0.249158052908653,0.242136158985246,
-0.13585535317503));
#75400=CARTESIAN_POINT('Ctrl Pts',(-0.338746263568963,-0.0771308789397851,
-0.120018874150026));
#75401=CARTESIAN_POINT('Ctrl Pts',(-0.119765825135592,-0.326168414764973,
-0.104182395125021));
#75402=CARTESIAN_POINT('Ctrl Pts',(0.208418103123617,-0.277971021936984,
-0.0883459161000174));
#75403=CARTESIAN_POINT('Ctrl Pts',(0.346548858735595,0.0233234950411567,
-0.0725094370750124));
#75404=CARTESIAN_POINT('Ctrl Pts',(0.169289569309017,0.303656447029769,
-0.0566729580500089));
#75405=CARTESIAN_POINT('Ctrl Pts',(-0.162873930760557,0.306774327850024,
-0.0408364790250043));
#75406=CARTESIAN_POINT('Ctrl Pts',(-0.284353669323579,0.123363072257457,
-0.030278826341668));
#75407=CARTESIAN_POINT('Ctrl Pts',(-0.293033728012268,0.0261701021632011,
-0.0249999999999999));
#75408=CARTESIAN_POINT('Ctrl Pts',(0.159774743137963,-0.224059110187414,
-1.97774893273369));
#75409=CARTESIAN_POINT('Ctrl Pts',(0.234090319517209,-0.171065272457665,
-1.97247010639202));
#75410=CARTESIAN_POINT('Ctrl Pts',(0.324598576417804,0.0137411606338018,
-1.96191245370869));
#75411=CARTESIAN_POINT('Ctrl Pts',(0.16490859998889,0.280281136023422,-1.94607597468369));
#75412=CARTESIAN_POINT('Ctrl Pts',(-0.145161932979434,0.290658817836682,
-1.93023949565868));
#75413=CARTESIAN_POINT('Ctrl Pts',(-0.322908575340647,0.0366366581141018,
-1.91440301663368));
#75414=CARTESIAN_POINT('Ctrl Pts',(-0.206506813364393,-0.250973821325134,
-1.89856653760867));
#75415=CARTESIAN_POINT('Ctrl Pts',(0.0980538995746365,-0.309823834786522,
-1.88273005858367));
#75416=CARTESIAN_POINT('Ctrl Pts',(0.313271690044925,-0.0864652725460799,
-1.86689357955866));
#75417=CARTESIAN_POINT('Ctrl Pts',(0.243087755192357,0.215697880601396,
-1.85105710053365));
#75418=CARTESIAN_POINT('Ctrl Pts',(-0.0485650232040169,0.321332969504216,
-1.83522062150865));
#75419=CARTESIAN_POINT('Ctrl Pts',(-0.295970950639192,0.134224790227357,
-1.81938414248365));
#75420=CARTESIAN_POINT('Ctrl Pts',(-0.27373230894877,-0.17517367061545,
-1.80354766345864));
#75421=CARTESIAN_POINT('Ctrl Pts',(-0.00210847940039634,-0.324977288206934,
-1.78771118443364));
#75422=CARTESIAN_POINT('Ctrl Pts',(0.271436069848747,-0.178710401399294,
-1.77187470540864));
#75423=CARTESIAN_POINT('Ctrl Pts',(0.29768795786963,0.130371837871251,-1.75603822638363));
#75424=CARTESIAN_POINT('Ctrl Pts',(0.0527301370850901,0.320678036404567,
-1.74020174735863));
#75425=CARTESIAN_POINT('Ctrl Pts',(-0.240267627187054,0.218829564741168,
-1.72436526833362));
#75426=CARTESIAN_POINT('Ctrl Pts',(-0.314368750635077,-0.0823844317250094,
-1.70852878930862));
#75427=CARTESIAN_POINT('Ctrl Pts',(-0.102063122156012,-0.308541758639157,
-1.69269231028361));
#75428=CARTESIAN_POINT('Ctrl Pts',(0.203227464163412,-0.253601067892011,
-1.67685583125861));
#75429=CARTESIAN_POINT('Ctrl Pts',(0.323366964960251,0.0323837703214412,
-1.6610193522336));
#75430=CARTESIAN_POINT('Ctrl Pts',(0.148901866718088,0.288865255298984,
-1.6451828732086));
#75431=CARTESIAN_POINT('Ctrl Pts',(-0.16122079430233,0.282175048518507,
-1.6293463941836));
#75432=CARTESIAN_POINT('Ctrl Pts',(-0.324462690427972,0.0184082807996913,
-1.61350991515859));
#75433=CARTESIAN_POINT('Ctrl Pts',(-0.192101724070109,-0.262129414190369,
-1.59767343613359));
#75434=CARTESIAN_POINT('Ctrl Pts',(0.115274185868449,-0.303853195431335,
-1.58183695710858));
#75435=CARTESIAN_POINT('Ctrl Pts',(0.317629147998793,-0.068750466180528,
-1.56600047808358));
#75436=CARTESIAN_POINT('Ctrl Pts',(0.230606970387799,0.228987614199426,
-1.55016399905857));
#75437=CARTESIAN_POINT('Ctrl Pts',(-0.0665104894277243,0.318105732519741,
-1.53432752003357));
#75438=CARTESIAN_POINT('Ctrl Pts',(-0.303033336592719,0.117412517101364,
-1.51849104100857));
#75439=CARTESIAN_POINT('Ctrl Pts',(-0.263476608770811,-0.190249780258789,
-1.50265456198356));
#75440=CARTESIAN_POINT('Ctrl Pts',(0.0161213996071919,-0.324584353804954,
-1.48681808295856));
#75441=CARTESIAN_POINT('Ctrl Pts',(0.281031950818167,-0.163205223195956,
-1.47098160393355));
#75442=CARTESIAN_POINT('Ctrl Pts',(0.289907366056511,0.146862593485521,
-1.45514512490855));
#75443=CARTESIAN_POINT('Ctrl Pts',(0.034661667409323,0.323130733715994,
-1.43930864588355));
#75444=CARTESIAN_POINT('Ctrl Pts',(-0.252162663853728,0.205009495432385,
-1.42347216685854));
#75445=CARTESIAN_POINT('Ctrl Pts',(-0.309253323415256,-0.0998863565052127,
-1.40763568783354));
#75446=CARTESIAN_POINT('Ctrl Pts',(-0.0845976673712967,-0.313780396033026,
-1.39179920880853));
#75447=CARTESIAN_POINT('Ctrl Pts',(0.21713098768676,-0.241803714705649,
-1.37596272978353));
#75448=CARTESIAN_POINT('Ctrl Pts',(0.321041701424293,0.0504690816825467,
-1.36012625075852));
#75449=CARTESIAN_POINT('Ctrl Pts',(0.132466256781675,0.296761845717303,
-1.34428977173352));
#75450=CARTESIAN_POINT('Ctrl Pts',(-0.176793031701735,0.272688698337488,
-1.32845329270851));
#75451=CARTESIAN_POINT('Ctrl Pts',(-0.324984413924328,0.000181564168509011,
-1.31261681368351));
#75452=CARTESIAN_POINT('Ctrl Pts',(-0.177097615834361,-0.272490984667515,
-1.29678033465851));
#75453=CARTESIAN_POINT('Ctrl Pts',(0.132134580949525,-0.296909674440862,
-1.2809438556335));
#75454=CARTESIAN_POINT('Ctrl Pts',(0.320985108312774,-0.0508277729270431,
-1.2651073766085));
#75455=CARTESIAN_POINT('Ctrl Pts',(0.217401036646898,0.241560947845756,
-1.24927089758349));
#75456=CARTESIAN_POINT('Ctrl Pts',(-0.0842470053836159,0.313874727149509,
-1.23343441855849));
#75457=CARTESIAN_POINT('Ctrl Pts',(-0.309141520223219,0.100231844906513,
-1.21759793953349));
#75458=CARTESIAN_POINT('Ctrl Pts',(-0.252391578144153,-0.204727608155788,
-1.20176146050848));
#75459=CARTESIAN_POINT('Ctrl Pts',(0.034300588796614,-0.32316926194719,
-1.18592498148348));
#75460=CARTESIAN_POINT('Ctrl Pts',(0.28974308504728,-0.147186435946288,
-1.17008850245847));
#75461=CARTESIAN_POINT('Ctrl Pts',(0.281214136196824,0.162891104307017,
-1.15425202343347));
#75462=CARTESIAN_POINT('Ctrl Pts',(0.0164840707515565,0.324566137591005,
-1.13841554440846));
#75463=CARTESIAN_POINT('Ctrl Pts',(-0.263263864668857,0.190544062670301,
-1.12257906538346));
#75464=CARTESIAN_POINT('Ctrl Pts',(-0.303164340785093,-0.117073843088991,
-1.10674258635845));
#75465=CARTESIAN_POINT('Ctrl Pts',(-0.0668658900930811,-0.318031217023338,
-1.09090610733345));
#75466=CARTESIAN_POINT('Ctrl Pts',(0.230350962268339,-0.22924514485881,
-1.07506962830844));
#75467=CARTESIAN_POINT('Ctrl Pts',(0.31770576949938,0.0683955136400972,
-1.05923314928344));
#75468=CARTESIAN_POINT('Ctrl Pts',(0.115613630729864,0.303724201618416,
-1.04339667025844));
#75469=CARTESIAN_POINT('Ctrl Pts',(-0.191808708317494,0.262343899629591,
-1.02756019123343));
#75470=CARTESIAN_POINT('Ctrl Pts',(-0.324483056712076,-0.018045724315569,
-1.01172371220843));
#75471=CARTESIAN_POINT('Ctrl Pts',(-0.161535988025596,-0.281994728376046,
-0.995887233183423));
#75472=CARTESIAN_POINT('Ctrl Pts',(0.148579004230125,-0.289031454622626,
-0.980050754158418));
#75473=CARTESIAN_POINT('Ctrl Pts',(0.323330578056337,-0.0327450691408802,
-0.964214275133415));
#75474=CARTESIAN_POINT('Ctrl Pts',(0.203510704488092,0.253373825439895,
-0.948377796108409));
#75475=CARTESIAN_POINT('Ctrl Pts',(-0.101718304033287,0.308655615344801,
-0.932541317083407));
#75476=CARTESIAN_POINT('Ctrl Pts',(-0.314276497979333,0.0827356336600666,
-0.9167048380584));
#75477=CARTESIAN_POINT('Ctrl Pts',(-0.240511995667115,-0.218560934751633,
-0.900868359033399));
#75478=CARTESIAN_POINT('Ctrl Pts',(0.0523717965844736,-0.32073680359728,
-0.885031880008391));
#75479=CARTESIAN_POINT('Ctrl Pts',(0.297542081455241,-0.130704292288237,
-0.86919540098339));
#75480=CARTESIAN_POINT('Ctrl Pts',(0.27163561842944,0.178406818983305,-0.853358921958384));
#75481=CARTESIAN_POINT('Ctrl Pts',(-0.00174541927363239,0.324979777479838,
-0.83752244293338));
#75482=CARTESIAN_POINT('Ctrl Pts',(-0.273536286678446,0.175478779712686,
-0.821685963908374));
#75483=CARTESIAN_POINT('Ctrl Pts',(-0.296120968988897,-0.133892770470861,
-0.805849484883371));
#75484=CARTESIAN_POINT('Ctrl Pts',(-0.0489236128566082,-0.321280846556937,
-0.790013005858366));
#75485=CARTESIAN_POINT('Ctrl Pts',(0.242845770881514,-0.21596489025823,
-0.774176526833362));
#75486=CARTESIAN_POINT('Ctrl Pts',(0.313369670656391,0.0861066302440811,
-0.758340047808358));
#75487=CARTESIAN_POINT('Ctrl Pts',(0.0983970423587119,0.309730405860231,
-0.742503568783354));
#75488=CARTESIAN_POINT('Ctrl Pts',(-0.206220553517287,0.251173218250494,
-0.726667089758349));
#75489=CARTESIAN_POINT('Ctrl Pts',(-0.322960197059656,-0.0362162032034551,
-0.710830610733345));
#75490=CARTESIAN_POINT('Ctrl Pts',(-0.145465830102453,-0.290610726801146,
-0.694994131708341));
#75491=CARTESIAN_POINT('Ctrl Pts',(0.164555687170394,-0.28024333726097,
-0.679157652683335));
#75492=CARTESIAN_POINT('Ctrl Pts',(0.3246581734683,-0.0145592808720665,
-0.663321173658333));
#75493=CARTESIAN_POINT('Ctrl Pts',(0.188979701955492,0.264389058979569,
-0.647484694633327));
#75494=CARTESIAN_POINT('Ctrl Pts',(-0.118869384127234,0.302464827337819,
-0.631648215608323));
#75495=CARTESIAN_POINT('Ctrl Pts',(-0.318422104478806,0.0649789630462639,
-0.615811736583319));
#75496=CARTESIAN_POINT('Ctrl Pts',(-0.227875259356083,-0.231706211467678,
-0.599975257558315));
#75497=CARTESIAN_POINT('Ctrl Pts',(0.0702781331505997,-0.31729463635576,
-0.58413877853331));
#75498=CARTESIAN_POINT('Ctrl Pts',(0.304404388085412,-0.113810679523475,
-0.568302299508307));
#75499=CARTESIAN_POINT('Ctrl Pts',(0.261201966807552,0.193360892621279,
-0.552465820483301));
#75500=CARTESIAN_POINT('Ctrl Pts',(-0.0199694145590941,0.324370351205662,
-0.536629341458298));
#75501=CARTESIAN_POINT('Ctrl Pts',(-0.282947591354669,0.159861073453475,
-0.520792862433293));
#75502=CARTESIAN_POINT('Ctrl Pts',(-0.288145381208641,-0.15029019112504,
-0.504956383408289));
#75503=CARTESIAN_POINT('Ctrl Pts',(-0.0308273195949118,-0.323519054499852,
-0.489119904383284));
#75504=CARTESIAN_POINT('Ctrl Pts',(0.254576078717811,-0.202004758367859,
-0.47328342535828));
#75505=CARTESIAN_POINT('Ctrl Pts',(0.308047055340646,0.10354667528121,-0.457446946333275));
#75506=CARTESIAN_POINT('Ctrl Pts',(0.0808706910526324,0.314761550347012,
-0.441610467308271));
#75507=CARTESIAN_POINT('Ctrl Pts',(-0.219983197459793,0.23921182055627,
-0.425773988283267));
#75508=CARTESIAN_POINT('Ctrl Pts',(-0.320420629126427,-0.0542726702097004,
-0.409937509258262));
#75509=CARTESIAN_POINT('Ctrl Pts',(-0.128937732287144,-0.29831185589437,
-0.394101030233258));
#75510=CARTESIAN_POINT('Ctrl Pts',(0.180014333496764,-0.270572988336741,
-0.378264551208253));
#75511=CARTESIAN_POINT('Ctrl Pts',(0.324963715556635,0.00367234169457965,
-0.362428072183249));
#75512=CARTESIAN_POINT('Ctrl Pts',(0.173853773214234,0.274571970838708,
-0.346591593158245));
#75513=CARTESIAN_POINT('Ctrl Pts',(-0.135646251031432,0.295321853558036,
-0.330755114133241));
#75514=CARTESIAN_POINT('Ctrl Pts',(-0.321565291760542,0.0470177302856763,
-0.314918635108236));
#75515=CARTESIAN_POINT('Ctrl Pts',(-0.214521145490182,-0.244122051166946,
-0.299082156083232));
#75516=CARTESIAN_POINT('Ctrl Pts',(0.0879632175303027,-0.312853605266472,
-0.283245677058228));
#75517=CARTESIAN_POINT('Ctrl Pts',(0.310308421199756,-0.0965587635143514,
-0.267409198033223));
#75518=CARTESIAN_POINT('Ctrl Pts',(0.249945990305456,0.20770621637189,-0.251572719008219));
#75519=CARTESIAN_POINT('Ctrl Pts',(-0.0381304733960651,0.322739838521851,
-0.235736239983215));
#75520=CARTESIAN_POINT('Ctrl Pts',(-0.291468286469691,0.143739992923516,
-0.21989976095821));
#75521=CARTESIAN_POINT('Ctrl Pts',(-0.279262426658274,-0.166214261098879,
-0.204063281933206));
#75522=CARTESIAN_POINT('Ctrl Pts',(-0.0126344731763009,-0.324739221417544,
-0.188226802908201));
#75523=CARTESIAN_POINT('Ctrl Pts',(0.265505901415917,-0.187407882030522,
-0.172390323883198));
#75524=CARTESIAN_POINT('Ctrl Pts',(0.301752877046697,0.120659189302949,
-0.156553844858192));
#75525=CARTESIAN_POINT('Ctrl Pts',(0.0630931944606496,0.318804769777907,
-0.140717365833189));
#75526=CARTESIAN_POINT('Ctrl Pts',(-0.233059890698008,0.226491683043557,
-0.124880886808183));
#75527=CARTESIAN_POINT('Ctrl Pts',(-0.316859785345509,-0.0721474341499148,
-0.10904440778318));
#75528=CARTESIAN_POINT('Ctrl Pts',(-0.112027726134506,-0.305094594402439,
-0.0932079287581754));
#75529=CARTESIAN_POINT('Ctrl Pts',(0.194952158946614,-0.260011246811268,
-0.0773714497331713));
#75530=CARTESIAN_POINT('Ctrl Pts',(0.324158252946565,0.021816558371408,
-0.0615349707081665));
#75531=CARTESIAN_POINT('Ctrl Pts',(0.158351729189089,0.284037130360981,
-0.0456984916831627));
#75532=CARTESIAN_POINT('Ctrl Pts',(-0.152350606602819,0.28695356414546,
-0.0298620126581584));
#75533=CARTESIAN_POINT('Ctrl Pts',(-0.265981509802645,0.115392554247619,
-0.0193043599748219));
#75534=CARTESIAN_POINT('Ctrl Pts',(-0.274100747794842,0.0244792455170898,
-0.0140255336331538));
#75535=CARTESIAN_POINT('Ctrl Pts',(0.148738611075532,-0.20858265952159,
-1.96677446636685));
#75536=CARTESIAN_POINT('Ctrl Pts',(0.217920982424313,-0.159249268869985,
-1.96149564002518));
#75537=CARTESIAN_POINT('Ctrl Pts',(0.302177556134698,0.0127920164795567,
-1.95093798734184));
#75538=CARTESIAN_POINT('Ctrl Pts',(0.153517856671363,0.2609212574155,-1.93510150831684));
#75539=CARTESIAN_POINT('Ctrl Pts',(-0.135135152580135,0.270582120883482,
-1.91926502929183));
#75540=CARTESIAN_POINT('Ctrl Pts',(-0.300604288620724,0.034106051653201,
-1.90342855026683));
#75541=CARTESIAN_POINT('Ctrl Pts',(-0.192242753730676,-0.233638288925213,
-1.88759207124182));
#75542=CARTESIAN_POINT('Ctrl Pts',(0.0912810156776652,-0.288423351270546,
-1.87175559221682));
#75543=CARTESIAN_POINT('Ctrl Pts',(0.291633052580356,-0.0804928506983476,
-1.85591911319182));
#75544=CARTESIAN_POINT('Ctrl Pts',(0.22629693759269,0.200798965734433,-1.84008263416681));
#75545=CARTESIAN_POINT('Ctrl Pts',(-0.0452104879428866,0.299137514716973,
-1.82424615514181));
#75546=CARTESIAN_POINT('Ctrl Pts',(-0.275527328363567,0.124953471858079,
-1.8084096761168));
#75547=CARTESIAN_POINT('Ctrl Pts',(-0.254824777933654,-0.163073887353064,
-1.7925731970918));
#75548=CARTESIAN_POINT('Ctrl Pts',(-0.00196284025457797,-0.3025301091378,
-1.7767367180668));
#75549=CARTESIAN_POINT('Ctrl Pts',(0.252687147118379,-0.166366325282896,
-1.76090023904179));
#75550=CARTESIAN_POINT('Ctrl Pts',(0.277125736632896,0.121366654750872,
-1.74506376001679));
#75551=CARTESIAN_POINT('Ctrl Pts',(0.0490879046201066,0.298527819857348,
-1.72922728099178));
#75552=CARTESIAN_POINT('Ctrl Pts',(-0.22367160448731,0.203714334835507,
-1.71339080196678));
#75553=CARTESIAN_POINT('Ctrl Pts',(-0.292654335827258,-0.0766938860821337,
-1.69755432294177));
#75554=CARTESIAN_POINT('Ctrl Pts',(-0.095013308945888,-0.287229832059019,
-1.68171784391677));
#75555=CARTESIAN_POINT('Ctrl Pts',(0.189189919247545,-0.236084063505319,
-1.66588136489176));
#75556=CARTESIAN_POINT('Ctrl Pts',(0.301031015861915,0.0301469238779581,
-1.65004488586676));
#75557=CARTESIAN_POINT('Ctrl Pts',(0.138616757612798,0.268912445217012,
-1.63420840684176));
#75558=CARTESIAN_POINT('Ctrl Pts',(-0.150084779046188,0.262684351559698,
-1.61837192781675));
#75559=CARTESIAN_POINT('Ctrl Pts',(-0.302051056207392,0.0171367643261984,
-1.60253544879175));
#75560=CARTESIAN_POINT('Ctrl Pts',(-0.178832668181669,-0.244023330740404,
-1.58669896976674));
#75561=CARTESIAN_POINT('Ctrl Pts',(0.107311843925988,-0.282865122307182,
-1.57086249074174));
#75562=CARTESIAN_POINT('Ctrl Pts',(0.295689527534716,-0.0640016603979571,
-1.55502601171673));
#75563=CARTESIAN_POINT('Ctrl Pts',(0.214678238914141,0.213170736629585,
-1.53918953269173));
#75564=CARTESIAN_POINT('Ctrl Pts',(-0.0619164057168387,0.29613319289955,
-1.52335305366672));
#75565=CARTESIAN_POINT('Ctrl Pts',(-0.282101893635751,0.109302474055358,
-1.50751657464172));
#75566=CARTESIAN_POINT('Ctrl Pts',(-0.245277470454903,-0.177108643815393,
-1.49168009561672));
#75567=CARTESIAN_POINT('Ctrl Pts',(0.0150078450390444,-0.302164315921385,
-1.47584361659171));
#75568=CARTESIAN_POINT('Ctrl Pts',(0.261620211127157,-0.151932137343368,
-1.46000713756671));
#75569=CARTESIAN_POINT('Ctrl Pts',(0.269882574184939,0.136718343243556,
-1.4441706585417));
#75570=CARTESIAN_POINT('Ctrl Pts',(0.0322674796201843,0.300811101834997,
-1.4283341795167));
#75571=CARTESIAN_POINT('Ctrl Pts',(-0.234745014450272,0.190848860145424,
-1.41249770049169));
#75572=CARTESIAN_POINT('Ctrl Pts',(-0.287892246871325,-0.0929868991818828,
-1.39666122146669));
#75573=CARTESIAN_POINT('Ctrl Pts',(-0.0787542467470654,-0.292106620683986,
-1.38082474244169));
#75574=CARTESIAN_POINT('Ctrl Pts',(0.202133083713364,-0.225101589724768,
-1.36498826341668));
#75575=CARTESIAN_POINT('Ctrl Pts',(0.298866365417606,0.0469830272563036,
-1.34915178439168));
#75576=CARTESIAN_POINT('Ctrl Pts',(0.123316405716688,0.27626359389036,-1.33331530536667));
#75577=CARTESIAN_POINT('Ctrl Pts',(-0.16458139419722,0.253853252711475,
-1.31747882634167));
#75578=CARTESIAN_POINT('Ctrl Pts',(-0.302536742660015,0.000169022973934383,
-1.30164234731666));
#75579=CARTESIAN_POINT('Ctrl Pts',(-0.164864939768642,-0.253669195731725,
-1.28580586829166));
#75580=CARTESIAN_POINT('Ctrl Pts',(0.123007639752607,-0.276401211630105,
-1.26996938926665));
#75581=CARTESIAN_POINT('Ctrl Pts',(0.298813681366057,-0.0473169425952548,
-1.25413291024165));
#75582=CARTESIAN_POINT('Ctrl Pts',(0.202384479562695,0.224875591517254,
-1.23829643121665));
#75583=CARTESIAN_POINT('Ctrl Pts',(-0.0784278060595097,0.29219443606063,
-1.22245995219164));
#75584=CARTESIAN_POINT('Ctrl Pts',(-0.287788166269031,0.0933085236385542,
-1.20662347316664));
#75585=CARTESIAN_POINT('Ctrl Pts',(-0.234958116927824,-0.190586443688498,
-1.19078699414163));
#75586=CARTESIAN_POINT('Ctrl Pts',(0.0319313418158729,-0.300846968802971,
-1.17495051511663));
#75587=CARTESIAN_POINT('Ctrl Pts',(0.269729640569406,-0.137019816911266,
-1.15911403609162));
#75588=CARTESIAN_POINT('Ctrl Pts',(0.261789812402348,0.151639715610526,
-1.14327755706662));
#75589=CARTESIAN_POINT('Ctrl Pts',(0.0153454653739602,0.302147357957263,
-1.12744107804161));
#75590=CARTESIAN_POINT('Ctrl Pts',(-0.245079421241258,0.177382599237209,
-1.11160459901661));
#75591=CARTESIAN_POINT('Ctrl Pts',(-0.282223848966336,-0.108987193296848,
-1.09576811999161));
#75592=CARTESIAN_POINT('Ctrl Pts',(-0.0622472577670544,-0.296063824417269,
-1.0799316409666));
#75593=CARTESIAN_POINT('Ctrl Pts',(0.214439914061512,-0.21341047885563,
-1.0640951619416));
#75594=CARTESIAN_POINT('Ctrl Pts',(0.295760856553006,0.0636712255193022,
-1.04825868291659));
#75595=CARTESIAN_POINT('Ctrl Pts',(0.10762784228863,0.282745038492971,-1.03242220389159));
#75596=CARTESIAN_POINT('Ctrl Pts',(-0.178559891926731,0.244223001011805,
-1.01658572486658));
#75597=CARTESIAN_POINT('Ctrl Pts',(-0.302070015729723,-0.0167992507315895,
-1.00074924584158));
#75598=CARTESIAN_POINT('Ctrl Pts',(-0.150378201371251,-0.262516486683113,
-0.984912766816576));
#75599=CARTESIAN_POINT('Ctrl Pts',(0.138316196228161,-0.269067164643089,
-0.969076287791573));
#75600=CARTESIAN_POINT('Ctrl Pts',(0.300997142313173,-0.0304832666786445,
-0.953239808766568));
#75601=CARTESIAN_POINT('Ctrl Pts',(0.189453595293367,0.235872517387072,
-0.937403329741564));
#75602=CARTESIAN_POINT('Ctrl Pts',(-0.0946923084695934,0.28733582433243,
-0.92156685071656));
#75603=CARTESIAN_POINT('Ctrl Pts',(-0.292568455345688,0.077020829421243,
-0.905730371691556));
#75604=CARTESIAN_POINT('Ctrl Pts',(-0.22389909368617,-0.203464259944122,
-0.88989389266655));
#75605=CARTESIAN_POINT('Ctrl Pts',(0.0487543157980785,-0.298582527819628,
-0.874057413641548));
#75606=CARTESIAN_POINT('Ctrl Pts',(0.276989936350333,-0.121676145520544,
-0.858220934616541));
#75607=CARTESIAN_POINT('Ctrl Pts',(0.25287291226593,0.166083712236466,-0.842384455591539));
#75608=CARTESIAN_POINT('Ctrl Pts',(-0.00162485780547096,0.302532426468981,
-0.826547976566533));
#75609=CARTESIAN_POINT('Ctrl Pts',(-0.254642295523387,0.163357921628179,
-0.810711497541529));
#75610=CARTESIAN_POINT('Ctrl Pts',(-0.275666984485257,-0.124644385725563,
-0.794875018516526));
#75611=CARTESIAN_POINT('Ctrl Pts',(-0.0455443087071976,-0.299088992061696,
-0.77903853949152));
#75612=CARTESIAN_POINT('Ctrl Pts',(0.22607166788116,-0.201047532214471,
-0.763202060466516));
#75613=CARTESIAN_POINT('Ctrl Pts',(0.291724265370159,0.0801589809212851,
-0.747365581441513));
#75614=CARTESIAN_POINT('Ctrl Pts',(0.0916004565360948,0.288336375767049,
-0.731529102416506));
#75615=CARTESIAN_POINT('Ctrl Pts',(-0.191976266730112,0.23382391289273,
-0.715692623391504));
#75616=CARTESIAN_POINT('Ctrl Pts',(-0.300652344669107,-0.0337146388541525,
-0.699856144366498));
#75617=CARTESIAN_POINT('Ctrl Pts',(-0.135418058595813,-0.270537351643426,
-0.684019665341495));
#75618=CARTESIAN_POINT('Ctrl Pts',(0.153189320624786,-0.260886069529622,
-0.668183186316489));
#75619=CARTESIAN_POINT('Ctrl Pts',(0.302233036633937,-0.013553626641099,
-0.652346707291486));
#75620=CARTESIAN_POINT('Ctrl Pts',(0.175926293720004,0.246126894926262,
-0.636510228266482));
#75621=CARTESIAN_POINT('Ctrl Pts',(-0.110658710802758,0.28157265306057,
-0.620673749241477));
#75622=CARTESIAN_POINT('Ctrl Pts',(-0.296427712076052,0.0604906665647636,
-0.604837270216473));
#75623=CARTESIAN_POINT('Ctrl Pts',(-0.212135215550515,-0.215701552037653,
-0.589000791191469));
#75624=CARTESIAN_POINT('Ctrl Pts',(0.0654238067200374,-0.295378121637912,
-0.573164312166464));
#75625=CARTESIAN_POINT('Ctrl Pts',(0.283378242392325,-0.105949426457638,
-0.55732783314146));
#75626=CARTESIAN_POINT('Ctrl Pts',(0.243159944995843,0.180004862095007,
-0.541491354116455));
#75627=CARTESIAN_POINT('Ctrl Pts',(-0.0185900657837185,0.301965095138675,
-0.525654875091452));
#75628=CARTESIAN_POINT('Ctrl Pts',(-0.263403532490242,0.14881897829109,
-0.509818396066446));
#75629=CARTESIAN_POINT('Ctrl Pts',(-0.268242295040306,-0.139909186190414,
-0.493981917041443));
#75630=CARTESIAN_POINT('Ctrl Pts',(-0.0286979819818524,-0.301172600110059,
-0.478145438016438));
#75631=CARTESIAN_POINT('Ctrl Pts',(0.236991727339823,-0.188051669495342,
-0.462308958991434));
#75632=CARTESIAN_POINT('Ctrl Pts',(0.286769299436215,0.0963943885018026,
-0.446472479966429));
#75633=CARTESIAN_POINT('Ctrl Pts',(0.0752847041256083,0.293020003657083,
-0.430636000941425));
#75634=CARTESIAN_POINT('Ctrl Pts',(-0.204788282600279,0.222688725662139,
-0.414799521916421));
#75635=CARTESIAN_POINT('Ctrl Pts',(-0.298288192490222,-0.0505238902457886,
-0.398963042891416));
#75636=CARTESIAN_POINT('Ctrl Pts',(-0.120031607242568,-0.277706540105525,
-0.383126563866412));
#75637=CARTESIAN_POINT('Ctrl Pts',(0.167580190786954,-0.25188368129631,
-0.367290084841407));
#75638=CARTESIAN_POINT('Ctrl Pts',(0.302517473992129,0.00341868177860365,
-0.351453605816403));
#75639=CARTESIAN_POINT('Ctrl Pts',(0.161845159317807,0.255606441798855,
-0.335617126791399));
#75640=CARTESIAN_POINT('Ctrl Pts',(-0.126276748000131,0.274923066410718,
-0.319780647766394));
#75641=CARTESIAN_POINT('Ctrl Pts',(-0.29935378976176,0.0437700712970414,
-0.303944168741391));
#75642=CARTESIAN_POINT('Ctrl Pts',(-0.199703511330258,-0.227259791568734,
-0.288107689716386));
#75643=CARTESIAN_POINT('Ctrl Pts',(0.0818873280233965,-0.291243846201189,
-0.272271210691382));
#75644=CARTESIAN_POINT('Ctrl Pts',(0.288874465812401,-0.0898891532555531,
-0.256434731666377));
#75645=CARTESIAN_POINT('Ctrl Pts',(0.232681453349795,0.19335931028994,-0.240598252641373));
#75646=CARTESIAN_POINT('Ctrl Pts',(-0.035496684527205,0.300447206972072,
-0.224761773616368));
#75647=CARTESIAN_POINT('Ctrl Pts',(-0.271335677032713,0.133811430289637,
-0.208925294591364));
#75648=CARTESIAN_POINT('Ctrl Pts',(-0.259972913433929,-0.154733331759737,
-0.19308881556636));
#75649=CARTESIAN_POINT('Ctrl Pts',(-0.0117617713225866,-0.302308486352486,
-0.177252336541355));
#75650=CARTESIAN_POINT('Ctrl Pts',(0.247166593626507,-0.174463044223185,
-0.161415857516351));
#75651=CARTESIAN_POINT('Ctrl Pts',(0.280909879361946,0.112324888639776,
-0.145579378491347));
#75652=CARTESIAN_POINT('Ctrl Pts',(0.0587351538052031,0.296783945508053,
-0.129742899466343));
#75653=CARTESIAN_POINT('Ctrl Pts',(-0.216961728487364,0.210847207101868,
-0.113906420441338));
#75654=CARTESIAN_POINT('Ctrl Pts',(-0.294973307122055,-0.0671639893600439,
-0.0980699414163342));
#75655=CARTESIAN_POINT('Ctrl Pts',(-0.10428962713342,-0.284020774039906,
-0.0822334623913293));
#75656=CARTESIAN_POINT('Ctrl Pts',(0.181486214769611,-0.242051471685551,
-0.0663969833663252));
#75657=CARTESIAN_POINT('Ctrl Pts',(0.301767647157536,0.0203096217016589,
-0.0505605043413204));
#75658=CARTESIAN_POINT('Ctrl Pts',(0.147413889069162,0.264417813692194,
-0.0347240253163167));
#75659=CARTESIAN_POINT('Ctrl Pts',(-0.141827282445081,0.267132800440896,
-0.0188875462913122));
#75660=CARTESIAN_POINT('Ctrl Pts',(-0.247609350281711,0.107422036237781,
-0.00832989360797585));
#75661=CARTESIAN_POINT('Ctrl Pts',(-0.255167767577417,0.0227883888709785,
-0.00305106726630777));
#75662=CARTESIAN_POINT('Ctrl Pts',(0.137702479013101,-0.193106208855765,
-1.9558));
#75663=CARTESIAN_POINT('Ctrl Pts',(0.201751645331416,-0.147433265282304,
-1.95052117365833));
#75664=CARTESIAN_POINT('Ctrl Pts',(0.279756535851592,0.0118428723253114,
-1.939963520975));
#75665=CARTESIAN_POINT('Ctrl Pts',(0.142127113353835,0.241561378807579,
-1.92412704194999));
#75666=CARTESIAN_POINT('Ctrl Pts',(-0.125108372180837,0.250505423930283,
-1.90829056292499));
#75667=CARTESIAN_POINT('Ctrl Pts',(-0.278300001900802,0.0315754451923003,
-1.89245408389998));
#75668=CARTESIAN_POINT('Ctrl Pts',(-0.177978694096959,-0.216302756525292,
-1.87661760487498));
#75669=CARTESIAN_POINT('Ctrl Pts',(0.0845081317806936,-0.26702286775457,
-1.86078112584997));
#75670=CARTESIAN_POINT('Ctrl Pts',(0.269994415115787,-0.0745204288506152,
-1.84494464682497));
#75671=CARTESIAN_POINT('Ctrl Pts',(0.209506119993022,0.185900050867469,
-1.82910816779996));
#75672=CARTESIAN_POINT('Ctrl Pts',(-0.0418559526817564,0.27694205992973,
-1.81327168877496));
#75673=CARTESIAN_POINT('Ctrl Pts',(-0.255083706087942,0.115682153488801,
-1.79743520974995));
#75674=CARTESIAN_POINT('Ctrl Pts',(-0.235917246918538,-0.150974104090677,
-1.78159873072495));
#75675=CARTESIAN_POINT('Ctrl Pts',(-0.0018172011087593,-0.280082930068666,
-1.76576225169995));
#75676=CARTESIAN_POINT('Ctrl Pts',(0.23393822438801,-0.154022249166496,
-1.74992577267494));
#75677=CARTESIAN_POINT('Ctrl Pts',(0.256563515396163,0.112361471630493,
-1.73408929364994));
#75678=CARTESIAN_POINT('Ctrl Pts',(0.0454456721551229,0.27637760331013,
-1.71825281462493));
#75679=CARTESIAN_POINT('Ctrl Pts',(-0.207075581787567,0.188599104929845,
-1.70241633559993));
#75680=CARTESIAN_POINT('Ctrl Pts',(-0.270939921019438,-0.0710033404392579,
-1.68657985657493));
#75681=CARTESIAN_POINT('Ctrl Pts',(-0.087963495735764,-0.265917905478881,
-1.67074337754992));
#75682=CARTESIAN_POINT('Ctrl Pts',(0.175152374331677,-0.218567059118628,
-1.65490689852492));
#75683=CARTESIAN_POINT('Ctrl Pts',(0.27869506676358,0.0279100774344748,
-1.63907041949991));
#75684=CARTESIAN_POINT('Ctrl Pts',(0.128331648507507,0.248959635135041,
-1.62323394047491));
#75685=CARTESIAN_POINT('Ctrl Pts',(-0.138948763790046,0.243193654600889,
-1.6073974614499));
#75686=CARTESIAN_POINT('Ctrl Pts',(-0.279639421986813,0.0158652478527055,
-1.5915609824249));
#75687=CARTESIAN_POINT('Ctrl Pts',(-0.165563612293228,-0.225917247290439,
-1.5757245033999));
#75688=CARTESIAN_POINT('Ctrl Pts',(0.0993495019835277,-0.261877049183029,
-1.55988802437489));
#75689=CARTESIAN_POINT('Ctrl Pts',(0.273749907070638,-0.059252854615386,
-1.54405154534989));
#75690=CARTESIAN_POINT('Ctrl Pts',(0.198749507440483,0.197353859059745,
-1.52821506632488));
#75691=CARTESIAN_POINT('Ctrl Pts',(-0.057322322005953,0.27416065327936,
-1.51237858729988));
#75692=CARTESIAN_POINT('Ctrl Pts',(-0.261170450678782,0.101192431009352,
-1.49654210827487));
#75693=CARTESIAN_POINT('Ctrl Pts',(-0.227078332138994,-0.163967507371998,
-1.48070562924987));
#75694=CARTESIAN_POINT('Ctrl Pts',(0.0138942904708965,-0.279744278037816,
-1.46486915022487));
#75695=CARTESIAN_POINT('Ctrl Pts',(0.242208471436148,-0.140659051490779,
-1.44903267119986));
#75696=CARTESIAN_POINT('Ctrl Pts',(0.249857782313367,0.12657409300159,-1.43319619217486));
#75697=CARTESIAN_POINT('Ctrl Pts',(0.0298732918310454,0.278491469954,-1.41735971314985));
#75698=CARTESIAN_POINT('Ctrl Pts',(-0.217327365046816,0.176688224858463,
-1.40152323412485));
#75699=CARTESIAN_POINT('Ctrl Pts',(-0.266531170327395,-0.0860874418585526,
-1.38568675509984));
#75700=CARTESIAN_POINT('Ctrl Pts',(-0.0729108261228343,-0.270432845334947,
-1.36985027607484));
#75701=CARTESIAN_POINT('Ctrl Pts',(0.187135179739969,-0.208399464743887,
-1.35401379704983));
#75702=CARTESIAN_POINT('Ctrl Pts',(0.276691029410919,0.0434969728300605,
-1.33817731802483));
#75703=CARTESIAN_POINT('Ctrl Pts',(0.114166554651702,0.255765342063417,
-1.32234083899983));
#75704=CARTESIAN_POINT('Ctrl Pts',(-0.152369756692705,0.235017807085461,
-1.30650435997482));
#75705=CARTESIAN_POINT('Ctrl Pts',(-0.280089071395702,0.000156481779360123,
-1.29066788094982));
#75706=CARTESIAN_POINT('Ctrl Pts',(-0.152632263702923,-0.234847406795936,
-1.27483140192481));
#75707=CARTESIAN_POINT('Ctrl Pts',(0.11388069855569,-0.255892748819348,
-1.25899492289981));
#75708=CARTESIAN_POINT('Ctrl Pts',(0.27664225441934,-0.0438061122634664,
-1.2431584438748));
#75709=CARTESIAN_POINT('Ctrl Pts',(0.187367922478493,0.208190235188752,
-1.2273219648498));
#75710=CARTESIAN_POINT('Ctrl Pts',(-0.0726086067354031,0.270514144971751,
-1.2114854858248));
#75711=CARTESIAN_POINT('Ctrl Pts',(-0.266434812314843,0.086385202370595,
-1.19564900679979));
#75712=CARTESIAN_POINT('Ctrl Pts',(-0.217524655711494,-0.176445279221209,
-1.17981252777479));
#75713=CARTESIAN_POINT('Ctrl Pts',(0.0295620948351317,-0.278524675658752,
-1.16397604874978));
#75714=CARTESIAN_POINT('Ctrl Pts',(0.249716196091533,-0.126853197876244,
-1.14813956972478));
#75715=CARTESIAN_POINT('Ctrl Pts',(0.242365488607872,0.140388326914034,
-1.13230309069977));
#75716=CARTESIAN_POINT('Ctrl Pts',(0.0142068599963639,0.27972857832352,
-1.11646661167477));
#75717=CARTESIAN_POINT('Ctrl Pts',(-0.226894977813658,0.164221135804117,
-1.10063013264977));
#75718=CARTESIAN_POINT('Ctrl Pts',(-0.261283357147579,-0.100900543504706,
-1.08479365362476));
#75719=CARTESIAN_POINT('Ctrl Pts',(-0.0576286254410279,-0.2740964318112,
-1.06895717459976));
#75720=CARTESIAN_POINT('Ctrl Pts',(0.198528865854686,-0.197575812852451,
-1.05312069557475));
#75721=CARTESIAN_POINT('Ctrl Pts',(0.273815943606632,0.0589469373985079,
-1.03728421654975));
#75722=CARTESIAN_POINT('Ctrl Pts',(0.0996420538473957,0.261765875367525,
-1.02144773752474));
#75723=CARTESIAN_POINT('Ctrl Pts',(-0.165311075535969,0.22610210239402,
-1.00561125849974));
#75724=CARTESIAN_POINT('Ctrl Pts',(-0.279656974747369,-0.0155527771476102,
-0.989774779474735));
#75725=CARTESIAN_POINT('Ctrl Pts',(-0.139220414716906,-0.24303824499018,
-0.973938300449731));
#75726=CARTESIAN_POINT('Ctrl Pts',(0.128053388226197,-0.249102874663553,
-0.958101821424727));
#75727=CARTESIAN_POINT('Ctrl Pts',(0.278663706570009,-0.0282214642164085,
-0.942265342399722));
#75728=CARTESIAN_POINT('Ctrl Pts',(0.175396486098643,0.218371209334249,
-0.926428863374717));
#75729=CARTESIAN_POINT('Ctrl Pts',(-0.0876663129058996,0.26601603332006,
-0.910592384349715));
#75730=CARTESIAN_POINT('Ctrl Pts',(-0.270860412712043,0.0713060251824191,
-0.894755905324708));
#75731=CARTESIAN_POINT('Ctrl Pts',(-0.207286191705226,-0.188367585136611,
-0.878919426299706));
#75732=CARTESIAN_POINT('Ctrl Pts',(0.0451368350116836,-0.276428252041976,
-0.8630829472747));
#75733=CARTESIAN_POINT('Ctrl Pts',(0.256437791245425,-0.112647998752851,
-0.847246468249696));
#75734=CARTESIAN_POINT('Ctrl Pts',(0.23411020610242,0.153760605489627,-0.831409989224693));
#75735=CARTESIAN_POINT('Ctrl Pts',(-0.00150429633730956,0.280085075458125,
-0.815573510199687));
#75736=CARTESIAN_POINT('Ctrl Pts',(-0.235748304368328,0.151237063543671,
-0.799737031174683));
#75737=CARTESIAN_POINT('Ctrl Pts',(-0.255212999981617,-0.115396000980265,
-0.78390055214968));
#75738=CARTESIAN_POINT('Ctrl Pts',(-0.0421650045577871,-0.276897137566454,
-0.768064073124674));
#75739=CARTESIAN_POINT('Ctrl Pts',(0.209297564880806,-0.186130174170711,
-0.752227594099669));
#75740=CARTESIAN_POINT('Ctrl Pts',(0.270078860083927,0.0742113315984893,
-0.736391115074667));
#75741=CARTESIAN_POINT('Ctrl Pts',(0.0848038707134778,0.266942345673866,
-0.720554636049661));
#75742=CARTESIAN_POINT('Ctrl Pts',(-0.177731979942937,0.216474607534967,
-0.704718157024658));
#75743=CARTESIAN_POINT('Ctrl Pts',(-0.278344492278559,-0.0312130745048499,
-0.688881677999652));
#75744=CARTESIAN_POINT('Ctrl Pts',(-0.125370287089174,-0.250463976485706,
-0.673045198974649));
#75745=CARTESIAN_POINT('Ctrl Pts',(0.141822954079178,-0.241528801798274,
-0.657208719949644));
#75746=CARTESIAN_POINT('Ctrl Pts',(0.279807899799573,-0.0125479724101313,
-0.64137224092464));
#75747=CARTESIAN_POINT('Ctrl Pts',(0.162872885484516,0.227864730872955,
-0.625535761899635));
#75748=CARTESIAN_POINT('Ctrl Pts',(-0.102448037478282,0.260680478783321,
-0.609699282874631));
#75749=CARTESIAN_POINT('Ctrl Pts',(-0.274433319673298,0.0560023700832632,
-0.593862803849627));
#75750=CARTESIAN_POINT('Ctrl Pts',(-0.196395171744947,-0.199696892607627,
-0.578026324824622));
#75751=CARTESIAN_POINT('Ctrl Pts',(0.0605694802894751,-0.273461606920063,
-0.562189845799617));
#75752=CARTESIAN_POINT('Ctrl Pts',(0.262352096699239,-0.0980881733918026,
-0.546353366774615));
#75753=CARTESIAN_POINT('Ctrl Pts',(0.225117923184134,0.166648831568735,
-0.530516887749609));
#75754=CARTESIAN_POINT('Ctrl Pts',(-0.0172107170083428,0.279559839071688,
-0.514680408724605));
#75755=CARTESIAN_POINT('Ctrl Pts',(-0.243859473625816,0.137776883128706,
-0.498843929699601));
#75756=CARTESIAN_POINT('Ctrl Pts',(-0.24833920887197,-0.129528181255788,
-0.483007450674596));
#75757=CARTESIAN_POINT('Ctrl Pts',(-0.0265686443687933,-0.278826145720265,
-0.467170971649592));
#75758=CARTESIAN_POINT('Ctrl Pts',(0.219407375961836,-0.174098580622825,
-0.451334492624588));
#75759=CARTESIAN_POINT('Ctrl Pts',(0.265491543531784,0.0892421017223949,
-0.435498013599583));
#75760=CARTESIAN_POINT('Ctrl Pts',(0.0696987171985843,0.271278456967154,
-0.419661534574579));
#75761=CARTESIAN_POINT('Ctrl Pts',(-0.189593367740764,0.206165630768008,
-0.403825055549574));
#75762=CARTESIAN_POINT('Ctrl Pts',(-0.276155755854017,-0.0467751102818765,
-0.38798857652457));
#75763=CARTESIAN_POINT('Ctrl Pts',(-0.111125482197992,-0.25710122431668,
-0.372152097499565));
#75764=CARTESIAN_POINT('Ctrl Pts',(0.155146048077143,-0.23319437425588,
-0.356315618474562));
#75765=CARTESIAN_POINT('Ctrl Pts',(0.280071232427623,0.00316502186262762,
-0.340479139449557));
#75766=CARTESIAN_POINT('Ctrl Pts',(0.149836545421379,0.236640912759002,
-0.324642660424553));
#75767=CARTESIAN_POINT('Ctrl Pts',(-0.116907244968831,0.254524279263399,
-0.308806181399548));
#75768=CARTESIAN_POINT('Ctrl Pts',(-0.277142287762978,0.0405224123084065,
-0.292969702374544));
#75769=CARTESIAN_POINT('Ctrl Pts',(-0.184885877170335,-0.210397531970522,
-0.277133223349539));
#75770=CARTESIAN_POINT('Ctrl Pts',(0.0758114385164903,-0.269634087135906,
-0.261296744324535));
#75771=CARTESIAN_POINT('Ctrl Pts',(0.267440510425046,-0.0832195429967548,
-0.245460265299531));
#75772=CARTESIAN_POINT('Ctrl Pts',(0.215416916394134,0.17901240420799,-0.229623786274526));
#75773=CARTESIAN_POINT('Ctrl Pts',(-0.0328628956583448,0.278154575422294,
-0.213787307249523));
#75774=CARTESIAN_POINT('Ctrl Pts',(-0.251203067595735,0.123882867655757,
-0.197950828224518));
#75775=CARTESIAN_POINT('Ctrl Pts',(-0.240683400209584,-0.143252402420595,
-0.182114349199514));
#75776=CARTESIAN_POINT('Ctrl Pts',(-0.0108890694688725,-0.279877751287428,
-0.166277870174509));
#75777=CARTESIAN_POINT('Ctrl Pts',(0.228827285837098,-0.161518206415849,
-0.150441391149505));
#75778=CARTESIAN_POINT('Ctrl Pts',(0.260066881677195,0.103990587976603,
-0.134604912124501));
#75779=CARTESIAN_POINT('Ctrl Pts',(0.054377113149757,0.274763121238199,
-0.118768433099496));
#75780=CARTESIAN_POINT('Ctrl Pts',(-0.200863566276719,0.195202731160179,
-0.102931954074492));
#75781=CARTESIAN_POINT('Ctrl Pts',(-0.273086828898601,-0.0621805445701736,
-0.0870954750494882));
#75782=CARTESIAN_POINT('Ctrl Pts',(-0.0965515281323339,-0.262946953677372,
-0.0712589960244833));
#75783=CARTESIAN_POINT('Ctrl Pts',(0.168020270592608,-0.224091696559834,
-0.0554225169994791));
#75784=CARTESIAN_POINT('Ctrl Pts',(0.279377041368506,0.0188026850319098,
-0.0395860379744744));
#75785=CARTESIAN_POINT('Ctrl Pts',(0.136476048949234,0.244798497023407,
-0.0237495589494706));
#75786=CARTESIAN_POINT('Ctrl Pts',(-0.131303958287343,0.247312036736331,
-0.00791307992446619));
#75787=CARTESIAN_POINT('Ctrl Pts',(-0.229237190760777,0.0994515182279436,
0.00264457275887023));
#75788=CARTESIAN_POINT('Ctrl Pts',(-0.236234787359992,0.0210975322248671,
0.0079233991005383));
#75789=CARTESIAN_POINT('Origin',(0.,0.,-0.025));
#75790=CARTESIAN_POINT('',(-0.3192,3.90907258287835E-17,0.));
#75791=CARTESIAN_POINT('Origin',(-0.3192,-3.90907258287835E-17,-0.025));
#75792=CARTESIAN_POINT('Origin',(0.,0.,0.));
#75793=CARTESIAN_POINT('Origin',(0.,0.,-0.025));
#75794=CARTESIAN_POINT('Origin',(0.,0.,-0.975));
#75795=CARTESIAN_POINT('Origin',(0.47,0.,0.));
#75796=CARTESIAN_POINT('',(-0.47,-5.75583995599256E-17,1.21430643318376E-17));
#75797=CARTESIAN_POINT('Origin',(0.,0.,0.));
#75798=CARTESIAN_POINT('Origin',(0.,0.,0.24));
#75799=CARTESIAN_POINT('',(0.144337567297406,0.25,0.24));
#75800=CARTESIAN_POINT('',(0.288675134594813,0.,0.24));
#75801=CARTESIAN_POINT('',(0.288675134594813,0.,0.24));
#75802=CARTESIAN_POINT('Origin',(0.,0.,0.24));
#75803=CARTESIAN_POINT('Origin',(0.,0.,0.24));
#75804=CARTESIAN_POINT('',(0.144337567297406,-0.25,0.24));
#75805=CARTESIAN_POINT('',(0.144337567297406,-0.25,0.24));
#75806=CARTESIAN_POINT('Origin',(0.,0.,0.24));
#75807=CARTESIAN_POINT('Origin',(0.,0.,0.24));
#75808=CARTESIAN_POINT('',(-0.144337567297407,-0.25,0.24));
#75809=CARTESIAN_POINT('',(-0.144337567297407,-0.25,0.24));
#75810=CARTESIAN_POINT('Origin',(0.,0.,0.24));
#75811=CARTESIAN_POINT('Origin',(0.,0.,0.24));
#75812=CARTESIAN_POINT('',(-0.288675134594813,5.55111512312578E-17,0.24));
#75813=CARTESIAN_POINT('',(-0.288675134594813,3.53525079574969E-17,0.24));
#75814=CARTESIAN_POINT('Origin',(0.,0.,0.24));
#75815=CARTESIAN_POINT('Origin',(0.,0.,0.24));
#75816=CARTESIAN_POINT('',(-0.144337567297406,0.25,0.24));
#75817=CARTESIAN_POINT('',(-0.144337567297406,0.25,0.24));
#75818=CARTESIAN_POINT('Origin',(0.,0.,0.24));
#75819=CARTESIAN_POINT('Origin',(0.,0.,0.24));
#75820=CARTESIAN_POINT('',(0.144337567297406,0.25,0.24));
#75821=CARTESIAN_POINT('Origin',(0.,0.,0.24));
#75822=CARTESIAN_POINT('Origin',(0.,0.,0.153397459621556));
#75823=CARTESIAN_POINT('',(0.,0.,0.0667949192431123));
#75824=CARTESIAN_POINT('',(-0.144337567297406,-1.76762539787485E-17,0.153397459621556));
#75825=CARTESIAN_POINT('Origin',(0.144337567297406,0.25,0.6));
#75826=CARTESIAN_POINT('',(0.144337567297406,0.25,0.6));
#75827=CARTESIAN_POINT('',(0.288675134594813,0.,0.6));
#75828=CARTESIAN_POINT('',(0.180421959121758,0.1875,0.6));
#75829=CARTESIAN_POINT('',(0.144337567297406,0.25,0.6));
#75830=CARTESIAN_POINT('',(0.288675134594813,0.,0.6));
#75831=CARTESIAN_POINT('Origin',(-0.144337567297406,0.25,0.6));
#75832=CARTESIAN_POINT('',(-0.144337567297406,0.25,0.6));
#75833=CARTESIAN_POINT('',(-0.0721687836487032,0.25,0.6));
#75834=CARTESIAN_POINT('',(-0.144337567297406,0.25,0.6));
#75835=CARTESIAN_POINT('Origin',(-0.288675134594813,5.55111512312578E-17,
0.6));
#75836=CARTESIAN_POINT('',(-0.288675134594813,3.53525079574969E-17,0.6));
#75837=CARTESIAN_POINT('',(-0.252590742770461,0.0625000000000001,0.6));
#75838=CARTESIAN_POINT('',(-0.288675134594813,3.53525079574969E-17,0.6));
#75839=CARTESIAN_POINT('Origin',(-0.144337567297407,-0.25,0.6));
#75840=CARTESIAN_POINT('',(-0.144337567297407,-0.25,0.6));
#75841=CARTESIAN_POINT('',(-0.180421959121758,-0.1875,0.6));
#75842=CARTESIAN_POINT('',(-0.144337567297407,-0.25,0.6));
#75843=CARTESIAN_POINT('Origin',(0.144337567297406,-0.25,0.6));
#75844=CARTESIAN_POINT('',(0.144337567297406,-0.25,0.6));
#75845=CARTESIAN_POINT('',(0.0721687836487032,-0.25,0.6));
#75846=CARTESIAN_POINT('',(0.144337567297406,-0.25,0.6));
#75847=CARTESIAN_POINT('Origin',(0.288675134594813,0.,0.6));
#75848=CARTESIAN_POINT('',(0.252590742770461,-0.0625,0.6));
#75849=CARTESIAN_POINT('Origin',(0.497072620864318,-0.210994809384208,0.55));
#75850=CARTESIAN_POINT('',(0.466514061501753,-0.179901724341759,0.05));
#75851=CARTESIAN_POINT('',(0.466514061501753,-0.179901724341759,0.55));
#75852=CARTESIAN_POINT('',(0.466514061501753,-0.179901724341759,0.29));
#75853=CARTESIAN_POINT('',(0.451052457977236,-0.164169668796321,0.05));
#75854=CARTESIAN_POINT('',(0.497072620864318,-0.210994809384208,0.05));
#75855=CARTESIAN_POINT('',(0.451052457977236,-0.164169668796321,0.55));
#75856=CARTESIAN_POINT('',(0.451052457977236,-0.164169668796321,0.55));
#75857=CARTESIAN_POINT('',(0.497072620864318,-0.210994809384208,0.55));
#75858=CARTESIAN_POINT('Origin',(0.483728513098638,-0.184437764967243,0.55));
#75859=CARTESIAN_POINT('',(0.473009103818409,-0.162056742238344,0.55));
#75860=CARTESIAN_POINT('Origin',(0.,0.,0.55));
#75861=CARTESIAN_POINT('',(0.451052457977236,-0.164169668796321,0.55));
#75862=CARTESIAN_POINT('Origin',(0.451052457977236,-0.164169668796321,0.55));
#75863=CARTESIAN_POINT('',(0.473009103818409,-0.162056742238344,0.05));
#75864=CARTESIAN_POINT('',(0.473009103818409,-0.162056742238344,0.29));
#75865=CARTESIAN_POINT('',(0.451052457977236,-0.164169668796321,0.05));
#75866=CARTESIAN_POINT('Origin',(0.483728513098638,-0.184437764967243,0.05));
#75867=CARTESIAN_POINT('Origin',(0.,0.,0.05));
#75868=CARTESIAN_POINT('Origin',(0.394930998874352,-0.368279114433749,0.55));
#75869=CARTESIAN_POINT('',(0.376849807542158,-0.328609529008881,0.05));
#75870=CARTESIAN_POINT('',(0.376849807542158,-0.328609529008881,0.55));
#75871=CARTESIAN_POINT('',(0.376849807542158,-0.328609529008881,0.29));
#75872=CARTESIAN_POINT('',(0.367701332697109,-0.308538052649539,0.05));
#75873=CARTESIAN_POINT('',(0.394930998874352,-0.368279114433749,0.05));
#75874=CARTESIAN_POINT('',(0.367701332697109,-0.308538052649539,0.55));
#75875=CARTESIAN_POINT('',(0.367701332697109,-0.308538052649539,0.55));
#75876=CARTESIAN_POINT('',(0.394930998874352,-0.368279114433749,0.55));
#75877=CARTESIAN_POINT('Origin',(0.399482254061324,-0.338408583541644,0.55));
#75878=CARTESIAN_POINT('',(0.389056494215466,-0.314062166312295,0.55));
#75879=CARTESIAN_POINT('Origin',(0.,0.,0.55));
#75880=CARTESIAN_POINT('',(0.367701332697109,-0.308538052649539,0.55));
#75881=CARTESIAN_POINT('Origin',(0.367701332697109,-0.308538052649539,0.55));
#75882=CARTESIAN_POINT('',(0.389056494215466,-0.314062166312295,0.05));
#75883=CARTESIAN_POINT('',(0.389056494215466,-0.314062166312295,0.29));
#75884=CARTESIAN_POINT('',(0.367701332697109,-0.308538052649539,0.05));
#75885=CARTESIAN_POINT('Origin',(0.399482254061324,-0.338408583541644,0.05));
#75886=CARTESIAN_POINT('Origin',(0.,0.,0.05));
#75887=CARTESIAN_POINT('Origin',(0.245154869859355,-0.481143523061719,0.55));
#75888=CARTESIAN_POINT('',(0.241731905082157,-0.437682174717398,0.05));
#75889=CARTESIAN_POINT('',(0.241731905082157,-0.437682174717398,0.55));
#75890=CARTESIAN_POINT('',(0.241731905082157,-0.437682174717398,0.29));
#75891=CARTESIAN_POINT('',(0.24,-0.41569219381653,0.05));
#75892=CARTESIAN_POINT('',(0.245154869859355,-0.481143523061719,0.05));
#75893=CARTESIAN_POINT('',(0.24,-0.41569219381653,0.55));
#75894=CARTESIAN_POINT('',(0.24,-0.41569219381653,0.55));
#75895=CARTESIAN_POINT('',(0.245154869859355,-0.481143523061719,0.55));
#75896=CARTESIAN_POINT('Origin',(0.267052539454057,-0.448417858439125,0.55));
#75897=CARTESIAN_POINT('',(0.258177929547807,-0.428187058065056,0.55));
#75898=CARTESIAN_POINT('Origin',(0.,0.,0.55));
#75899=CARTESIAN_POINT('',(0.24,-0.41569219381653,0.55));
#75900=CARTESIAN_POINT('Origin',(0.24,-0.41569219381653,0.55));
#75901=CARTESIAN_POINT('',(0.258177929547807,-0.428187058065056,0.05));
#75902=CARTESIAN_POINT('',(0.258177929547807,-0.428187058065056,0.29));
#75903=CARTESIAN_POINT('',(0.24,-0.41569219381653,0.05));
#75904=CARTESIAN_POINT('Origin',(0.267052539454057,-0.448417858439125,0.05));
#75905=CARTESIAN_POINT('Origin',(0.,0.,0.05));
#75906=CARTESIAN_POINT('Origin',(0.0658094454387798,-0.535974921886314,
0.55));
#75907=CARTESIAN_POINT('',(0.0774575672862877,-0.493963890654054,0.05));
#75908=CARTESIAN_POINT('',(0.0774575672862877,-0.493963890654054,0.55));
#75909=CARTESIAN_POINT('',(0.0774575672862877,-0.493963890654054,0.29));
#75910=CARTESIAN_POINT('',(0.0833511252801264,-0.47270772144586,0.05));
#75911=CARTESIAN_POINT('',(0.0658094454387798,-0.535974921886314,0.05));
#75912=CARTESIAN_POINT('',(0.0833511252801264,-0.47270772144586,0.55));
#75913=CARTESIAN_POINT('',(0.0833511252801264,-0.47270772144586,0.55));
#75914=CARTESIAN_POINT('',(0.0658094454387798,-0.535974921886314,0.55));
#75915=CARTESIAN_POINT('Origin',(0.0936415073922334,-0.504341321666087,
0.55));
#75916=CARTESIAN_POINT('',(0.0961592962762517,-0.490666271247226,0.55));
#75917=CARTESIAN_POINT('Origin',(0.,0.,0.55));
#75918=CARTESIAN_POINT('',(0.0833511252801264,-0.47270772144586,0.55));
#75919=CARTESIAN_POINT('Origin',(0.0833511252801264,-0.47270772144586,0.55));
#75920=CARTESIAN_POINT('',(0.0961592962762517,-0.490666271247226,0.05));
#75921=CARTESIAN_POINT('',(0.0961592962762517,-0.490666271247226,0.29));
#75922=CARTESIAN_POINT('',(0.0833511252801264,-0.47270772144586,0.05));
#75923=CARTESIAN_POINT('Origin',(0.0936415073922334,-0.504341321666087,
0.05));
#75924=CARTESIAN_POINT('Origin',(0.,0.,0.05));
#75925=CARTESIAN_POINT('Origin',(-0.121473569345687,-0.526159834984027,
0.55));
#75926=CARTESIAN_POINT('',(-0.0961592962762519,-0.490666271247226,0.05));
#75927=CARTESIAN_POINT('',(-0.0961592962762519,-0.490666271247226,0.55));
#75928=CARTESIAN_POINT('',(-0.0961592962762519,-0.490666271247226,0.29));
#75929=CARTESIAN_POINT('',(-0.0833511252801266,-0.47270772144586,0.05));
#75930=CARTESIAN_POINT('',(-0.121473569345687,-0.526159834984027,0.05));
#75931=CARTESIAN_POINT('',(-0.0833511252801266,-0.47270772144586,0.55));
#75932=CARTESIAN_POINT('',(-0.0833511252801266,-0.47270772144586,0.55));
#75933=CARTESIAN_POINT('',(-0.121473569345687,-0.526159834984027,0.55));
#75934=CARTESIAN_POINT('Origin',(-0.0936415073922334,-0.504341321666087,
0.55));
#75935=CARTESIAN_POINT('',(-0.0774575672862877,-0.493963890654054,0.55));
#75936=CARTESIAN_POINT('Origin',(0.,0.,0.55));
#75937=CARTESIAN_POINT('',(-0.0833511252801266,-0.47270772144586,0.55));
#75938=CARTESIAN_POINT('Origin',(-0.0833511252801266,-0.47270772144586,
0.55));
#75939=CARTESIAN_POINT('',(-0.0774575672862877,-0.493963890654054,0.05));
#75940=CARTESIAN_POINT('',(-0.0774575672862877,-0.493963890654054,0.29));
#75941=CARTESIAN_POINT('',(-0.0833511252801266,-0.47270772144586,0.05));
#75942=CARTESIAN_POINT('Origin',(-0.0936415073922334,-0.504341321666087,
0.05));
#75943=CARTESIAN_POINT('Origin',(0.,0.,0.05));
#75944=CARTESIAN_POINT('Origin',(-0.294105078908115,-0.452882106690529,
0.55));
#75945=CARTESIAN_POINT('',(-0.258177929547807,-0.428187058065056,0.05));
#75946=CARTESIAN_POINT('',(-0.258177929547807,-0.428187058065056,0.55));
#75947=CARTESIAN_POINT('',(-0.258177929547807,-0.428187058065056,0.29));
#75948=CARTESIAN_POINT('',(-0.24,-0.41569219381653,0.05));
#75949=CARTESIAN_POINT('',(-0.294105078908115,-0.452882106690529,0.05));
#75950=CARTESIAN_POINT('',(-0.24,-0.41569219381653,0.55));
#75951=CARTESIAN_POINT('',(-0.24,-0.41569219381653,0.55));
#75952=CARTESIAN_POINT('',(-0.294105078908115,-0.452882106690529,0.55));
#75953=CARTESIAN_POINT('Origin',(-0.267052539454057,-0.448417858439125,
0.55));
#75954=CARTESIAN_POINT('',(-0.241731905082157,-0.437682174717398,0.55));
#75955=CARTESIAN_POINT('Origin',(0.,0.,0.55));
#75956=CARTESIAN_POINT('',(-0.24,-0.41569219381653,0.55));
#75957=CARTESIAN_POINT('Origin',(-0.24,-0.41569219381653,0.55));
#75958=CARTESIAN_POINT('',(-0.241731905082157,-0.437682174717398,0.05));
#75959=CARTESIAN_POINT('',(-0.241731905082157,-0.437682174717398,0.29));
#75960=CARTESIAN_POINT('',(-0.24,-0.41569219381653,0.05));
#75961=CARTESIAN_POINT('Origin',(-0.267052539454057,-0.448417858439125,
0.05));
#75962=CARTESIAN_POINT('Origin',(0.,0.,0.05));
#75963=CARTESIAN_POINT('Origin',(-0.431263175425538,-0.324980112502106,
0.55));
#75964=CARTESIAN_POINT('',(-0.389056494215466,-0.314062166312295,0.05));
#75965=CARTESIAN_POINT('',(-0.389056494215466,-0.314062166312295,0.55));
#75966=CARTESIAN_POINT('',(-0.389056494215466,-0.314062166312295,0.29));
#75967=CARTESIAN_POINT('',(-0.367701332697109,-0.308538052649539,0.05));
#75968=CARTESIAN_POINT('',(-0.431263175425538,-0.324980112502106,0.05));
#75969=CARTESIAN_POINT('',(-0.367701332697109,-0.308538052649539,0.55));
#75970=CARTESIAN_POINT('',(-0.367701332697109,-0.308538052649539,0.55));
#75971=CARTESIAN_POINT('',(-0.431263175425538,-0.324980112502106,0.55));
#75972=CARTESIAN_POINT('Origin',(-0.399482254061324,-0.338408583541644,
0.55));
#75973=CARTESIAN_POINT('',(-0.376849807542158,-0.328609529008881,0.55));
#75974=CARTESIAN_POINT('Origin',(0.,0.,0.55));
#75975=CARTESIAN_POINT('',(-0.367701332697109,-0.308538052649539,0.55));
#75976=CARTESIAN_POINT('Origin',(-0.367701332697109,-0.308538052649539,
0.55));
#75977=CARTESIAN_POINT('',(-0.376849807542158,-0.328609529008881,0.05));
#75978=CARTESIAN_POINT('',(-0.376849807542158,-0.328609529008881,0.29));
#75979=CARTESIAN_POINT('',(-0.367701332697109,-0.308538052649539,0.05));
#75980=CARTESIAN_POINT('Origin',(-0.399482254061324,-0.338408583541644,
0.05));
#75981=CARTESIAN_POINT('Origin',(0.,0.,0.05));
#75982=CARTESIAN_POINT('Origin',(-0.516404568220039,-0.157880720550278,
0.55));
#75983=CARTESIAN_POINT('',(-0.473009103818409,-0.162056742238344,0.05));
#75984=CARTESIAN_POINT('',(-0.473009103818409,-0.162056742238344,0.55));
#75985=CARTESIAN_POINT('',(-0.473009103818409,-0.162056742238344,0.29));
#75986=CARTESIAN_POINT('',(-0.451052457977236,-0.164169668796321,0.05));
#75987=CARTESIAN_POINT('',(-0.516404568220039,-0.157880720550278,0.05));
#75988=CARTESIAN_POINT('',(-0.451052457977236,-0.164169668796321,0.55));
#75989=CARTESIAN_POINT('',(-0.451052457977236,-0.164169668796321,0.55));
#75990=CARTESIAN_POINT('',(-0.516404568220039,-0.157880720550278,0.55));
#75991=CARTESIAN_POINT('Origin',(-0.483728513098638,-0.184437764967243,
0.55));
#75992=CARTESIAN_POINT('',(-0.466514061501753,-0.179901724341759,0.55));
#75993=CARTESIAN_POINT('Origin',(0.,0.,0.55));
#75994=CARTESIAN_POINT('',(-0.451052457977236,-0.164169668796321,0.55));
#75995=CARTESIAN_POINT('Origin',(-0.451052457977236,-0.164169668796321,
0.55));
#75996=CARTESIAN_POINT('',(-0.466514061501753,-0.179901724341759,0.05));
#75997=CARTESIAN_POINT('',(-0.466514061501753,-0.179901724341759,0.29));
#75998=CARTESIAN_POINT('',(-0.451052457977236,-0.164169668796321,0.05));
#75999=CARTESIAN_POINT('Origin',(-0.483728513098638,-0.184437764967243,
0.05));
#76000=CARTESIAN_POINT('Origin',(0.,0.,0.05));
#76001=CARTESIAN_POINT('Origin',(-0.53925994876747,0.0282614163711897,0.55));
#76002=CARTESIAN_POINT('',(-0.499909834629965,0.00949511665234234,0.05));
#76003=CARTESIAN_POINT('',(-0.499909834629965,0.00949511665234234,0.55));
#76004=CARTESIAN_POINT('',(-0.499909834629965,0.00949511665234234,0.29));
#76005=CARTESIAN_POINT('',(-0.48,5.87830463590729E-17,0.05));
#76006=CARTESIAN_POINT('',(-0.53925994876747,0.0282614163711897,0.05));
#76007=CARTESIAN_POINT('',(-0.48,5.87830463590729E-17,0.55));
#76008=CARTESIAN_POINT('',(-0.48,5.87830463590729E-17,0.55));
#76009=CARTESIAN_POINT('',(-0.53925994876747,0.0282614163711897,0.55));
#76010=CARTESIAN_POINT('Origin',(-0.509629974383735,6.59194920871187E-17,
0.55));
#76011=CARTESIAN_POINT('',(-0.5,-6.12323399573677E-17,0.55));
#76012=CARTESIAN_POINT('Origin',(0.,0.,0.55));
#76013=CARTESIAN_POINT('',(-0.499909834629965,-0.00949511665234226,0.55));
#76014=CARTESIAN_POINT('',(-0.48,5.87830463590729E-17,0.55));
#76015=CARTESIAN_POINT('Origin',(0.,0.,0.55));
#76016=CARTESIAN_POINT('Origin',(-0.48,5.87830463590729E-17,0.55));
#76017=CARTESIAN_POINT('',(-0.499909834629965,-0.00949511665234226,0.05));
#76018=CARTESIAN_POINT('',(-0.499909834629965,-0.00949511665234226,0.29));
#76019=CARTESIAN_POINT('',(-0.48,5.87830463590729E-17,0.05));
#76020=CARTESIAN_POINT('Origin',(-0.509629974383735,6.59194920871187E-17,
0.05));
#76021=CARTESIAN_POINT('',(-0.5,-6.12323399573677E-17,0.05));
#76022=CARTESIAN_POINT('Origin',(0.,0.,0.05));
#76023=CARTESIAN_POINT('Origin',(0.,0.,0.05));
#76024=CARTESIAN_POINT('Origin',(-0.526159834984027,0.121473569345687,0.55));
#76025=CARTESIAN_POINT('',(-0.490666271247226,0.0961592962762519,0.05));
#76026=CARTESIAN_POINT('',(-0.490666271247226,0.0961592962762519,0.55));
#76027=CARTESIAN_POINT('',(-0.490666271247226,0.0961592962762519,0.29));
#76028=CARTESIAN_POINT('',(-0.47270772144586,0.0833511252801265,0.05));
#76029=CARTESIAN_POINT('',(-0.526159834984027,0.121473569345687,0.05));
#76030=CARTESIAN_POINT('',(-0.47270772144586,0.0833511252801265,0.55));
#76031=CARTESIAN_POINT('',(-0.47270772144586,0.0833511252801265,0.55));
#76032=CARTESIAN_POINT('',(-0.526159834984027,0.121473569345687,0.55));
#76033=CARTESIAN_POINT('Origin',(-0.504341321666087,0.0936415073922334,
0.55));
#76034=CARTESIAN_POINT('',(-0.493963890654054,0.0774575672862877,0.55));
#76035=CARTESIAN_POINT('Origin',(0.,0.,0.55));
#76036=CARTESIAN_POINT('',(-0.47270772144586,0.0833511252801265,0.55));
#76037=CARTESIAN_POINT('Origin',(-0.47270772144586,0.0833511252801265,0.55));
#76038=CARTESIAN_POINT('',(-0.493963890654054,0.0774575672862877,0.05));
#76039=CARTESIAN_POINT('',(-0.493963890654054,0.0774575672862877,0.29));
#76040=CARTESIAN_POINT('',(-0.47270772144586,0.0833511252801265,0.05));
#76041=CARTESIAN_POINT('Origin',(-0.504341321666087,0.0936415073922334,
0.05));
#76042=CARTESIAN_POINT('Origin',(0.,0.,0.05));
#76043=CARTESIAN_POINT('Origin',(-0.452882106690529,0.294105078908115,0.55));
#76044=CARTESIAN_POINT('',(-0.428187058065056,0.258177929547807,0.05));
#76045=CARTESIAN_POINT('',(-0.428187058065056,0.258177929547807,0.55));
#76046=CARTESIAN_POINT('',(-0.428187058065056,0.258177929547807,0.29));
#76047=CARTESIAN_POINT('',(-0.415692193816531,0.24,0.05));
#76048=CARTESIAN_POINT('',(-0.452882106690529,0.294105078908115,0.05));
#76049=CARTESIAN_POINT('',(-0.415692193816531,0.24,0.55));
#76050=CARTESIAN_POINT('',(-0.415692193816531,0.24,0.55));
#76051=CARTESIAN_POINT('',(-0.452882106690529,0.294105078908115,0.55));
#76052=CARTESIAN_POINT('Origin',(-0.448417858439125,0.267052539454057,0.55));
#76053=CARTESIAN_POINT('',(-0.437682174717398,0.241731905082157,0.55));
#76054=CARTESIAN_POINT('Origin',(0.,0.,0.55));
#76055=CARTESIAN_POINT('',(-0.415692193816531,0.24,0.55));
#76056=CARTESIAN_POINT('Origin',(-0.415692193816531,0.24,0.55));
#76057=CARTESIAN_POINT('',(-0.437682174717398,0.241731905082157,0.05));
#76058=CARTESIAN_POINT('',(-0.437682174717398,0.241731905082157,0.29));
#76059=CARTESIAN_POINT('',(-0.415692193816531,0.24,0.05));
#76060=CARTESIAN_POINT('Origin',(-0.448417858439125,0.267052539454057,0.05));
#76061=CARTESIAN_POINT('Origin',(0.,0.,0.05));
#76062=CARTESIAN_POINT('Origin',(-0.324980112502106,0.431263175425538,0.55));
#76063=CARTESIAN_POINT('',(-0.314062166312295,0.389056494215465,0.05));
#76064=CARTESIAN_POINT('',(-0.314062166312295,0.389056494215465,0.55));
#76065=CARTESIAN_POINT('',(-0.314062166312295,0.389056494215465,0.29));
#76066=CARTESIAN_POINT('',(-0.308538052649539,0.367701332697109,0.05));
#76067=CARTESIAN_POINT('',(-0.324980112502106,0.431263175425538,0.05));
#76068=CARTESIAN_POINT('',(-0.308538052649539,0.367701332697109,0.55));
#76069=CARTESIAN_POINT('',(-0.308538052649539,0.367701332697109,0.55));
#76070=CARTESIAN_POINT('',(-0.324980112502106,0.431263175425538,0.55));
#76071=CARTESIAN_POINT('Origin',(-0.338408583541644,0.399482254061324,0.55));
#76072=CARTESIAN_POINT('',(-0.328609529008881,0.376849807542158,0.55));
#76073=CARTESIAN_POINT('Origin',(0.,0.,0.55));
#76074=CARTESIAN_POINT('',(-0.308538052649539,0.367701332697109,0.55));
#76075=CARTESIAN_POINT('Origin',(-0.308538052649539,0.367701332697109,0.55));
#76076=CARTESIAN_POINT('',(-0.328609529008881,0.376849807542158,0.05));
#76077=CARTESIAN_POINT('',(-0.328609529008881,0.376849807542158,0.29));
#76078=CARTESIAN_POINT('',(-0.308538052649539,0.367701332697109,0.05));
#76079=CARTESIAN_POINT('Origin',(-0.338408583541644,0.399482254061324,0.05));
#76080=CARTESIAN_POINT('Origin',(0.,0.,0.05));
#76081=CARTESIAN_POINT('Origin',(-0.157880720550278,0.516404568220039,0.55));
#76082=CARTESIAN_POINT('',(-0.162056742238344,0.473009103818409,0.05));
#76083=CARTESIAN_POINT('',(-0.162056742238344,0.473009103818409,0.55));
#76084=CARTESIAN_POINT('',(-0.162056742238344,0.473009103818409,0.29));
#76085=CARTESIAN_POINT('',(-0.164169668796321,0.451052457977236,0.05));
#76086=CARTESIAN_POINT('',(-0.157880720550278,0.516404568220039,0.05));
#76087=CARTESIAN_POINT('',(-0.164169668796321,0.451052457977236,0.55));
#76088=CARTESIAN_POINT('',(-0.164169668796321,0.451052457977236,0.55));
#76089=CARTESIAN_POINT('',(-0.157880720550278,0.516404568220039,0.55));
#76090=CARTESIAN_POINT('Origin',(-0.184437764967243,0.483728513098638,0.55));
#76091=CARTESIAN_POINT('',(-0.179901724341759,0.466514061501753,0.55));
#76092=CARTESIAN_POINT('Origin',(0.,0.,0.55));
#76093=CARTESIAN_POINT('',(-0.164169668796321,0.451052457977236,0.55));
#76094=CARTESIAN_POINT('Origin',(-0.164169668796321,0.451052457977236,0.55));
#76095=CARTESIAN_POINT('',(-0.179901724341759,0.466514061501753,0.05));
#76096=CARTESIAN_POINT('',(-0.179901724341759,0.466514061501753,0.29));
#76097=CARTESIAN_POINT('',(-0.164169668796321,0.451052457977236,0.05));
#76098=CARTESIAN_POINT('Origin',(-0.184437764967243,0.483728513098638,0.05));
#76099=CARTESIAN_POINT('Origin',(0.,0.,0.05));
#76100=CARTESIAN_POINT('Origin',(0.0282614163711897,0.53925994876747,0.55));
#76101=CARTESIAN_POINT('',(0.00949511665234237,0.499909834629964,0.05));
#76102=CARTESIAN_POINT('',(0.00949511665234237,0.499909834629964,0.55));
#76103=CARTESIAN_POINT('',(0.00949511665234237,0.499909834629964,0.29));
#76104=CARTESIAN_POINT('',(2.93915231795365E-17,0.48,0.05));
#76105=CARTESIAN_POINT('',(0.0282614163711897,0.53925994876747,0.05));
#76106=CARTESIAN_POINT('',(2.93915231795365E-17,0.48,0.55));
#76107=CARTESIAN_POINT('',(2.93915231795365E-17,0.48,0.55));
#76108=CARTESIAN_POINT('',(0.0282614163711897,0.53925994876747,0.55));
#76109=CARTESIAN_POINT('Origin',(3.46944695195361E-17,0.509629974383735,
0.55));
#76110=CARTESIAN_POINT('',(-0.00949511665234229,0.499909834629964,0.55));
#76111=CARTESIAN_POINT('Origin',(0.,0.,0.55));
#76112=CARTESIAN_POINT('',(2.93915231795365E-17,0.48,0.55));
#76113=CARTESIAN_POINT('Origin',(2.93915231795365E-17,0.48,0.55));
#76114=CARTESIAN_POINT('',(-0.00949511665234229,0.499909834629964,0.05));
#76115=CARTESIAN_POINT('',(-0.00949511665234229,0.499909834629964,0.29));
#76116=CARTESIAN_POINT('',(2.93915231795365E-17,0.48,0.05));
#76117=CARTESIAN_POINT('Origin',(3.46944695195361E-17,0.509629974383735,
0.05));
#76118=CARTESIAN_POINT('Origin',(0.,0.,0.05));
#76119=CARTESIAN_POINT('Origin',(0.210994809384208,0.497072620864318,0.55));
#76120=CARTESIAN_POINT('',(0.179901724341759,0.466514061501753,0.05));
#76121=CARTESIAN_POINT('',(0.179901724341759,0.466514061501753,0.55));
#76122=CARTESIAN_POINT('',(0.179901724341759,0.466514061501753,0.29));
#76123=CARTESIAN_POINT('',(0.164169668796321,0.451052457977236,0.05));
#76124=CARTESIAN_POINT('',(0.210994809384208,0.497072620864318,0.05));
#76125=CARTESIAN_POINT('',(0.164169668796321,0.451052457977236,0.55));
#76126=CARTESIAN_POINT('',(0.164169668796321,0.451052457977236,0.55));
#76127=CARTESIAN_POINT('',(0.210994809384208,0.497072620864318,0.55));
#76128=CARTESIAN_POINT('Origin',(0.184437764967243,0.483728513098638,0.55));
#76129=CARTESIAN_POINT('',(0.162056742238344,0.473009103818409,0.55));
#76130=CARTESIAN_POINT('Origin',(0.,0.,0.55));
#76131=CARTESIAN_POINT('',(0.164169668796321,0.451052457977236,0.55));
#76132=CARTESIAN_POINT('Origin',(0.164169668796321,0.451052457977236,0.55));
#76133=CARTESIAN_POINT('',(0.162056742238344,0.473009103818409,0.05));
#76134=CARTESIAN_POINT('',(0.162056742238344,0.473009103818409,0.29));
#76135=CARTESIAN_POINT('',(0.164169668796321,0.451052457977236,0.05));
#76136=CARTESIAN_POINT('Origin',(0.184437764967243,0.483728513098638,0.05));
#76137=CARTESIAN_POINT('Origin',(0.,0.,0.05));
#76138=CARTESIAN_POINT('Origin',(0.368279114433749,0.394930998874352,0.55));
#76139=CARTESIAN_POINT('',(0.328609529008881,0.376849807542157,0.05));
#76140=CARTESIAN_POINT('',(0.328609529008881,0.376849807542157,0.55));
#76141=CARTESIAN_POINT('',(0.328609529008881,0.376849807542157,0.29));
#76142=CARTESIAN_POINT('',(0.308538052649539,0.367701332697109,0.05));
#76143=CARTESIAN_POINT('',(0.368279114433749,0.394930998874352,0.05));
#76144=CARTESIAN_POINT('',(0.308538052649539,0.367701332697109,0.55));
#76145=CARTESIAN_POINT('',(0.308538052649539,0.367701332697109,0.55));
#76146=CARTESIAN_POINT('',(0.368279114433749,0.394930998874352,0.55));
#76147=CARTESIAN_POINT('Origin',(0.338408583541644,0.399482254061324,0.55));
#76148=CARTESIAN_POINT('',(0.314062166312295,0.389056494215466,0.55));
#76149=CARTESIAN_POINT('Origin',(0.,0.,0.55));
#76150=CARTESIAN_POINT('',(0.308538052649539,0.367701332697109,0.55));
#76151=CARTESIAN_POINT('Origin',(0.308538052649539,0.367701332697109,0.55));
#76152=CARTESIAN_POINT('',(0.314062166312295,0.389056494215466,0.05));
#76153=CARTESIAN_POINT('',(0.314062166312295,0.389056494215466,0.29));
#76154=CARTESIAN_POINT('',(0.308538052649539,0.367701332697109,0.05));
#76155=CARTESIAN_POINT('Origin',(0.338408583541644,0.399482254061324,0.05));
#76156=CARTESIAN_POINT('Origin',(0.,0.,0.05));
#76157=CARTESIAN_POINT('Origin',(0.481143523061719,0.245154869859355,0.55));
#76158=CARTESIAN_POINT('',(0.437682174717398,0.241731905082157,0.05));
#76159=CARTESIAN_POINT('',(0.437682174717398,0.241731905082157,0.55));
#76160=CARTESIAN_POINT('',(0.437682174717398,0.241731905082157,0.29));
#76161=CARTESIAN_POINT('',(0.415692193816531,0.24,0.05));
#76162=CARTESIAN_POINT('',(0.481143523061719,0.245154869859355,0.05));
#76163=CARTESIAN_POINT('',(0.415692193816531,0.24,0.55));
#76164=CARTESIAN_POINT('',(0.415692193816531,0.24,0.55));
#76165=CARTESIAN_POINT('',(0.481143523061719,0.245154869859355,0.55));
#76166=CARTESIAN_POINT('Origin',(0.448417858439125,0.267052539454057,0.55));
#76167=CARTESIAN_POINT('',(0.428187058065056,0.258177929547807,0.55));
#76168=CARTESIAN_POINT('Origin',(0.,0.,0.55));
#76169=CARTESIAN_POINT('',(0.415692193816531,0.24,0.55));
#76170=CARTESIAN_POINT('Origin',(0.415692193816531,0.24,0.55));
#76171=CARTESIAN_POINT('',(0.428187058065056,0.258177929547807,0.05));
#76172=CARTESIAN_POINT('',(0.428187058065056,0.258177929547807,0.29));
#76173=CARTESIAN_POINT('',(0.415692193816531,0.24,0.05));
#76174=CARTESIAN_POINT('Origin',(0.448417858439125,0.267052539454057,0.05));
#76175=CARTESIAN_POINT('Origin',(0.,0.,0.05));
#76176=CARTESIAN_POINT('Origin',(0.535974921886314,0.0658094454387796,0.55));
#76177=CARTESIAN_POINT('',(0.493963890654054,0.0774575672862878,0.05));
#76178=CARTESIAN_POINT('',(0.493963890654054,0.0774575672862878,0.55));
#76179=CARTESIAN_POINT('',(0.493963890654054,0.0774575672862878,0.29));
#76180=CARTESIAN_POINT('',(0.47270772144586,0.0833511252801266,0.05));
#76181=CARTESIAN_POINT('',(0.535974921886314,0.0658094454387796,0.05));
#76182=CARTESIAN_POINT('',(0.47270772144586,0.0833511252801266,0.55));
#76183=CARTESIAN_POINT('',(0.47270772144586,0.0833511252801266,0.55));
#76184=CARTESIAN_POINT('',(0.535974921886314,0.0658094454387796,0.55));
#76185=CARTESIAN_POINT('Origin',(0.504341321666087,0.0936415073922334,0.55));
#76186=CARTESIAN_POINT('',(0.490666271247226,0.0961592962762519,0.55));
#76187=CARTESIAN_POINT('Origin',(0.,0.,0.55));
#76188=CARTESIAN_POINT('',(0.47270772144586,0.0833511252801266,0.55));
#76189=CARTESIAN_POINT('Origin',(0.47270772144586,0.0833511252801266,0.55));
#76190=CARTESIAN_POINT('',(0.490666271247226,0.0961592962762519,0.05));
#76191=CARTESIAN_POINT('',(0.490666271247226,0.0961592962762519,0.29));
#76192=CARTESIAN_POINT('',(0.47270772144586,0.0833511252801266,0.05));
#76193=CARTESIAN_POINT('Origin',(0.504341321666087,0.0936415073922334,0.05));
#76194=CARTESIAN_POINT('Origin',(0.,0.,0.05));
#76195=CARTESIAN_POINT('Origin',(0.516404568220039,0.157880720550278,0.55));
#76196=CARTESIAN_POINT('',(0.473009103818409,0.162056742238344,0.05));
#76197=CARTESIAN_POINT('',(0.473009103818409,0.162056742238344,0.55));
#76198=CARTESIAN_POINT('',(0.473009103818409,0.162056742238344,0.29));
#76199=CARTESIAN_POINT('',(0.451052457977236,0.164169668796321,0.05));
#76200=CARTESIAN_POINT('',(0.516404568220039,0.157880720550278,0.05));
#76201=CARTESIAN_POINT('',(0.451052457977236,0.164169668796321,0.55));
#76202=CARTESIAN_POINT('',(0.451052457977236,0.164169668796321,0.55));
#76203=CARTESIAN_POINT('',(0.516404568220039,0.157880720550278,0.55));
#76204=CARTESIAN_POINT('Origin',(0.483728513098638,0.184437764967243,0.55));
#76205=CARTESIAN_POINT('',(0.466514061501753,0.179901724341759,0.55));
#76206=CARTESIAN_POINT('Origin',(0.,0.,0.55));
#76207=CARTESIAN_POINT('',(0.451052457977236,0.164169668796321,0.55));
#76208=CARTESIAN_POINT('Origin',(0.451052457977236,0.164169668796321,0.55));
#76209=CARTESIAN_POINT('',(0.466514061501753,0.179901724341759,0.05));
#76210=CARTESIAN_POINT('',(0.466514061501753,0.179901724341759,0.29));
#76211=CARTESIAN_POINT('',(0.451052457977236,0.164169668796321,0.05));
#76212=CARTESIAN_POINT('Origin',(0.483728513098638,0.184437764967243,0.05));
#76213=CARTESIAN_POINT('Origin',(0.,0.,0.05));
#76214=CARTESIAN_POINT('Origin',(0.431263175425538,0.324980112502106,0.55));
#76215=CARTESIAN_POINT('',(0.389056494215466,0.314062166312295,0.05));
#76216=CARTESIAN_POINT('',(0.389056494215466,0.314062166312295,0.55));
#76217=CARTESIAN_POINT('',(0.389056494215466,0.314062166312295,0.29));
#76218=CARTESIAN_POINT('',(0.367701332697109,0.308538052649539,0.05));
#76219=CARTESIAN_POINT('',(0.431263175425538,0.324980112502106,0.05));
#76220=CARTESIAN_POINT('',(0.367701332697109,0.308538052649539,0.55));
#76221=CARTESIAN_POINT('',(0.367701332697109,0.308538052649539,0.55));
#76222=CARTESIAN_POINT('',(0.431263175425538,0.324980112502106,0.55));
#76223=CARTESIAN_POINT('Origin',(0.399482254061324,0.338408583541644,0.55));
#76224=CARTESIAN_POINT('',(0.376849807542158,0.328609529008881,0.55));
#76225=CARTESIAN_POINT('Origin',(0.,0.,0.55));
#76226=CARTESIAN_POINT('',(0.367701332697109,0.308538052649539,0.55));
#76227=CARTESIAN_POINT('Origin',(0.367701332697109,0.308538052649539,0.55));
#76228=CARTESIAN_POINT('',(0.376849807542158,0.328609529008881,0.05));
#76229=CARTESIAN_POINT('',(0.376849807542158,0.328609529008881,0.29));
#76230=CARTESIAN_POINT('',(0.367701332697109,0.308538052649539,0.05));
#76231=CARTESIAN_POINT('Origin',(0.399482254061324,0.338408583541644,0.05));
#76232=CARTESIAN_POINT('Origin',(0.,0.,0.05));
#76233=CARTESIAN_POINT('Origin',(0.294105078908115,0.452882106690529,0.55));
#76234=CARTESIAN_POINT('',(0.258177929547807,0.428187058065056,0.05));
#76235=CARTESIAN_POINT('',(0.258177929547807,0.428187058065056,0.55));
#76236=CARTESIAN_POINT('',(0.258177929547807,0.428187058065056,0.29));
#76237=CARTESIAN_POINT('',(0.24,0.41569219381653,0.05));
#76238=CARTESIAN_POINT('',(0.294105078908115,0.452882106690529,0.05));
#76239=CARTESIAN_POINT('',(0.24,0.41569219381653,0.55));
#76240=CARTESIAN_POINT('',(0.24,0.41569219381653,0.55));
#76241=CARTESIAN_POINT('',(0.294105078908115,0.452882106690529,0.55));
#76242=CARTESIAN_POINT('Origin',(0.267052539454057,0.448417858439125,0.55));
#76243=CARTESIAN_POINT('',(0.241731905082157,0.437682174717398,0.55));
#76244=CARTESIAN_POINT('Origin',(0.,0.,0.55));
#76245=CARTESIAN_POINT('',(0.24,0.41569219381653,0.55));
#76246=CARTESIAN_POINT('Origin',(0.24,0.41569219381653,0.55));
#76247=CARTESIAN_POINT('',(0.241731905082157,0.437682174717398,0.05));
#76248=CARTESIAN_POINT('',(0.241731905082157,0.437682174717398,0.29));
#76249=CARTESIAN_POINT('',(0.24,0.41569219381653,0.05));
#76250=CARTESIAN_POINT('Origin',(0.267052539454057,0.448417858439125,0.05));
#76251=CARTESIAN_POINT('Origin',(0.,0.,0.05));
#76252=CARTESIAN_POINT('Origin',(0.121473569345687,0.526159834984027,0.55));
#76253=CARTESIAN_POINT('',(0.0961592962762519,0.490666271247226,0.05));
#76254=CARTESIAN_POINT('',(0.0961592962762519,0.490666271247226,0.55));
#76255=CARTESIAN_POINT('',(0.0961592962762519,0.490666271247226,0.29));
#76256=CARTESIAN_POINT('',(0.0833511252801266,0.47270772144586,0.05));
#76257=CARTESIAN_POINT('',(0.121473569345687,0.526159834984027,0.05));
#76258=CARTESIAN_POINT('',(0.0833511252801266,0.47270772144586,0.55));
#76259=CARTESIAN_POINT('',(0.0833511252801266,0.47270772144586,0.55));
#76260=CARTESIAN_POINT('',(0.121473569345687,0.526159834984027,0.55));
#76261=CARTESIAN_POINT('Origin',(0.0936415073922334,0.504341321666087,0.55));
#76262=CARTESIAN_POINT('',(0.0774575672862878,0.493963890654054,0.55));
#76263=CARTESIAN_POINT('Origin',(0.,0.,0.55));
#76264=CARTESIAN_POINT('',(0.0833511252801266,0.47270772144586,0.55));
#76265=CARTESIAN_POINT('Origin',(0.0833511252801266,0.47270772144586,0.55));
#76266=CARTESIAN_POINT('',(0.0774575672862878,0.493963890654054,0.05));
#76267=CARTESIAN_POINT('',(0.0774575672862878,0.493963890654054,0.29));
#76268=CARTESIAN_POINT('',(0.0833511252801266,0.47270772144586,0.05));
#76269=CARTESIAN_POINT('Origin',(0.0936415073922334,0.504341321666087,0.05));
#76270=CARTESIAN_POINT('Origin',(0.,0.,0.05));
#76271=CARTESIAN_POINT('Origin',(-0.0658094454387796,0.535974921886314,
0.55));
#76272=CARTESIAN_POINT('',(-0.0774575672862878,0.493963890654054,0.05));
#76273=CARTESIAN_POINT('',(-0.0774575672862878,0.493963890654054,0.55));
#76274=CARTESIAN_POINT('',(-0.0774575672862878,0.493963890654054,0.29));
#76275=CARTESIAN_POINT('',(-0.0833511252801265,0.47270772144586,0.05));
#76276=CARTESIAN_POINT('',(-0.0658094454387796,0.535974921886314,0.05));
#76277=CARTESIAN_POINT('',(-0.0833511252801265,0.47270772144586,0.55));
#76278=CARTESIAN_POINT('',(-0.0833511252801265,0.47270772144586,0.55));
#76279=CARTESIAN_POINT('',(-0.0658094454387796,0.535974921886314,0.55));
#76280=CARTESIAN_POINT('Origin',(-0.0936415073922333,0.504341321666087,
0.55));
#76281=CARTESIAN_POINT('',(-0.0961592962762518,0.490666271247226,0.55));
#76282=CARTESIAN_POINT('Origin',(0.,0.,0.55));
#76283=CARTESIAN_POINT('',(-0.0833511252801265,0.47270772144586,0.55));
#76284=CARTESIAN_POINT('Origin',(-0.0833511252801265,0.47270772144586,0.55));
#76285=CARTESIAN_POINT('',(-0.0961592962762518,0.490666271247226,0.05));
#76286=CARTESIAN_POINT('',(-0.0961592962762518,0.490666271247226,0.29));
#76287=CARTESIAN_POINT('',(-0.0833511252801265,0.47270772144586,0.05));
#76288=CARTESIAN_POINT('Origin',(-0.0936415073922333,0.504341321666087,
0.05));
#76289=CARTESIAN_POINT('Origin',(0.,0.,0.05));
#76290=CARTESIAN_POINT('Origin',(-0.245154869859355,0.481143523061719,0.55));
#76291=CARTESIAN_POINT('',(-0.241731905082157,0.437682174717398,0.05));
#76292=CARTESIAN_POINT('',(-0.241731905082157,0.437682174717398,0.55));
#76293=CARTESIAN_POINT('',(-0.241731905082157,0.437682174717398,0.29));
#76294=CARTESIAN_POINT('',(-0.24,0.415692193816531,0.05));
#76295=CARTESIAN_POINT('',(-0.245154869859355,0.481143523061719,0.05));
#76296=CARTESIAN_POINT('',(-0.24,0.415692193816531,0.55));
#76297=CARTESIAN_POINT('',(-0.24,0.415692193816531,0.55));
#76298=CARTESIAN_POINT('',(-0.245154869859355,0.481143523061719,0.55));
#76299=CARTESIAN_POINT('Origin',(-0.267052539454057,0.448417858439125,0.55));
#76300=CARTESIAN_POINT('',(-0.258177929547807,0.428187058065056,0.55));
#76301=CARTESIAN_POINT('Origin',(0.,0.,0.55));
#76302=CARTESIAN_POINT('',(-0.24,0.415692193816531,0.55));
#76303=CARTESIAN_POINT('Origin',(-0.24,0.415692193816531,0.55));
#76304=CARTESIAN_POINT('',(-0.258177929547807,0.428187058065056,0.05));
#76305=CARTESIAN_POINT('',(-0.258177929547807,0.428187058065056,0.29));
#76306=CARTESIAN_POINT('',(-0.24,0.415692193816531,0.05));
#76307=CARTESIAN_POINT('Origin',(-0.267052539454057,0.448417858439125,0.05));
#76308=CARTESIAN_POINT('Origin',(0.,0.,0.05));
#76309=CARTESIAN_POINT('Origin',(-0.394930998874352,0.368279114433749,0.55));
#76310=CARTESIAN_POINT('',(-0.376849807542157,0.328609529008881,0.05));
#76311=CARTESIAN_POINT('',(-0.376849807542157,0.328609529008881,0.55));
#76312=CARTESIAN_POINT('',(-0.376849807542157,0.328609529008881,0.29));
#76313=CARTESIAN_POINT('',(-0.367701332697109,0.308538052649539,0.05));
#76314=CARTESIAN_POINT('',(-0.394930998874352,0.368279114433749,0.05));
#76315=CARTESIAN_POINT('',(-0.367701332697109,0.308538052649539,0.55));
#76316=CARTESIAN_POINT('',(-0.367701332697109,0.308538052649539,0.55));
#76317=CARTESIAN_POINT('',(-0.394930998874352,0.368279114433749,0.55));
#76318=CARTESIAN_POINT('Origin',(-0.399482254061324,0.338408583541644,0.55));
#76319=CARTESIAN_POINT('',(-0.389056494215466,0.314062166312295,0.55));
#76320=CARTESIAN_POINT('Origin',(0.,0.,0.55));
#76321=CARTESIAN_POINT('',(-0.367701332697109,0.308538052649539,0.55));
#76322=CARTESIAN_POINT('Origin',(-0.367701332697109,0.308538052649539,0.55));
#76323=CARTESIAN_POINT('',(-0.389056494215466,0.314062166312295,0.05));
#76324=CARTESIAN_POINT('',(-0.389056494215466,0.314062166312295,0.29));
#76325=CARTESIAN_POINT('',(-0.367701332697109,0.308538052649539,0.05));
#76326=CARTESIAN_POINT('Origin',(-0.399482254061324,0.338408583541644,0.05));
#76327=CARTESIAN_POINT('Origin',(0.,0.,0.05));
#76328=CARTESIAN_POINT('Origin',(-0.497072620864318,0.210994809384208,0.55));
#76329=CARTESIAN_POINT('',(-0.466514061501753,0.179901724341759,0.05));
#76330=CARTESIAN_POINT('',(-0.466514061501753,0.179901724341759,0.55));
#76331=CARTESIAN_POINT('',(-0.466514061501753,0.179901724341759,0.29));
#76332=CARTESIAN_POINT('',(-0.451052457977236,0.164169668796321,0.05));
#76333=CARTESIAN_POINT('',(-0.497072620864318,0.210994809384208,0.05));
#76334=CARTESIAN_POINT('',(-0.451052457977236,0.164169668796321,0.55));
#76335=CARTESIAN_POINT('',(-0.451052457977236,0.164169668796321,0.55));
#76336=CARTESIAN_POINT('',(-0.497072620864318,0.210994809384208,0.55));
#76337=CARTESIAN_POINT('Origin',(-0.483728513098638,0.184437764967243,0.55));
#76338=CARTESIAN_POINT('',(-0.473009103818409,0.162056742238344,0.55));
#76339=CARTESIAN_POINT('Origin',(0.,0.,0.55));
#76340=CARTESIAN_POINT('',(-0.451052457977236,0.164169668796321,0.55));
#76341=CARTESIAN_POINT('Origin',(-0.451052457977236,0.164169668796321,0.55));
#76342=CARTESIAN_POINT('',(-0.473009103818409,0.162056742238344,0.05));
#76343=CARTESIAN_POINT('',(-0.473009103818409,0.162056742238344,0.29));
#76344=CARTESIAN_POINT('',(-0.451052457977236,0.164169668796321,0.05));
#76345=CARTESIAN_POINT('Origin',(-0.483728513098638,0.184437764967243,0.05));
#76346=CARTESIAN_POINT('Origin',(0.,0.,0.05));
#76347=CARTESIAN_POINT('Origin',(0.509629974383735,0.,0.55));
#76348=CARTESIAN_POINT('',(0.499909834629964,-0.00949511665234232,0.55));
#76349=CARTESIAN_POINT('',(0.499909834629965,0.00949511665234234,0.55));
#76350=CARTESIAN_POINT('Origin',(0.,0.,0.55));
#76351=CARTESIAN_POINT('',(0.48,0.,0.55));
#76352=CARTESIAN_POINT('',(0.53925994876747,-0.0282614163711897,0.55));
#76353=CARTESIAN_POINT('',(0.48,0.,0.55));
#76354=CARTESIAN_POINT('Origin',(0.53925994876747,-0.0282614163711897,0.55));
#76355=CARTESIAN_POINT('',(0.499909834629964,-0.00949511665234232,0.05));
#76356=CARTESIAN_POINT('',(0.499909834629964,-0.00949511665234232,0.29));
#76357=CARTESIAN_POINT('',(0.48,0.,0.05));
#76358=CARTESIAN_POINT('',(0.53925994876747,-0.0282614163711897,0.05));
#76359=CARTESIAN_POINT('',(0.48,0.,0.55));
#76360=CARTESIAN_POINT('Origin',(0.48,0.,0.55));
#76361=CARTESIAN_POINT('',(0.499909834629965,0.00949511665234234,0.05));
#76362=CARTESIAN_POINT('',(0.499909834629965,0.00949511665234234,0.29));
#76363=CARTESIAN_POINT('',(0.48,0.,0.05));
#76364=CARTESIAN_POINT('Origin',(0.509629974383735,0.,0.05));
#76365=CARTESIAN_POINT('Origin',(0.,0.,0.05));
#76366=CARTESIAN_POINT('Origin',(-0.535974921886314,-0.0658094454387796,
0.55));
#76367=CARTESIAN_POINT('',(-0.493963890654054,-0.0774575672862878,0.05));
#76368=CARTESIAN_POINT('',(-0.493963890654054,-0.0774575672862878,0.55));
#76369=CARTESIAN_POINT('',(-0.493963890654054,-0.0774575672862878,0.29));
#76370=CARTESIAN_POINT('',(-0.47270772144586,-0.0833511252801266,0.05));
#76371=CARTESIAN_POINT('',(-0.535974921886314,-0.0658094454387796,0.05));
#76372=CARTESIAN_POINT('',(-0.47270772144586,-0.0833511252801266,0.55));
#76373=CARTESIAN_POINT('',(-0.47270772144586,-0.0833511252801266,0.55));
#76374=CARTESIAN_POINT('',(-0.535974921886314,-0.0658094454387796,0.55));
#76375=CARTESIAN_POINT('Origin',(-0.504341321666087,-0.0936415073922333,
0.55));
#76376=CARTESIAN_POINT('',(-0.490666271247226,-0.0961592962762519,0.55));
#76377=CARTESIAN_POINT('Origin',(0.,0.,0.55));
#76378=CARTESIAN_POINT('',(-0.47270772144586,-0.0833511252801266,0.55));
#76379=CARTESIAN_POINT('Origin',(-0.47270772144586,-0.0833511252801266,
0.55));
#76380=CARTESIAN_POINT('',(-0.490666271247226,-0.0961592962762519,0.05));
#76381=CARTESIAN_POINT('',(-0.490666271247226,-0.0961592962762519,0.29));
#76382=CARTESIAN_POINT('',(-0.47270772144586,-0.0833511252801266,0.05));
#76383=CARTESIAN_POINT('Origin',(-0.504341321666087,-0.0936415073922333,
0.05));
#76384=CARTESIAN_POINT('Origin',(0.,0.,0.05));
#76385=CARTESIAN_POINT('Origin',(-0.481143523061719,-0.245154869859355,
0.55));
#76386=CARTESIAN_POINT('',(-0.437682174717398,-0.241731905082157,0.05));
#76387=CARTESIAN_POINT('',(-0.437682174717398,-0.241731905082157,0.55));
#76388=CARTESIAN_POINT('',(-0.437682174717398,-0.241731905082157,0.29));
#76389=CARTESIAN_POINT('',(-0.41569219381653,-0.24,0.05));
#76390=CARTESIAN_POINT('',(-0.481143523061719,-0.245154869859355,0.05));
#76391=CARTESIAN_POINT('',(-0.41569219381653,-0.24,0.55));
#76392=CARTESIAN_POINT('',(-0.41569219381653,-0.24,0.55));
#76393=CARTESIAN_POINT('',(-0.481143523061719,-0.245154869859355,0.55));
#76394=CARTESIAN_POINT('Origin',(-0.448417858439125,-0.267052539454057,
0.55));
#76395=CARTESIAN_POINT('',(-0.428187058065056,-0.258177929547807,0.55));
#76396=CARTESIAN_POINT('Origin',(0.,0.,0.55));
#76397=CARTESIAN_POINT('',(-0.41569219381653,-0.24,0.55));
#76398=CARTESIAN_POINT('Origin',(-0.41569219381653,-0.24,0.55));
#76399=CARTESIAN_POINT('',(-0.428187058065056,-0.258177929547807,0.05));
#76400=CARTESIAN_POINT('',(-0.428187058065056,-0.258177929547807,0.29));
#76401=CARTESIAN_POINT('',(-0.41569219381653,-0.24,0.05));
#76402=CARTESIAN_POINT('Origin',(-0.448417858439125,-0.267052539454057,
0.05));
#76403=CARTESIAN_POINT('Origin',(0.,0.,0.05));
#76404=CARTESIAN_POINT('Origin',(-0.368279114433749,-0.394930998874352,
0.55));
#76405=CARTESIAN_POINT('',(-0.328609529008881,-0.376849807542157,0.05));
#76406=CARTESIAN_POINT('',(-0.328609529008881,-0.376849807542157,0.55));
#76407=CARTESIAN_POINT('',(-0.328609529008881,-0.376849807542157,0.29));
#76408=CARTESIAN_POINT('',(-0.308538052649539,-0.367701332697109,0.05));
#76409=CARTESIAN_POINT('',(-0.368279114433749,-0.394930998874352,0.05));
#76410=CARTESIAN_POINT('',(-0.308538052649539,-0.367701332697109,0.55));
#76411=CARTESIAN_POINT('',(-0.308538052649539,-0.367701332697109,0.55));
#76412=CARTESIAN_POINT('',(-0.368279114433749,-0.394930998874352,0.55));
#76413=CARTESIAN_POINT('Origin',(-0.338408583541644,-0.399482254061324,
0.55));
#76414=CARTESIAN_POINT('',(-0.314062166312295,-0.389056494215465,0.55));
#76415=CARTESIAN_POINT('Origin',(0.,0.,0.55));
#76416=CARTESIAN_POINT('',(-0.308538052649539,-0.367701332697109,0.55));
#76417=CARTESIAN_POINT('Origin',(-0.308538052649539,-0.367701332697109,
0.55));
#76418=CARTESIAN_POINT('',(-0.314062166312295,-0.389056494215465,0.05));
#76419=CARTESIAN_POINT('',(-0.314062166312295,-0.389056494215465,0.29));
#76420=CARTESIAN_POINT('',(-0.308538052649539,-0.367701332697109,0.05));
#76421=CARTESIAN_POINT('Origin',(-0.338408583541644,-0.399482254061324,
0.05));
#76422=CARTESIAN_POINT('Origin',(0.,0.,0.05));
#76423=CARTESIAN_POINT('Origin',(-0.210994809384208,-0.497072620864318,
0.55));
#76424=CARTESIAN_POINT('',(-0.179901724341759,-0.466514061501753,0.05));
#76425=CARTESIAN_POINT('',(-0.179901724341759,-0.466514061501753,0.55));
#76426=CARTESIAN_POINT('',(-0.179901724341759,-0.466514061501753,0.29));
#76427=CARTESIAN_POINT('',(-0.164169668796321,-0.451052457977236,0.05));
#76428=CARTESIAN_POINT('',(-0.210994809384208,-0.497072620864318,0.05));
#76429=CARTESIAN_POINT('',(-0.164169668796321,-0.451052457977236,0.55));
#76430=CARTESIAN_POINT('',(-0.164169668796321,-0.451052457977236,0.55));
#76431=CARTESIAN_POINT('',(-0.210994809384208,-0.497072620864318,0.55));
#76432=CARTESIAN_POINT('Origin',(-0.184437764967243,-0.483728513098638,
0.55));
#76433=CARTESIAN_POINT('',(-0.162056742238344,-0.473009103818409,0.55));
#76434=CARTESIAN_POINT('Origin',(0.,0.,0.55));
#76435=CARTESIAN_POINT('',(-0.164169668796321,-0.451052457977236,0.55));
#76436=CARTESIAN_POINT('Origin',(-0.164169668796321,-0.451052457977236,
0.55));
#76437=CARTESIAN_POINT('',(-0.162056742238344,-0.473009103818409,0.05));
#76438=CARTESIAN_POINT('',(-0.162056742238344,-0.473009103818409,0.29));
#76439=CARTESIAN_POINT('',(-0.164169668796321,-0.451052457977236,0.05));
#76440=CARTESIAN_POINT('Origin',(-0.184437764967243,-0.483728513098638,
0.05));
#76441=CARTESIAN_POINT('Origin',(0.,0.,0.05));
#76442=CARTESIAN_POINT('Origin',(-0.0282614163711899,-0.53925994876747,
0.55));
#76443=CARTESIAN_POINT('',(-0.00949511665234243,-0.499909834629964,0.05));
#76444=CARTESIAN_POINT('',(-0.00949511665234243,-0.499909834629964,0.55));
#76445=CARTESIAN_POINT('',(-0.00949511665234243,-0.499909834629964,0.29));
#76446=CARTESIAN_POINT('',(-8.81745695386094E-17,-0.48,0.05));
#76447=CARTESIAN_POINT('',(-0.0282614163711899,-0.53925994876747,0.05));
#76448=CARTESIAN_POINT('',(-8.81745695386094E-17,-0.48,0.55));
#76449=CARTESIAN_POINT('',(-8.81745695386094E-17,-0.48,0.55));
#76450=CARTESIAN_POINT('',(-0.0282614163711899,-0.53925994876747,0.55));
#76451=CARTESIAN_POINT('Origin',(-9.71445146547012E-17,-0.509629974383735,
0.55));
#76452=CARTESIAN_POINT('',(0.00949511665234229,-0.499909834629964,0.55));
#76453=CARTESIAN_POINT('Origin',(0.,0.,0.55));
#76454=CARTESIAN_POINT('',(-8.81745695386094E-17,-0.48,0.55));
#76455=CARTESIAN_POINT('Origin',(-8.81745695386094E-17,-0.48,0.55));
#76456=CARTESIAN_POINT('',(0.00949511665234229,-0.499909834629964,0.05));
#76457=CARTESIAN_POINT('',(0.00949511665234229,-0.499909834629964,0.29));
#76458=CARTESIAN_POINT('',(-8.81745695386094E-17,-0.48,0.05));
#76459=CARTESIAN_POINT('Origin',(-9.71445146547012E-17,-0.509629974383735,
0.05));
#76460=CARTESIAN_POINT('Origin',(0.,0.,0.05));
#76461=CARTESIAN_POINT('Origin',(0.157880720550278,-0.516404568220039,0.55));
#76462=CARTESIAN_POINT('',(0.162056742238344,-0.473009103818409,0.05));
#76463=CARTESIAN_POINT('',(0.162056742238344,-0.473009103818409,0.55));
#76464=CARTESIAN_POINT('',(0.162056742238344,-0.473009103818409,0.29));
#76465=CARTESIAN_POINT('',(0.164169668796321,-0.451052457977236,0.05));
#76466=CARTESIAN_POINT('',(0.157880720550278,-0.516404568220039,0.05));
#76467=CARTESIAN_POINT('',(0.164169668796321,-0.451052457977236,0.55));
#76468=CARTESIAN_POINT('',(0.164169668796321,-0.451052457977236,0.55));
#76469=CARTESIAN_POINT('',(0.157880720550278,-0.516404568220039,0.55));
#76470=CARTESIAN_POINT('Origin',(0.184437764967243,-0.483728513098638,0.55));
#76471=CARTESIAN_POINT('',(0.179901724341759,-0.466514061501753,0.55));
#76472=CARTESIAN_POINT('Origin',(0.,0.,0.55));
#76473=CARTESIAN_POINT('',(0.164169668796321,-0.451052457977236,0.55));
#76474=CARTESIAN_POINT('Origin',(0.164169668796321,-0.451052457977236,0.55));
#76475=CARTESIAN_POINT('',(0.179901724341759,-0.466514061501753,0.05));
#76476=CARTESIAN_POINT('',(0.179901724341759,-0.466514061501753,0.29));
#76477=CARTESIAN_POINT('',(0.164169668796321,-0.451052457977236,0.05));
#76478=CARTESIAN_POINT('Origin',(0.184437764967243,-0.483728513098638,0.05));
#76479=CARTESIAN_POINT('Origin',(0.,0.,0.05));
#76480=CARTESIAN_POINT('Origin',(0.324980112502106,-0.431263175425538,0.55));
#76481=CARTESIAN_POINT('',(0.314062166312295,-0.389056494215466,0.05));
#76482=CARTESIAN_POINT('',(0.314062166312295,-0.389056494215466,0.55));
#76483=CARTESIAN_POINT('',(0.314062166312295,-0.389056494215466,0.29));
#76484=CARTESIAN_POINT('',(0.308538052649539,-0.367701332697109,0.05));
#76485=CARTESIAN_POINT('',(0.324980112502106,-0.431263175425538,0.05));
#76486=CARTESIAN_POINT('',(0.308538052649539,-0.367701332697109,0.55));
#76487=CARTESIAN_POINT('',(0.308538052649539,-0.367701332697109,0.55));
#76488=CARTESIAN_POINT('',(0.324980112502106,-0.431263175425538,0.55));
#76489=CARTESIAN_POINT('Origin',(0.338408583541644,-0.399482254061324,0.55));
#76490=CARTESIAN_POINT('',(0.328609529008881,-0.376849807542158,0.55));
#76491=CARTESIAN_POINT('Origin',(0.,0.,0.55));
#76492=CARTESIAN_POINT('',(0.308538052649539,-0.367701332697109,0.55));
#76493=CARTESIAN_POINT('Origin',(0.308538052649539,-0.367701332697109,0.55));
#76494=CARTESIAN_POINT('',(0.328609529008881,-0.376849807542158,0.05));
#76495=CARTESIAN_POINT('',(0.328609529008881,-0.376849807542158,0.29));
#76496=CARTESIAN_POINT('',(0.308538052649539,-0.367701332697109,0.05));
#76497=CARTESIAN_POINT('Origin',(0.338408583541644,-0.399482254061324,0.05));
#76498=CARTESIAN_POINT('Origin',(0.,0.,0.05));
#76499=CARTESIAN_POINT('Origin',(0.452882106690529,-0.294105078908115,0.55));
#76500=CARTESIAN_POINT('',(0.428187058065056,-0.258177929547807,0.05));
#76501=CARTESIAN_POINT('',(0.428187058065056,-0.258177929547807,0.55));
#76502=CARTESIAN_POINT('',(0.428187058065056,-0.258177929547807,0.29));
#76503=CARTESIAN_POINT('',(0.41569219381653,-0.24,0.05));
#76504=CARTESIAN_POINT('',(0.452882106690529,-0.294105078908115,0.05));
#76505=CARTESIAN_POINT('',(0.41569219381653,-0.24,0.55));
#76506=CARTESIAN_POINT('',(0.41569219381653,-0.24,0.55));
#76507=CARTESIAN_POINT('',(0.452882106690529,-0.294105078908115,0.55));
#76508=CARTESIAN_POINT('Origin',(0.448417858439125,-0.267052539454057,0.55));
#76509=CARTESIAN_POINT('',(0.437682174717398,-0.241731905082157,0.55));
#76510=CARTESIAN_POINT('Origin',(0.,0.,0.55));
#76511=CARTESIAN_POINT('',(0.41569219381653,-0.24,0.55));
#76512=CARTESIAN_POINT('Origin',(0.41569219381653,-0.24,0.55));
#76513=CARTESIAN_POINT('',(0.437682174717398,-0.241731905082157,0.05));
#76514=CARTESIAN_POINT('',(0.437682174717398,-0.241731905082157,0.29));
#76515=CARTESIAN_POINT('',(0.41569219381653,-0.24,0.05));
#76516=CARTESIAN_POINT('Origin',(0.448417858439125,-0.267052539454057,0.05));
#76517=CARTESIAN_POINT('Origin',(0.,0.,0.05));
#76518=CARTESIAN_POINT('Origin',(0.526159834984027,-0.121473569345687,0.55));
#76519=CARTESIAN_POINT('',(0.490666271247226,-0.096159296276252,0.05));
#76520=CARTESIAN_POINT('',(0.490666271247226,-0.096159296276252,0.55));
#76521=CARTESIAN_POINT('',(0.490666271247226,-0.096159296276252,0.29));
#76522=CARTESIAN_POINT('',(0.47270772144586,-0.0833511252801266,0.05));
#76523=CARTESIAN_POINT('',(0.526159834984027,-0.121473569345687,0.05));
#76524=CARTESIAN_POINT('',(0.47270772144586,-0.0833511252801266,0.55));
#76525=CARTESIAN_POINT('',(0.47270772144586,-0.0833511252801266,0.55));
#76526=CARTESIAN_POINT('',(0.526159834984027,-0.121473569345687,0.55));
#76527=CARTESIAN_POINT('Origin',(0.504341321666087,-0.0936415073922334,
0.55));
#76528=CARTESIAN_POINT('',(0.493963890654054,-0.0774575672862878,0.55));
#76529=CARTESIAN_POINT('Origin',(0.,0.,0.55));
#76530=CARTESIAN_POINT('',(0.47270772144586,-0.0833511252801266,0.55));
#76531=CARTESIAN_POINT('Origin',(0.47270772144586,-0.0833511252801266,0.55));
#76532=CARTESIAN_POINT('',(0.493963890654054,-0.0774575672862878,0.05));
#76533=CARTESIAN_POINT('',(0.493963890654054,-0.0774575672862878,0.29));
#76534=CARTESIAN_POINT('',(0.47270772144586,-0.0833511252801266,0.05));
#76535=CARTESIAN_POINT('Origin',(0.504341321666087,-0.0936415073922334,
0.05));
#76536=CARTESIAN_POINT('Origin',(0.,0.,0.05));
#76537=CARTESIAN_POINT('Origin',(0.25,0.,-2.));
#76538=CARTESIAN_POINT('',(-0.25,-3.06161699786838E-17,-2.));
#76539=CARTESIAN_POINT('Origin',(0.,0.,-2.));
#76540=CARTESIAN_POINT('Origin',(0.,0.,-1.975));
#76541=CARTESIAN_POINT('',(-0.275,-3.36777869765522E-17,-1.975));
#76542=CARTESIAN_POINT('Origin',(0.,0.,0.015));
#76543=CARTESIAN_POINT('',(-0.5,-6.12323399573677E-17,0.03));
#76544=CARTESIAN_POINT('Origin',(0.,0.,0.03));
#76545=CARTESIAN_POINT('',(-0.485,-5.93953697586466E-17,0.015));
#76546=CARTESIAN_POINT('Origin',(0.,0.,0.29));
#76547=CARTESIAN_POINT('Origin',(0.,0.,0.55));
#76548=CARTESIAN_POINT('Origin',(0.,0.,0.55));
#76549=CARTESIAN_POINT('Origin',(0.,0.,0.55));
#76550=CARTESIAN_POINT('Origin',(0.,0.,0.55));
#76551=CARTESIAN_POINT('Origin',(0.,0.,0.55));
#76552=CARTESIAN_POINT('Origin',(0.,0.,0.55));
#76553=CARTESIAN_POINT('Origin',(0.,0.,0.55));
#76554=CARTESIAN_POINT('Origin',(0.,0.,0.55));
#76555=CARTESIAN_POINT('Origin',(0.,0.,0.55));
#76556=CARTESIAN_POINT('Origin',(0.,0.,0.55));
#76557=CARTESIAN_POINT('Origin',(0.,0.,0.55));
#76558=CARTESIAN_POINT('Origin',(0.,0.,0.55));
#76559=CARTESIAN_POINT('Origin',(0.,0.,0.55));
#76560=CARTESIAN_POINT('Origin',(0.,0.,0.55));
#76561=CARTESIAN_POINT('Origin',(0.,0.,0.55));
#76562=CARTESIAN_POINT('Origin',(0.,0.,0.55));
#76563=CARTESIAN_POINT('',(-0.5,-6.12323399573677E-17,0.29));
#76564=CARTESIAN_POINT('Origin',(0.,0.,0.55));
#76565=CARTESIAN_POINT('Origin',(0.,0.,0.55));
#76566=CARTESIAN_POINT('Origin',(0.,0.,0.55));
#76567=CARTESIAN_POINT('Origin',(0.,0.,0.55));
#76568=CARTESIAN_POINT('Origin',(0.,0.,0.55));
#76569=CARTESIAN_POINT('Origin',(0.,0.,0.55));
#76570=CARTESIAN_POINT('Origin',(0.,0.,0.55));
#76571=CARTESIAN_POINT('Origin',(0.,0.,0.55));
#76572=CARTESIAN_POINT('Origin',(0.,0.,0.55));
#76573=CARTESIAN_POINT('Origin',(0.,0.,0.55));
#76574=CARTESIAN_POINT('Origin',(0.,0.,0.55));
#76575=CARTESIAN_POINT('Origin',(0.,0.,0.55));
#76576=CARTESIAN_POINT('Origin',(0.,0.,0.55));
#76577=CARTESIAN_POINT('Origin',(0.,0.,0.55));
#76578=CARTESIAN_POINT('Origin',(0.,0.,0.55));
#76579=CARTESIAN_POINT('Origin',(0.,0.,0.55));
#76580=CARTESIAN_POINT('Origin',(0.,0.,0.55));
#76581=CARTESIAN_POINT('Origin',(0.,0.,0.55));
#76582=CARTESIAN_POINT('Origin',(0.,0.,0.55));
#76583=CARTESIAN_POINT('Origin',(0.,0.,0.55));
#76584=CARTESIAN_POINT('Origin',(0.,0.,0.575));
#76585=CARTESIAN_POINT('',(-0.45,-5.51091059616309E-17,0.6));
#76586=CARTESIAN_POINT('Origin',(0.,0.,0.6));
#76587=CARTESIAN_POINT('',(-0.475,-5.81707229594993E-17,0.575));
#76588=CARTESIAN_POINT('Origin',(0.,0.,0.6));
#76637=UNCERTAINTY_MEASURE_WITH_UNIT(LENGTH_MEASURE(0.001),#76661,
'DISTANCE_ACCURACY_VALUE',
'Maximum model space distance between geometric entities at asserted c
onnectivities');
#76638=UNCERTAINTY_MEASURE_WITH_UNIT(LENGTH_MEASURE(0.001),#76661,
'DISTANCE_ACCURACY_VALUE',
'Maximum model space distance between geometric entities at asserted c
onnectivities');
#76659=(
GEOMETRIC_REPRESENTATION_CONTEXT(3)
GLOBAL_UNCERTAINTY_ASSIGNED_CONTEXT((#76637))
GLOBAL_UNIT_ASSIGNED_CONTEXT((#76661,#76663,#76664))
REPRESENTATION_CONTEXT('','3D')
);
#76660=(
GEOMETRIC_REPRESENTATION_CONTEXT(3)
GLOBAL_UNCERTAINTY_ASSIGNED_CONTEXT((#76638))
GLOBAL_UNIT_ASSIGNED_CONTEXT((#76661,#76663,#76664))
REPRESENTATION_CONTEXT('','3D')
);
#76661=(
LENGTH_UNIT()
NAMED_UNIT(*)
SI_UNIT(.CENTI.,.METRE.)
);
#76663=(
NAMED_UNIT(*)
PLANE_ANGLE_UNIT()
SI_UNIT($,.RADIAN.)
);
#76664=(
NAMED_UNIT(*)
SI_UNIT($,.STERADIAN.)
SOLID_ANGLE_UNIT()
);
#76685=SHAPE_DEFINITION_REPRESENTATION(#76706,#76755);
#76706=PRODUCT_DEFINITION_SHAPE('',$,#76777);
#76755=SHAPE_REPRESENTATION('',(#28978),#76659);
#76756=PRODUCT_DEFINITION_CONTEXT('part definition',#76821,'design');
#76777=PRODUCT_DEFINITION('2026-10-26-11-14-00-117',
'20_Rear_Cap_Screw_ISO_4762_M6x20',#76798,#76756);
#76798=PRODUCT_DEFINITION_FORMATION('',$,#76843);
#76821=APPLICATION_CONTEXT(
'Core Data for Automotive Mechanical Design Process');
#76822=PRODUCT_CONTEXT('part definition',#76821,'mechanical');
#76843=PRODUCT('2026-10-26-11-14-00-117',
'20_Rear_Cap_Screw_ISO_4762_M6x20',$,(#76822));
#76907=COLOUR_RGB('Black',0.12,0.14,0.17);
#76908=FILL_AREA_STYLE_COLOUR('',#76907);
#76909=FILL_AREA_STYLE('',(#76908));
#76910=SURFACE_STYLE_FILL_AREA(#76909);
#76911=SURFACE_SIDE_STYLE('',(#76910));
#76912=SURFACE_STYLE_USAGE(.BOTH.,#76911);
#76913=PRESENTATION_STYLE_ASSIGNMENT((#76912));
ENDSEC;
END-ISO-10303-21;
